ISO-10303-21;
HEADER;
/* Generated by software containing ST-Developer
 * from STEP Tools, Inc. (www.steptools.com) 
 */
/* OPTION: using custom renumber hook */

FILE_DESCRIPTION(
/* description */ ('STEP AP242 Edition 2', 'CAx-IF Rec.Pracs.---Representation and Presentation of Product Manufa
cturing Information (PMI)---4.0---2014-10-13', 'CAx-IF Rec.Pracs.---3D Tessellated Geometry---0.4---2014-09-14', '2;1', 'CAx-IF Rec.Pracs.---User Defined Attributes---1.5---2016-08-15'),
/* implementation_level */ '2;1');

FILE_NAME(
/* name */ 'Bottle.step',
/* time_stamp */ '2026-10-08T12:15:07Z',
/* author */ (''),
/* organization */ (''),
/* preprocessor_version */ 'ST-DEVELOPER v20',
/* originating_system */ 'ONSHAPE BY PTC INC, 1.221',
/* authorisation */ '  ');

FILE_SCHEMA (('AP242_MANAGED_MODEL_BASED_3D_ENGINEERING_MIM_LF { 1 0 10303 442 3 1 4 }'));
ENDSEC;

DATA;
#30=CONICAL_SURFACE('',#14962,0.05,0.723351005491207);
#221=SHAPE_REPRESENTATION_RELATIONSHIP('','',#13795,#248);
#248=ADVANCED_BREP_SHAPE_REPRESENTATION('',(#13739),#45485);
#321=TOROIDAL_SURFACE('',#14977,0.04,0.01);
#322=TOROIDAL_SURFACE('',#14978,0.02,0.001);
#323=TOROIDAL_SURFACE('',#14979,0.0188,0.0002);
#324=TOROIDAL_SURFACE('',#14980,0.0123,0.0002);
#325=TOROIDAL_SURFACE('',#14982,0.0123,0.0002);
#326=TOROIDAL_SURFACE('',#14985,0.012,0.001);
#327=TOROIDAL_SURFACE('',#14986,0.012,0.004);
#328=TOROIDAL_SURFACE('',#14987,0.019,0.003);
#329=TOROIDAL_SURFACE('',#14988,0.047,0.003);
#330=TOROIDAL_SURFACE('',#14989,0.043,0.01);
#848=CIRCLE('',#14849,0.05);
#849=CIRCLE('',#14850,0.053);
#850=CIRCLE('',#14852,0.005);
#851=CIRCLE('',#14853,0.005);
#852=CIRCLE('',#14855,0.001397);
#853=CIRCLE('',#14856,0.003);
#854=CIRCLE('',#14857,0.003);
#855=CIRCLE('',#14858,0.005);
#856=CIRCLE('',#14859,0.05);
#857=CIRCLE('',#14861,0.005);
#858=CIRCLE('',#14863,0.001397);
#859=CIRCLE('',#14864,0.003);
#860=CIRCLE('',#14865,0.05);
#861=CIRCLE('',#14866,0.003);
#862=CIRCLE('',#14868,0.001397);
#863=CIRCLE('',#14869,0.003);
#864=CIRCLE('',#14870,0.003);
#865=CIRCLE('',#14871,0.005);
#866=CIRCLE('',#14872,0.05);
#867=CIRCLE('',#14873,0.005);
#868=CIRCLE('',#14875,0.005);
#869=CIRCLE('',#14877,0.001397);
#870=CIRCLE('',#14878,0.003);
#871=CIRCLE('',#14879,0.005);
#872=CIRCLE('',#14880,0.05);
#873=CIRCLE('',#14881,0.003);
#874=CIRCLE('',#14884,0.001397);
#875=CIRCLE('',#14885,0.003);
#876=CIRCLE('',#14886,0.003);
#877=CIRCLE('',#14887,0.005);
#878=CIRCLE('',#14888,0.05);
#879=CIRCLE('',#14889,0.005);
#880=CIRCLE('',#14891,0.001397);
#881=CIRCLE('',#14892,0.003);
#882=CIRCLE('',#14893,0.005);
#883=CIRCLE('',#14894,0.05);
#884=CIRCLE('',#14895,0.005);
#885=CIRCLE('',#14896,0.003);
#886=CIRCLE('',#14898,0.001397);
#887=CIRCLE('',#14899,0.003);
#888=CIRCLE('',#14900,0.003);
#889=CIRCLE('',#14901,0.005);
#890=CIRCLE('',#14902,0.05);
#891=CIRCLE('',#14903,0.005);
#892=CIRCLE('',#14905,0.005);
#893=CIRCLE('',#14907,0.001397);
#894=CIRCLE('',#14908,0.003);
#895=CIRCLE('',#14909,0.005);
#896=CIRCLE('',#14910,0.05);
#897=CIRCLE('',#14911,0.003);
#898=CIRCLE('',#14934,0.043);
#899=CIRCLE('',#14939,0.01);
#900=CIRCLE('',#14940,0.012);
#901=CIRCLE('',#14942,0.000202360810977542);
#902=CIRCLE('',#14944,0.0002);
#903=CIRCLE('',#14946,0.001);
#904=CIRCLE('',#14948,0.001);
#905=CIRCLE('',#14950,0.04);
#906=CIRCLE('',#14952,0.0188);
#907=CIRCLE('',#14953,0.0123);
#908=CIRCLE('',#14955,0.013);
#909=CIRCLE('',#14956,0.047);
#910=CIRCLE('',#14957,0.019);
#911=CIRCLE('',#14959,0.0441317460907982);
#912=CIRCLE('',#14960,0.01);
#913=CIRCLE('',#14961,0.02);
#914=CIRCLE('',#14963,0.05);
#915=CIRCLE('',#14966,0.019);
#916=CIRCLE('',#14967,0.019);
#917=CIRCLE('',#14969,0.0121);
#918=CIRCLE('',#14970,0.0121);
#919=CIRCLE('',#14972,0.016);
#920=CIRCLE('',#14973,0.016);
#921=CIRCLE('',#14975,0.05);
#922=CIRCLE('',#14976,0.05);
#923=CIRCLE('',#14981,0.0122857142857138);
#924=CIRCLE('',#14984,0.013);
#925=CIRCLE('',#14990,0.053);
#1110=B_SPLINE_CURVE_WITH_KNOTS('',3,(#37214,#37215,#37216,#37217),
 .UNSPECIFIED.,.F.,.F.,(4,4),(0.,1.),.UNSPECIFIED.);
#1111=B_SPLINE_CURVE_WITH_KNOTS('',3,(#37220,#37221,#37222,#37223,#37224,
#37225,#37226,#37227,#37228,#37229,#37230,#37231,#37232,#37233,#37234,#37235,
#37236,#37237,#37238,#37239,#37240,#37241,#37242,#37243,#37244,#37245,#37246,
#37247,#37248,#37249,#37250,#37251,#37252,#37253,#37254,#37255,#37256,#37257,
#37258,#37259,#37260,#37261,#37262,#37263,#37264,#37265,#37266,#37267,#37268,
#37269,#37270,#37271,#37272,#37273,#37274,#37275,#37276,#37277,#37278,#37279,
#37280,#37281,#37282,#37283,#37284,#37285,#37286,#37287,#37288,#37289,#37290,
#37291,#37292,#37293,#37294,#37295,#37296,#37297,#37298,#37299,#37300,#37301,
#37302,#37303,#37304,#37305,#37306,#37307,#37308,#37309,#37310,#37311,#37312,
#37313,#37314,#37315,#37316,#37317,#37318,#37319,#37320,#37321,#37322,#37323,
#37324,#37325,#37326,#37327,#37328,#37329,#37330,#37331,#37332,#37333),
 .UNSPECIFIED.,.F.,.F.,(4,1,1,1,1,1,1,1,1,1,1,1,1,1,1,1,1,1,1,1,1,1,1,1,
1,1,1,1,1,1,1,1,1,1,1,1,1,1,1,1,1,1,1,1,1,1,1,1,1,1,1,1,1,1,1,1,1,1,1,1,
1,1,1,1,1,1,1,1,1,1,1,1,1,1,1,1,1,1,1,1,1,1,1,1,1,1,1,1,1,1,1,1,1,1,1,1,
1,1,1,1,1,1,1,1,1,1,1,1,1,1,1,4),(0.,0.0078125,0.015625,0.0234375,0.03125,
0.046875,0.0546875,0.0625,0.0703125,0.078125,0.0859375,0.09375,0.109375,
0.1171875,0.125,0.1328125,0.140625,0.1484375,0.15625,0.171875,0.1796875,
0.1875,0.1953125,0.203125,0.2109375,0.21875,0.234375,0.2421875,0.25,0.2578125,
0.265625,0.2734375,0.28125,0.296875,0.3046875,0.3125,0.3203125,0.328125,
0.3359375,0.34375,0.359375,0.3671875,0.375,0.3828125,0.390625,0.3984375,
0.40625,0.421875,0.4296875,0.4375,0.4453125,0.453125,0.4609375,0.46875,
0.484375,0.4921875,0.5,0.515625,0.5234375,0.53125,0.546875,0.5546875,0.5625,
0.5703125,0.578125,0.5859375,0.59375,0.609375,0.6171875,0.625,0.6328125,
0.640625,0.6484375,0.65625,0.671875,0.6796875,0.6875,0.6953125,0.703125,
0.7109375,0.71875,0.734375,0.7421875,0.75,0.7578125,0.765625,0.7734375,
0.78125,0.796875,0.8046875,0.8125,0.8203125,0.828125,0.8359375,0.84375,
0.859375,0.8671875,0.875,0.8828125,0.890625,0.8984375,0.90625,0.921875,
0.9296875,0.9375,0.9453125,0.953125,0.9609375,0.96875,0.984375,0.9921875,
1.),.UNSPECIFIED.);
#1112=B_SPLINE_CURVE_WITH_KNOTS('',3,(#37335,#37336,#37337,#37338),
 .UNSPECIFIED.,.F.,.F.,(4,4),(0.,1.),.UNSPECIFIED.);
#1113=B_SPLINE_CURVE_WITH_KNOTS('',3,(#37340,#37341,#37342,#37343,#37344),
 .UNSPECIFIED.,.F.,.F.,(4,1,4),(3.80821390671777E-7,0.500000190410695,1.),
 .UNSPECIFIED.);
#1114=B_SPLINE_CURVE_WITH_KNOTS('',3,(#37346,#37347,#37348,#37349,#37350),
 .UNSPECIFIED.,.F.,.F.,(4,1,4),(0.,0.5,1.),.UNSPECIFIED.);
#1115=B_SPLINE_CURVE_WITH_KNOTS('',3,(#37352,#37353,#37354,#37355,#37356,
#37357,#37358,#37359,#37360,#37361,#37362),.UNSPECIFIED.,.F.,.F.,(4,1,1,
1,1,1,1,1,4),(0.,0.125,0.25,0.375,0.5,0.625,0.75,0.875,1.),
 .UNSPECIFIED.);
#1116=B_SPLINE_CURVE_WITH_KNOTS('',3,(#37364,#37365,#37366,#37367,#37368,
#37369,#37370,#37371,#37372,#37373,#37374),.UNSPECIFIED.,.F.,.F.,(4,1,1,
1,1,1,1,1,4),(0.,0.125,0.25,0.375,0.5,0.625,0.75,0.875,1.),
 .UNSPECIFIED.);
#1117=B_SPLINE_CURVE_WITH_KNOTS('',3,(#37376,#37377,#37378,#37379,#37380,
#37381,#37382,#37383,#37384,#37385,#37386),.UNSPECIFIED.,.F.,.F.,(4,1,1,
1,1,1,1,1,4),(0.,0.125,0.25,0.375,0.5,0.625,0.75,0.875,1.),
 .UNSPECIFIED.);
#1118=B_SPLINE_CURVE_WITH_KNOTS('',3,(#37388,#37389,#37390,#37391,#37392,
#37393,#37394,#37395,#37396,#37397,#37398),.UNSPECIFIED.,.F.,.F.,(4,1,1,
1,1,1,1,1,4),(0.,0.125,0.25,0.375,0.5,0.625,0.75,0.875,1.),
 .UNSPECIFIED.);
#1119=B_SPLINE_CURVE_WITH_KNOTS('',3,(#37400,#37401,#37402,#37403,#37404,
#37405,#37406,#37407,#37408,#37409,#37410),.UNSPECIFIED.,.F.,.F.,(4,1,1,
1,1,1,1,1,4),(0.,0.125,0.25,0.375,0.5,0.625,0.75,0.875,1.),
 .UNSPECIFIED.);
#1120=B_SPLINE_CURVE_WITH_KNOTS('',3,(#37412,#37413,#37414,#37415,#37416,
#37417,#37418),.UNSPECIFIED.,.F.,.F.,(4,1,1,1,4),(0.,0.25,0.5,0.75,1.),
 .UNSPECIFIED.);
#1121=B_SPLINE_CURVE_WITH_KNOTS('',3,(#37420,#37421,#37422,#37423,#37424),
 .UNSPECIFIED.,.F.,.F.,(4,1,4),(0.,0.499999802342316,0.999999604684632),
 .UNSPECIFIED.);
#1122=B_SPLINE_CURVE_WITH_KNOTS('',3,(#37426,#37427,#37428,#37429,#37430),
 .UNSPECIFIED.,.F.,.F.,(4,1,4),(0.,0.49999980888236,0.99999961776472),
 .UNSPECIFIED.);
#1123=B_SPLINE_CURVE_WITH_KNOTS('',3,(#37433,#37434,#37435,#37436),
 .UNSPECIFIED.,.F.,.F.,(4,4),(1.04486053410473E-7,0.999999895529088),
 .UNSPECIFIED.);
#1124=B_SPLINE_CURVE_WITH_KNOTS('',3,(#37437,#37438,#37439,#37440),
 .UNSPECIFIED.,.F.,.F.,(4,4),(0.,1.),.UNSPECIFIED.);
#1125=B_SPLINE_CURVE_WITH_KNOTS('',3,(#37442,#37443,#37444,#37445),
 .UNSPECIFIED.,.F.,.F.,(4,4),(0.,0.999999872405437),.UNSPECIFIED.);
#1126=B_SPLINE_CURVE_WITH_KNOTS('',3,(#37449,#37450,#37451,#37452),
 .UNSPECIFIED.,.F.,.F.,(4,4),(1.27661041249407E-7,0.999999872030063),
 .UNSPECIFIED.);
#1127=B_SPLINE_CURVE_WITH_KNOTS('',3,(#37455,#37456,#37457,#37458),
 .UNSPECIFIED.,.F.,.F.,(4,4),(0.,1.),.UNSPECIFIED.);
#1128=B_SPLINE_CURVE_WITH_KNOTS('',3,(#37459,#37460,#37461,#37462),
 .UNSPECIFIED.,.F.,.F.,(4,4),(1.14719167408304E-7,1.),.UNSPECIFIED.);
#1129=B_SPLINE_CURVE_WITH_KNOTS('',3,(#37464,#37465,#37466,#37467),
 .UNSPECIFIED.,.F.,.F.,(4,4),(0.,1.),.UNSPECIFIED.);
#1130=B_SPLINE_CURVE_WITH_KNOTS('',3,(#37469,#37470,#37471,#37472),
 .UNSPECIFIED.,.F.,.F.,(4,4),(0.,1.),.UNSPECIFIED.);
#1131=B_SPLINE_CURVE_WITH_KNOTS('',3,(#37474,#37475,#37476,#37477),
 .UNSPECIFIED.,.F.,.F.,(4,4),(0.,1.),.UNSPECIFIED.);
#1132=B_SPLINE_CURVE_WITH_KNOTS('',3,(#38519,#38520,#38521,#38522,#38523,
#38524,#38525),.UNSPECIFIED.,.F.,.F.,(4,1,1,1,4),(0.,0.25,0.5,0.75,1.),
 .UNSPECIFIED.);
#1133=B_SPLINE_CURVE_WITH_KNOTS('',3,(#38527,#38528,#38529,#38530,#38531,
#38532,#38533,#38534,#38535,#38536,#38537),.UNSPECIFIED.,.F.,.F.,(4,1,1,
1,1,1,1,1,4),(0.,0.125,0.25,0.375,0.5,0.625,0.75,0.875,1.),
 .UNSPECIFIED.);
#1134=B_SPLINE_CURVE_WITH_KNOTS('',3,(#38539,#38540,#38541,#38542,#38543,
#38544,#38545,#38546,#38547,#38548,#38549),.UNSPECIFIED.,.F.,.F.,(4,1,1,
1,1,1,1,1,4),(0.,0.125,0.25,0.375,0.5,0.625,0.75,0.875,1.),
 .UNSPECIFIED.);
#1135=B_SPLINE_CURVE_WITH_KNOTS('',3,(#38551,#38552,#38553,#38554,#38555,
#38556,#38557,#38558,#38559,#38560,#38561),.UNSPECIFIED.,.F.,.F.,(4,1,1,
1,1,1,1,1,4),(0.,0.125,0.25,0.375,0.5,0.625,0.75,0.875,1.),
 .UNSPECIFIED.);
#1136=B_SPLINE_CURVE_WITH_KNOTS('',3,(#38563,#38564,#38565,#38566,#38567,
#38568,#38569,#38570,#38571,#38572,#38573),.UNSPECIFIED.,.F.,.F.,(4,1,1,
1,1,1,1,1,4),(0.,0.125,0.25,0.375,0.5,0.625,0.75,0.875,1.),
 .UNSPECIFIED.);
#1137=B_SPLINE_CURVE_WITH_KNOTS('',3,(#38575,#38576,#38577,#38578,#38579,
#38580,#38581,#38582,#38583,#38584,#38585),.UNSPECIFIED.,.F.,.F.,(4,1,1,
1,1,1,1,1,4),(0.,0.125,0.25,0.375,0.5,0.625,0.75,0.875,1.),
 .UNSPECIFIED.);
#1138=B_SPLINE_CURVE_WITH_KNOTS('',3,(#38587,#38588,#38589,#38590,#38591),
 .UNSPECIFIED.,.F.,.F.,(4,1,4),(0.,0.5,1.),.UNSPECIFIED.);
#1139=B_SPLINE_CURVE_WITH_KNOTS('',3,(#38592,#38593,#38594,#38595),
 .UNSPECIFIED.,.F.,.F.,(4,4),(0.,1.),.UNSPECIFIED.);
#1140=B_SPLINE_CURVE_WITH_KNOTS('',3,(#38597,#38598,#38599,#38600,#38601,
#38602,#38603,#38604,#38605,#38606,#38607,#38608,#38609,#38610,#38611,#38612,
#38613,#38614,#38615,#38616,#38617,#38618,#38619,#38620,#38621,#38622,#38623,
#38624,#38625,#38626,#38627,#38628,#38629,#38630,#38631,#38632,#38633,#38634,
#38635,#38636,#38637,#38638,#38639,#38640,#38641,#38642,#38643,#38644,#38645,
#38646,#38647,#38648,#38649,#38650,#38651,#38652,#38653,#38654,#38655,#38656,
#38657,#38658,#38659,#38660,#38661,#38662,#38663,#38664,#38665,#38666,#38667,
#38668,#38669,#38670,#38671,#38672,#38673,#38674,#38675,#38676,#38677,#38678,
#38679,#38680,#38681,#38682,#38683,#38684,#38685,#38686,#38687,#38688,#38689,
#38690,#38691,#38692,#38693,#38694,#38695,#38696,#38697,#38698,#38699,#38700,
#38701,#38702,#38703,#38704,#38705,#38706),.UNSPECIFIED.,.F.,.F.,(4,1,1,
1,1,1,1,1,1,1,1,1,1,1,1,1,1,1,1,1,1,1,1,1,1,1,1,1,1,1,1,1,1,1,1,1,1,1,1,
1,1,1,1,1,1,1,1,1,1,1,1,1,1,1,1,1,1,1,1,1,1,1,1,1,1,1,1,1,1,1,1,1,1,1,1,
1,1,1,1,1,1,1,1,1,1,1,1,1,1,1,1,1,1,1,1,1,1,1,1,1,1,1,1,1,1,1,1,4),(0.,
0.03125,0.046875,0.0546875,0.0625,0.0703125,0.078125,0.0859375,0.09375,
0.1015625,0.109375,0.1171875,0.125,0.1328125,0.140625,0.15625,0.1640625,
0.171875,0.1796875,0.1875,0.203125,0.2109375,0.21875,0.2265625,0.234375,
0.2421875,0.25,0.265625,0.2734375,0.28125,0.2890625,0.296875,0.3125,0.3203125,
0.328125,0.3359375,0.34375,0.3515625,0.359375,0.375,0.3828125,0.390625,
0.3984375,0.40625,0.421875,0.4296875,0.4375,0.4453125,0.453125,0.4609375,
0.46875,0.4765625,0.484375,0.4921875,0.5,0.515625,0.5234375,0.53125,0.546875,
0.5546875,0.5625,0.5703125,0.578125,0.59375,0.6015625,0.609375,0.6171875,
0.625,0.6328125,0.640625,0.6484375,0.65625,0.6640625,0.671875,0.6796875,
0.6875,0.703125,0.7109375,0.71875,0.7265625,0.734375,0.7421875,0.75,0.7578125,
0.765625,0.7734375,0.78125,0.7890625,0.796875,0.8125,0.8203125,0.828125,
0.8359375,0.84375,0.859375,0.8671875,0.875,0.8828125,0.890625,0.8984375,
0.90625,0.921875,0.9296875,0.9375,0.9453125,0.953125,0.96875,1.),
 .UNSPECIFIED.);
#1141=B_SPLINE_CURVE_WITH_KNOTS('',3,(#38719,#38720,#38721,#38722),
 .UNSPECIFIED.,.F.,.F.,(4,4),(0.,1.),.UNSPECIFIED.);
#1142=B_SPLINE_CURVE_WITH_KNOTS('',3,(#38724,#38725,#38726,#38727,#38728,
#38729),.UNSPECIFIED.,.F.,.F.,(4,1,1,4),(0.,0.25,0.5,1.),.UNSPECIFIED.);
#1143=B_SPLINE_CURVE_WITH_KNOTS('',3,(#38760,#38761,#38762,#38763),
 .UNSPECIFIED.,.F.,.F.,(4,4),(0.,1.),.UNSPECIFIED.);
#1144=B_SPLINE_CURVE_WITH_KNOTS('',3,(#38764,#38765,#38766,#38767,#38768),
 .UNSPECIFIED.,.F.,.F.,(4,1,4),(0.,0.5,1.),.UNSPECIFIED.);
#1145=B_SPLINE_CURVE_WITH_KNOTS('',3,(#38798,#38799,#38800,#38801,#38802,
#38803,#38804),.UNSPECIFIED.,.F.,.F.,(4,1,1,1,4),(0.,0.00242728027803591,
0.00485456055607181,0.00728184083410772,0.00970912111214362),
 .UNSPECIFIED.);
#1146=B_SPLINE_CURVE_WITH_KNOTS('',3,(#39435,#39436,#39437,#39438,#39439,
#39440,#39441),.UNSPECIFIED.,.F.,.F.,(4,1,1,1,4),(0.,0.00298225036522322,
0.00596450073044643,0.00894675109566965,0.0119290014608929),
 .UNSPECIFIED.);
#1433=PLANE('',#14848);
#1434=PLANE('',#14854);
#1435=PLANE('',#14862);
#1436=PLANE('',#14867);
#1437=PLANE('',#14876);
#1438=PLANE('',#14883);
#1439=PLANE('',#14890);
#1440=PLANE('',#14897);
#1441=PLANE('',#14906);
#1442=PLANE('',#14913);
#1443=PLANE('',#14915);
#1444=PLANE('',#14917);
#1445=PLANE('',#14919);
#1446=PLANE('',#14921);
#1447=PLANE('',#14922);
#1448=PLANE('',#14924);
#1449=PLANE('',#14926);
#1450=PLANE('',#14927);
#1451=PLANE('',#14929);
#1452=PLANE('',#14931);
#1453=PLANE('',#14932);
#1454=PLANE('',#14933);
#1455=PLANE('',#14936);
#1456=PLANE('',#14937);
#1457=PLANE('',#14938);
#1458=PLANE('',#14945);
#1459=PLANE('',#14947);
#1460=PLANE('',#14949);
#1461=PLANE('',#14951);
#1462=PLANE('',#14954);
#1463=PLANE('',#14958);
#1736=CYLINDRICAL_SURFACE('',#14851,0.005);
#1737=CYLINDRICAL_SURFACE('',#14860,0.005);
#1738=CYLINDRICAL_SURFACE('',#14874,0.005);
#1739=CYLINDRICAL_SURFACE('',#14882,0.005);
#1740=CYLINDRICAL_SURFACE('',#14904,0.005);
#1741=CYLINDRICAL_SURFACE('',#14912,0.005);
#1742=CYLINDRICAL_SURFACE('',#14914,0.003);
#1743=CYLINDRICAL_SURFACE('',#14916,0.003);
#1744=CYLINDRICAL_SURFACE('',#14918,0.003);
#1745=CYLINDRICAL_SURFACE('',#14920,0.003);
#1746=CYLINDRICAL_SURFACE('',#14923,0.003);
#1747=CYLINDRICAL_SURFACE('',#14925,0.003);
#1748=CYLINDRICAL_SURFACE('',#14928,0.003);
#1749=CYLINDRICAL_SURFACE('',#14930,0.003);
#1750=CYLINDRICAL_SURFACE('',#14935,0.0108118988125);
#1751=CYLINDRICAL_SURFACE('',#14941,0.000199965309748703);
#1752=CYLINDRICAL_SURFACE('',#14943,0.000199947311632309);
#1753=CYLINDRICAL_SURFACE('',#14964,0.01);
#1754=CYLINDRICAL_SURFACE('',#14965,0.019);
#1755=CYLINDRICAL_SURFACE('',#14968,0.0121);
#1756=CYLINDRICAL_SURFACE('',#14971,0.016);
#1757=CYLINDRICAL_SURFACE('',#14974,0.05);
#1758=CYLINDRICAL_SURFACE('',#14983,0.013);
#1759=CYLINDRICAL_SURFACE('',#14991,0.001397);
#1760=CYLINDRICAL_SURFACE('',#14992,0.001397);
#1761=CYLINDRICAL_SURFACE('',#14993,0.001397);
#1762=CYLINDRICAL_SURFACE('',#14994,0.001397);
#1763=CYLINDRICAL_SURFACE('',#14995,0.053);
#1764=CYLINDRICAL_SURFACE('',#14996,0.005);
#1765=CYLINDRICAL_SURFACE('',#14997,0.005);
#1766=CYLINDRICAL_SURFACE('',#14998,0.05);
#1911=(
BOUNDED_CURVE()
B_SPLINE_CURVE(2,(#35726,#35727,#35728,#35729,#35730,#35731,#35732,#35733,
#35734),.UNSPECIFIED.,.F.,.F.)
B_SPLINE_CURVE_WITH_KNOTS((3,2,2,2,3),(0.,0.03125,0.0625,0.09375,0.125),
 .UNSPECIFIED.)
CURVE()
GEOMETRIC_REPRESENTATION_ITEM()
RATIONAL_B_SPLINE_CURVE((1.,0.923879532511287,1.,0.923879532511287,1.,0.923879532511287,
1.,0.923879532511287,1.))
REPRESENTATION_ITEM('')
);
#1912=(
BOUNDED_CURVE()
B_SPLINE_CURVE(2,(#35736,#35737,#35738,#35739,#35740,#35741,#35742,#35743,
#35744),.UNSPECIFIED.,.F.,.F.)
B_SPLINE_CURVE_WITH_KNOTS((3,2,2,2,3),(0.125,0.15625,0.1875,0.21875,0.25),
 .UNSPECIFIED.)
CURVE()
GEOMETRIC_REPRESENTATION_ITEM()
RATIONAL_B_SPLINE_CURVE((1.,0.923879532511287,1.,0.923879532511287,1.,0.923879532511287,
1.,0.923879532511286,1.))
REPRESENTATION_ITEM('')
);
#1913=(
BOUNDED_CURVE()
B_SPLINE_CURVE(2,(#35746,#35747,#35748,#35749,#35750,#35751,#35752,#35753,
#35754),.UNSPECIFIED.,.F.,.F.)
B_SPLINE_CURVE_WITH_KNOTS((3,2,2,2,3),(0.25,0.28125,0.3125,0.34375,0.375),
 .UNSPECIFIED.)
CURVE()
GEOMETRIC_REPRESENTATION_ITEM()
RATIONAL_B_SPLINE_CURVE((1.,0.923879532511287,1.,0.923879532511287,1.,0.923879532511287,
1.,0.923879532511288,1.))
REPRESENTATION_ITEM('')
);
#1914=(
BOUNDED_CURVE()
B_SPLINE_CURVE(2,(#35756,#35757,#35758,#35759,#35760,#35761,#35762,#35763,
#35764),.UNSPECIFIED.,.F.,.F.)
B_SPLINE_CURVE_WITH_KNOTS((3,2,2,2,3),(0.375,0.40625,0.4375,0.46875,0.5),
 .UNSPECIFIED.)
CURVE()
GEOMETRIC_REPRESENTATION_ITEM()
RATIONAL_B_SPLINE_CURVE((1.,0.923879532511286,1.,0.923879532511287,1.,0.923879532511287,
1.,0.923879532511287,1.))
REPRESENTATION_ITEM('')
);
#1915=(
BOUNDED_CURVE()
B_SPLINE_CURVE(2,(#35766,#35767,#35768,#35769,#35770,#35771,#35772,#35773,
#35774),.UNSPECIFIED.,.F.,.F.)
B_SPLINE_CURVE_WITH_KNOTS((3,2,2,2,3),(0.5,0.53125,0.5625,0.59375,0.625),
 .UNSPECIFIED.)
CURVE()
GEOMETRIC_REPRESENTATION_ITEM()
RATIONAL_B_SPLINE_CURVE((1.,0.923879532511286,1.,0.923879532511287,1.,0.923879532511287,
1.,0.923879532511287,1.))
REPRESENTATION_ITEM('')
);
#1916=(
BOUNDED_CURVE()
B_SPLINE_CURVE(2,(#35776,#35777,#35778,#35779,#35780,#35781,#35782,#35783,
#35784),.UNSPECIFIED.,.F.,.F.)
B_SPLINE_CURVE_WITH_KNOTS((3,2,2,2,3),(0.625,0.65625,0.6875,0.71875,0.75),
 .UNSPECIFIED.)
CURVE()
GEOMETRIC_REPRESENTATION_ITEM()
RATIONAL_B_SPLINE_CURVE((1.,0.923879532511287,1.,0.923879532511287,1.,0.923879532511287,
1.,0.923879532511287,1.))
REPRESENTATION_ITEM('')
);
#1917=(
BOUNDED_CURVE()
B_SPLINE_CURVE(2,(#35786,#35787,#35788,#35789,#35790,#35791,#35792,#35793,
#35794),.UNSPECIFIED.,.F.,.F.)
B_SPLINE_CURVE_WITH_KNOTS((3,2,2,2,3),(0.75,0.78125,0.8125,0.84375,0.875),
 .UNSPECIFIED.)
CURVE()
GEOMETRIC_REPRESENTATION_ITEM()
RATIONAL_B_SPLINE_CURVE((1.,0.923879532511287,1.,0.923879532511287,1.,0.923879532511287,
1.,0.923879532511287,1.))
REPRESENTATION_ITEM('')
);
#1918=(
BOUNDED_CURVE()
B_SPLINE_CURVE(2,(#35796,#35797,#35798,#35799,#35800,#35801,#35802,#35803,
#35804),.UNSPECIFIED.,.F.,.F.)
B_SPLINE_CURVE_WITH_KNOTS((3,2,2,2,3),(0.875,0.90625,0.9375,0.96875,1.),
 .UNSPECIFIED.)
CURVE()
GEOMETRIC_REPRESENTATION_ITEM()
RATIONAL_B_SPLINE_CURVE((1.,0.923879532511287,1.,0.923879532511287,1.,0.923879532511287,
1.,0.923879532511287,1.))
REPRESENTATION_ITEM('')
);
#1919=(
BOUNDED_CURVE()
B_SPLINE_CURVE(2,(#35808,#35809,#35810,#35811,#35812,#35813,#35814,#35815,
#35816,#35817,#35818,#35819,#35820,#35821,#35822,#35823,#35824,#35825,#35826,
#35827,#35828,#35829,#35830,#35831,#35832,#35833,#35834,#35835,#35836,#35837,
#35838,#35839,#35840,#35841,#35842,#35843,#35844,#35845,#35846,#35847,#35848,
#35849,#35850,#35851,#35852,#35853,#35854,#35855,#35856,#35857,#35858,#35859,
#35860,#35861,#35862,#35863,#35864,#35865,#35866,#35867,#35868,#35869,#35870,
#35871,#35872),.UNSPECIFIED.,.F.,.F.)
B_SPLINE_CURVE_WITH_KNOTS((3,2,2,2,2,2,2,2,2,2,2,2,2,2,2,2,2,2,2,2,2,2,
2,2,2,2,2,2,2,2,2,2,3),(0.,0.03125,0.0625,0.09375,0.125,0.15625,0.1875,
0.21875,0.25,0.28125,0.3125,0.34375,0.375,0.40625,0.4375,0.46875,0.5,0.53125,
0.5625,0.59375,0.625,0.65625,0.6875,0.71875,0.75,0.78125,0.8125,0.84375,
0.875,0.90625,0.9375,0.96875,1.),.UNSPECIFIED.)
CURVE()
GEOMETRIC_REPRESENTATION_ITEM()
RATIONAL_B_SPLINE_CURVE((1.,0.923879532511287,1.,0.923879532511287,1.,0.923879532511287,
1.,0.923879532511287,1.,0.923879532511287,1.,0.923879532511287,1.,0.923879532511287,
1.,0.923879532511287,1.,0.923879532511287,1.,0.923879532511287,1.,0.923879532511287,
1.,0.923879532511287,1.,0.923879532511287,1.,0.923879532511287,1.,0.923879532511287,
1.,0.923879532511287,1.,0.923879532511287,1.,0.923879532511287,1.,0.923879532511287,
1.,0.923879532511287,1.,0.923879532511287,1.,0.923879532511287,1.,0.923879532511287,
1.,0.923879532511287,1.,0.923879532511287,1.,0.923879532511287,1.,0.923879532511287,
1.,0.923879532511287,1.,0.923879532511287,1.,0.923879532511287,1.,0.923879532511287,
1.,0.923879532511287,1.))
REPRESENTATION_ITEM('')
);
#1920=(
BOUNDED_CURVE()
B_SPLINE_CURVE(2,(#36006,#36007,#36008,#36009,#36010,#36011,#36012,#36013,
#36014,#36015,#36016,#36017,#36018,#36019,#36020,#36021,#36022,#36023,#36024,
#36025,#36026,#36027,#36028,#36029,#36030,#36031,#36032,#36033,#36034,#36035,
#36036,#36037,#36038,#36039,#36040,#36041,#36042,#36043,#36044,#36045,#36046,
#36047,#36048,#36049,#36050,#36051,#36052,#36053,#36054,#36055,#36056,#36057,
#36058,#36059,#36060,#36061,#36062,#36063,#36064,#36065,#36066,#36067,#36068,
#36069,#36070),.UNSPECIFIED.,.F.,.F.)
B_SPLINE_CURVE_WITH_KNOTS((3,2,2,2,2,2,2,2,2,2,2,2,2,2,2,2,2,2,2,2,2,2,
2,2,2,2,2,2,2,2,2,2,3),(0.,0.03125,0.0625,0.09375,0.125,0.15625,0.1875,
0.21875,0.25,0.28125,0.3125,0.34375,0.375,0.40625,0.4375,0.46875,0.5,0.53125,
0.5625,0.59375,0.625,0.65625,0.6875,0.71875,0.75,0.78125,0.8125,0.84375,
0.875,0.90625,0.9375,0.96875,1.),.UNSPECIFIED.)
CURVE()
GEOMETRIC_REPRESENTATION_ITEM()
RATIONAL_B_SPLINE_CURVE((1.,0.923879532511287,1.,0.923879532511287,1.,0.923879532511287,
1.,0.923879532511287,1.,0.923879532511287,1.,0.923879532511287,1.,0.923879532511287,
1.,0.923879532511287,1.,0.923879532511287,1.,0.923879532511287,1.,0.923879532511287,
1.,0.923879532511287,1.,0.923879532511287,1.,0.923879532511287,1.,0.923879532511287,
1.,0.923879532511287,1.,0.923879532511287,1.,0.923879532511287,1.,0.923879532511287,
1.,0.923879532511287,1.,0.923879532511287,1.,0.923879532511287,1.,0.923879532511287,
1.,0.923879532511287,1.,0.923879532511287,1.,0.923879532511287,1.,0.923879532511287,
1.,0.923879532511287,1.,0.923879532511287,1.,0.923879532511287,1.,0.923879532511287,
1.,0.923879532511287,1.))
REPRESENTATION_ITEM('')
);
#1921=(
BOUNDED_CURVE()
B_SPLINE_CURVE(2,(#36074,#36075,#36076,#36077,#36078,#36079,#36080,#36081,
#36082),.UNSPECIFIED.,.F.,.F.)
B_SPLINE_CURVE_WITH_KNOTS((3,2,2,2,3),(0.875,0.90625,0.9375,0.96875,1.),
 .UNSPECIFIED.)
CURVE()
GEOMETRIC_REPRESENTATION_ITEM()
RATIONAL_B_SPLINE_CURVE((1.,0.923879532511287,1.,0.923879532511287,1.,0.923879532511287,
1.,0.923879532511287,1.))
REPRESENTATION_ITEM('')
);
#1922=(
BOUNDED_CURVE()
B_SPLINE_CURVE(2,(#36084,#36085,#36086,#36087,#36088,#36089,#36090,#36091,
#36092),.UNSPECIFIED.,.F.,.F.)
B_SPLINE_CURVE_WITH_KNOTS((3,2,2,2,3),(0.75,0.78125,0.8125,0.84375,0.875),
 .UNSPECIFIED.)
CURVE()
GEOMETRIC_REPRESENTATION_ITEM()
RATIONAL_B_SPLINE_CURVE((1.,0.923879532511287,1.,0.923879532511287,1.,0.923879532511287,
1.,0.923879532511287,1.))
REPRESENTATION_ITEM('')
);
#1923=(
BOUNDED_CURVE()
B_SPLINE_CURVE(2,(#36094,#36095,#36096,#36097,#36098,#36099,#36100,#36101,
#36102),.UNSPECIFIED.,.F.,.F.)
B_SPLINE_CURVE_WITH_KNOTS((3,2,2,2,3),(0.625,0.65625,0.6875,0.71875,0.75),
 .UNSPECIFIED.)
CURVE()
GEOMETRIC_REPRESENTATION_ITEM()
RATIONAL_B_SPLINE_CURVE((1.,0.923879532511287,1.,0.923879532511287,1.,0.923879532511287,
1.,0.923879532511287,1.))
REPRESENTATION_ITEM('')
);
#1924=(
BOUNDED_CURVE()
B_SPLINE_CURVE(2,(#36104,#36105,#36106,#36107,#36108,#36109,#36110,#36111,
#36112),.UNSPECIFIED.,.F.,.F.)
B_SPLINE_CURVE_WITH_KNOTS((3,2,2,2,3),(0.5,0.53125,0.5625,0.59375,0.625),
 .UNSPECIFIED.)
CURVE()
GEOMETRIC_REPRESENTATION_ITEM()
RATIONAL_B_SPLINE_CURVE((1.,0.923879532511286,1.,0.923879532511287,1.,0.923879532511287,
1.,0.923879532511287,1.))
REPRESENTATION_ITEM('')
);
#1925=(
BOUNDED_CURVE()
B_SPLINE_CURVE(2,(#36114,#36115,#36116,#36117,#36118,#36119,#36120,#36121,
#36122),.UNSPECIFIED.,.F.,.F.)
B_SPLINE_CURVE_WITH_KNOTS((3,2,2,2,3),(0.375,0.40625,0.4375,0.46875,0.5),
 .UNSPECIFIED.)
CURVE()
GEOMETRIC_REPRESENTATION_ITEM()
RATIONAL_B_SPLINE_CURVE((1.,0.923879532511287,1.,0.923879532511287,1.,0.923879532511287,
1.,0.923879532511287,1.))
REPRESENTATION_ITEM('')
);
#1926=(
BOUNDED_CURVE()
B_SPLINE_CURVE(2,(#36124,#36125,#36126,#36127,#36128,#36129,#36130,#36131,
#36132),.UNSPECIFIED.,.F.,.F.)
B_SPLINE_CURVE_WITH_KNOTS((3,2,2,2,3),(0.25,0.28125,0.3125,0.34375,0.375),
 .UNSPECIFIED.)
CURVE()
GEOMETRIC_REPRESENTATION_ITEM()
RATIONAL_B_SPLINE_CURVE((1.,0.923879532511287,1.,0.923879532511287,1.,0.923879532511287,
1.,0.923879532511286,1.))
REPRESENTATION_ITEM('')
);
#1927=(
BOUNDED_CURVE()
B_SPLINE_CURVE(2,(#36134,#36135,#36136,#36137,#36138,#36139,#36140,#36141,
#36142),.UNSPECIFIED.,.F.,.F.)
B_SPLINE_CURVE_WITH_KNOTS((3,2,2,2,3),(0.125,0.15625,0.1875,0.21875,0.25),
 .UNSPECIFIED.)
CURVE()
GEOMETRIC_REPRESENTATION_ITEM()
RATIONAL_B_SPLINE_CURVE((1.,0.923879532511287,1.,0.923879532511287,1.,0.923879532511287,
1.,0.923879532511286,1.))
REPRESENTATION_ITEM('')
);
#1928=(
BOUNDED_CURVE()
B_SPLINE_CURVE(2,(#36144,#36145,#36146,#36147,#36148,#36149,#36150,#36151,
#36152),.UNSPECIFIED.,.F.,.F.)
B_SPLINE_CURVE_WITH_KNOTS((3,2,2,2,3),(0.,0.03125,0.0625,0.09375,0.125),
 .UNSPECIFIED.)
CURVE()
GEOMETRIC_REPRESENTATION_ITEM()
RATIONAL_B_SPLINE_CURVE((1.,0.923879532511287,1.,0.923879532511287,1.,0.923879532511287,
1.,0.923879532511287,1.))
REPRESENTATION_ITEM('')
);
#4362=ORIENTED_EDGE('',*,*,#6828,.F.);
#4363=ORIENTED_EDGE('',*,*,#6829,.T.);
#4364=ORIENTED_EDGE('',*,*,#6830,.F.);
#4365=ORIENTED_EDGE('',*,*,#6831,.F.);
#4366=ORIENTED_EDGE('',*,*,#6832,.F.);
#4367=ORIENTED_EDGE('',*,*,#6833,.F.);
#4368=ORIENTED_EDGE('',*,*,#6834,.T.);
#4369=ORIENTED_EDGE('',*,*,#6835,.F.);
#4370=ORIENTED_EDGE('',*,*,#6836,.T.);
#4371=ORIENTED_EDGE('',*,*,#6837,.F.);
#4372=ORIENTED_EDGE('',*,*,#6838,.F.);
#4373=ORIENTED_EDGE('',*,*,#6839,.T.);
#4374=ORIENTED_EDGE('',*,*,#6840,.F.);
#4375=ORIENTED_EDGE('',*,*,#6832,.T.);
#4376=ORIENTED_EDGE('',*,*,#6841,.T.);
#4377=ORIENTED_EDGE('',*,*,#6842,.F.);
#4378=ORIENTED_EDGE('',*,*,#6843,.F.);
#4379=ORIENTED_EDGE('',*,*,#6839,.F.);
#4380=ORIENTED_EDGE('',*,*,#6844,.F.);
#4381=ORIENTED_EDGE('',*,*,#6845,.F.);
#4382=ORIENTED_EDGE('',*,*,#6846,.T.);
#4383=ORIENTED_EDGE('',*,*,#6847,.F.);
#4384=ORIENTED_EDGE('',*,*,#6830,.T.);
#4385=ORIENTED_EDGE('',*,*,#6848,.T.);
#4386=ORIENTED_EDGE('',*,*,#6842,.T.);
#4387=ORIENTED_EDGE('',*,*,#6849,.T.);
#4388=ORIENTED_EDGE('',*,*,#6850,.T.);
#4389=ORIENTED_EDGE('',*,*,#6851,.F.);
#4390=ORIENTED_EDGE('',*,*,#6852,.T.);
#4391=ORIENTED_EDGE('',*,*,#6853,.F.);
#4392=ORIENTED_EDGE('',*,*,#6854,.T.);
#4393=ORIENTED_EDGE('',*,*,#6855,.F.);
#4394=ORIENTED_EDGE('',*,*,#6856,.F.);
#4395=ORIENTED_EDGE('',*,*,#6857,.T.);
#4396=ORIENTED_EDGE('',*,*,#6858,.F.);
#4397=ORIENTED_EDGE('',*,*,#6859,.T.);
#4398=ORIENTED_EDGE('',*,*,#6860,.T.);
#4399=ORIENTED_EDGE('',*,*,#6861,.F.);
#4400=ORIENTED_EDGE('',*,*,#6862,.F.);
#4401=ORIENTED_EDGE('',*,*,#6857,.F.);
#4402=ORIENTED_EDGE('',*,*,#6863,.F.);
#4403=ORIENTED_EDGE('',*,*,#6864,.F.);
#4404=ORIENTED_EDGE('',*,*,#6865,.T.);
#4405=ORIENTED_EDGE('',*,*,#6866,.F.);
#4406=ORIENTED_EDGE('',*,*,#6867,.T.);
#4407=ORIENTED_EDGE('',*,*,#6868,.T.);
#4408=ORIENTED_EDGE('',*,*,#6861,.T.);
#4409=ORIENTED_EDGE('',*,*,#6869,.T.);
#4410=ORIENTED_EDGE('',*,*,#6870,.T.);
#4411=ORIENTED_EDGE('',*,*,#6871,.F.);
#4412=ORIENTED_EDGE('',*,*,#6867,.F.);
#4413=ORIENTED_EDGE('',*,*,#6872,.F.);
#4414=ORIENTED_EDGE('',*,*,#6859,.F.);
#4415=ORIENTED_EDGE('',*,*,#6873,.F.);
#4416=ORIENTED_EDGE('',*,*,#6874,.T.);
#4417=ORIENTED_EDGE('',*,*,#6875,.F.);
#4418=ORIENTED_EDGE('',*,*,#6876,.T.);
#4419=ORIENTED_EDGE('',*,*,#6877,.F.);
#4420=ORIENTED_EDGE('',*,*,#6878,.F.);
#4421=ORIENTED_EDGE('',*,*,#6879,.T.);
#4422=ORIENTED_EDGE('',*,*,#6880,.F.);
#4423=ORIENTED_EDGE('',*,*,#6881,.T.);
#4424=ORIENTED_EDGE('',*,*,#6882,.T.);
#4425=ORIENTED_EDGE('',*,*,#6883,.F.);
#4426=ORIENTED_EDGE('',*,*,#6884,.T.);
#4427=ORIENTED_EDGE('',*,*,#6885,.F.);
#4428=ORIENTED_EDGE('',*,*,#6886,.T.);
#4429=ORIENTED_EDGE('',*,*,#6887,.T.);
#4430=ORIENTED_EDGE('',*,*,#6888,.T.);
#4431=ORIENTED_EDGE('',*,*,#6889,.T.);
#4432=ORIENTED_EDGE('',*,*,#6890,.T.);
#4433=ORIENTED_EDGE('',*,*,#6891,.F.);
#4434=ORIENTED_EDGE('',*,*,#6892,.T.);
#4435=ORIENTED_EDGE('',*,*,#6893,.F.);
#4436=ORIENTED_EDGE('',*,*,#6894,.T.);
#4437=ORIENTED_EDGE('',*,*,#6895,.F.);
#4438=ORIENTED_EDGE('',*,*,#6896,.F.);
#4439=ORIENTED_EDGE('',*,*,#6897,.T.);
#4440=ORIENTED_EDGE('',*,*,#6898,.F.);
#4441=ORIENTED_EDGE('',*,*,#6899,.T.);
#4442=ORIENTED_EDGE('',*,*,#6900,.T.);
#4443=ORIENTED_EDGE('',*,*,#6901,.F.);
#4444=ORIENTED_EDGE('',*,*,#6902,.F.);
#4445=ORIENTED_EDGE('',*,*,#6897,.F.);
#4446=ORIENTED_EDGE('',*,*,#6903,.F.);
#4447=ORIENTED_EDGE('',*,*,#6904,.F.);
#4448=ORIENTED_EDGE('',*,*,#6905,.T.);
#4449=ORIENTED_EDGE('',*,*,#6906,.F.);
#4450=ORIENTED_EDGE('',*,*,#6907,.T.);
#4451=ORIENTED_EDGE('',*,*,#6908,.T.);
#4452=ORIENTED_EDGE('',*,*,#6901,.T.);
#4453=ORIENTED_EDGE('',*,*,#6909,.T.);
#4454=ORIENTED_EDGE('',*,*,#6910,.T.);
#4455=ORIENTED_EDGE('',*,*,#6911,.F.);
#4456=ORIENTED_EDGE('',*,*,#6907,.F.);
#4457=ORIENTED_EDGE('',*,*,#6912,.F.);
#4458=ORIENTED_EDGE('',*,*,#6899,.F.);
#4459=ORIENTED_EDGE('',*,*,#6913,.F.);
#4460=ORIENTED_EDGE('',*,*,#6841,.F.);
#4461=ORIENTED_EDGE('',*,*,#6831,.T.);
#4462=ORIENTED_EDGE('',*,*,#6847,.T.);
#4463=ORIENTED_EDGE('',*,*,#6914,.T.);
#4464=ORIENTED_EDGE('',*,*,#6835,.T.);
#4465=ORIENTED_EDGE('',*,*,#6914,.F.);
#4466=ORIENTED_EDGE('',*,*,#6846,.F.);
#4467=ORIENTED_EDGE('',*,*,#6915,.T.);
#4468=ORIENTED_EDGE('',*,*,#6836,.F.);
#4469=ORIENTED_EDGE('',*,*,#6915,.F.);
#4470=ORIENTED_EDGE('',*,*,#6851,.T.);
#4471=ORIENTED_EDGE('',*,*,#6916,.T.);
#4472=ORIENTED_EDGE('',*,*,#6837,.T.);
#4473=ORIENTED_EDGE('',*,*,#6916,.F.);
#4474=ORIENTED_EDGE('',*,*,#6850,.F.);
#4475=ORIENTED_EDGE('',*,*,#6917,.T.);
#4476=ORIENTED_EDGE('',*,*,#6849,.F.);
#4477=ORIENTED_EDGE('',*,*,#6844,.T.);
#4478=ORIENTED_EDGE('',*,*,#6838,.T.);
#4479=ORIENTED_EDGE('',*,*,#6917,.F.);
#4480=ORIENTED_EDGE('',*,*,#6853,.T.);
#4481=ORIENTED_EDGE('',*,*,#6918,.F.);
#4482=ORIENTED_EDGE('',*,*,#6865,.F.);
#4483=ORIENTED_EDGE('',*,*,#6919,.T.);
#4484=ORIENTED_EDGE('',*,*,#6854,.F.);
#4485=ORIENTED_EDGE('',*,*,#6919,.F.);
#4486=ORIENTED_EDGE('',*,*,#6871,.T.);
#4487=ORIENTED_EDGE('',*,*,#6920,.T.);
#4488=ORIENTED_EDGE('',*,*,#6855,.T.);
#4489=ORIENTED_EDGE('',*,*,#6920,.F.);
#4490=ORIENTED_EDGE('',*,*,#6870,.F.);
#4491=ORIENTED_EDGE('',*,*,#6921,.T.);
#4492=ORIENTED_EDGE('',*,*,#6869,.F.);
#4493=ORIENTED_EDGE('',*,*,#6863,.T.);
#4494=ORIENTED_EDGE('',*,*,#6856,.T.);
#4495=ORIENTED_EDGE('',*,*,#6921,.F.);
#4496=ORIENTED_EDGE('',*,*,#6860,.F.);
#4497=ORIENTED_EDGE('',*,*,#6872,.T.);
#4498=ORIENTED_EDGE('',*,*,#6866,.T.);
#4499=ORIENTED_EDGE('',*,*,#6918,.T.);
#4500=ORIENTED_EDGE('',*,*,#6875,.T.);
#4501=ORIENTED_EDGE('',*,*,#6922,.F.);
#4502=ORIENTED_EDGE('',*,*,#6884,.F.);
#4503=ORIENTED_EDGE('',*,*,#6923,.T.);
#4504=ORIENTED_EDGE('',*,*,#6876,.F.);
#4505=ORIENTED_EDGE('',*,*,#6923,.F.);
#4506=ORIENTED_EDGE('',*,*,#6891,.T.);
#4507=ORIENTED_EDGE('',*,*,#6924,.T.);
#4508=ORIENTED_EDGE('',*,*,#6877,.T.);
#4509=ORIENTED_EDGE('',*,*,#6924,.F.);
#4510=ORIENTED_EDGE('',*,*,#6890,.F.);
#4511=ORIENTED_EDGE('',*,*,#6925,.T.);
#4512=ORIENTED_EDGE('',*,*,#6889,.F.);
#4513=ORIENTED_EDGE('',*,*,#6926,.T.);
#4514=ORIENTED_EDGE('',*,*,#6878,.T.);
#4515=ORIENTED_EDGE('',*,*,#6925,.F.);
#4516=ORIENTED_EDGE('',*,*,#6882,.F.);
#4517=ORIENTED_EDGE('',*,*,#6927,.T.);
#4518=ORIENTED_EDGE('',*,*,#6885,.T.);
#4519=ORIENTED_EDGE('',*,*,#6922,.T.);
#4520=ORIENTED_EDGE('',*,*,#6893,.T.);
#4521=ORIENTED_EDGE('',*,*,#6928,.F.);
#4522=ORIENTED_EDGE('',*,*,#6905,.F.);
#4523=ORIENTED_EDGE('',*,*,#6929,.T.);
#4524=ORIENTED_EDGE('',*,*,#6894,.F.);
#4525=ORIENTED_EDGE('',*,*,#6929,.F.);
#4526=ORIENTED_EDGE('',*,*,#6911,.T.);
#4527=ORIENTED_EDGE('',*,*,#6930,.T.);
#4528=ORIENTED_EDGE('',*,*,#6895,.T.);
#4529=ORIENTED_EDGE('',*,*,#6930,.F.);
#4530=ORIENTED_EDGE('',*,*,#6910,.F.);
#4531=ORIENTED_EDGE('',*,*,#6931,.T.);
#4532=ORIENTED_EDGE('',*,*,#6909,.F.);
#4533=ORIENTED_EDGE('',*,*,#6903,.T.);
#4534=ORIENTED_EDGE('',*,*,#6896,.T.);
#4535=ORIENTED_EDGE('',*,*,#6931,.F.);
#4536=ORIENTED_EDGE('',*,*,#6900,.F.);
#4537=ORIENTED_EDGE('',*,*,#6912,.T.);
#4538=ORIENTED_EDGE('',*,*,#6906,.T.);
#4539=ORIENTED_EDGE('',*,*,#6928,.T.);
#4540=ORIENTED_EDGE('',*,*,#6932,.T.);
#4541=ORIENTED_EDGE('',*,*,#6933,.T.);
#4542=ORIENTED_EDGE('',*,*,#6934,.T.);
#4543=ORIENTED_EDGE('',*,*,#6935,.T.);
#4544=ORIENTED_EDGE('',*,*,#6936,.T.);
#4545=ORIENTED_EDGE('',*,*,#6937,.T.);
#4546=ORIENTED_EDGE('',*,*,#6938,.T.);
#4547=ORIENTED_EDGE('',*,*,#6939,.T.);
#4548=ORIENTED_EDGE('',*,*,#6940,.T.);
#4549=ORIENTED_EDGE('',*,*,#6941,.T.);
#4550=ORIENTED_EDGE('',*,*,#6942,.T.);
#4551=ORIENTED_EDGE('',*,*,#6943,.F.);
#4552=ORIENTED_EDGE('',*,*,#6944,.T.);
#4553=ORIENTED_EDGE('',*,*,#6945,.T.);
#4554=ORIENTED_EDGE('',*,*,#6946,.T.);
#4555=ORIENTED_EDGE('',*,*,#6947,.F.);
#4556=ORIENTED_EDGE('',*,*,#6948,.F.);
#4557=ORIENTED_EDGE('',*,*,#6949,.F.);
#4558=ORIENTED_EDGE('',*,*,#6950,.F.);
#4559=ORIENTED_EDGE('',*,*,#6951,.F.);
#4560=ORIENTED_EDGE('',*,*,#6952,.F.);
#4561=ORIENTED_EDGE('',*,*,#6953,.F.);
#4562=ORIENTED_EDGE('',*,*,#6954,.F.);
#4563=ORIENTED_EDGE('',*,*,#6955,.T.);
#4564=ORIENTED_EDGE('',*,*,#6943,.T.);
#4565=ORIENTED_EDGE('',*,*,#6956,.T.);
#4566=ORIENTED_EDGE('',*,*,#6945,.F.);
#4567=ORIENTED_EDGE('',*,*,#6956,.F.);
#4568=ORIENTED_EDGE('',*,*,#6942,.F.);
#4569=ORIENTED_EDGE('',*,*,#6957,.F.);
#4570=ORIENTED_EDGE('',*,*,#6946,.F.);
#4571=ORIENTED_EDGE('',*,*,#6955,.F.);
#4572=ORIENTED_EDGE('',*,*,#6944,.F.);
#4573=ORIENTED_EDGE('',*,*,#6958,.F.);
#4574=ORIENTED_EDGE('',*,*,#6933,.F.);
#4575=ORIENTED_EDGE('',*,*,#6959,.F.);
#4576=ORIENTED_EDGE('',*,*,#6960,.T.);
#4577=ORIENTED_EDGE('',*,*,#6961,.F.);
#4578=ORIENTED_EDGE('',*,*,#6962,.F.);
#4579=ORIENTED_EDGE('',*,*,#6963,.F.);
#4580=ORIENTED_EDGE('',*,*,#6964,.T.);
#4581=ORIENTED_EDGE('',*,*,#6965,.F.);
#4582=ORIENTED_EDGE('',*,*,#6966,.F.);
#4583=ORIENTED_EDGE('',*,*,#6967,.F.);
#4584=ORIENTED_EDGE('',*,*,#6968,.F.);
#4585=ORIENTED_EDGE('',*,*,#6969,.F.);
#4586=ORIENTED_EDGE('',*,*,#6970,.F.);
#4587=ORIENTED_EDGE('',*,*,#6971,.F.);
#4588=ORIENTED_EDGE('',*,*,#6972,.T.);
#4589=ORIENTED_EDGE('',*,*,#6973,.T.);
#4590=ORIENTED_EDGE('',*,*,#6974,.F.);
#4591=ORIENTED_EDGE('',*,*,#6964,.F.);
#4592=ORIENTED_EDGE('',*,*,#6975,.F.);
#4593=ORIENTED_EDGE('',*,*,#6976,.F.);
#4594=ORIENTED_EDGE('',*,*,#6977,.F.);
#4595=ORIENTED_EDGE('',*,*,#6978,.F.);
#4596=ORIENTED_EDGE('',*,*,#6979,.F.);
#4597=ORIENTED_EDGE('',*,*,#6972,.F.);
#4598=ORIENTED_EDGE('',*,*,#6980,.F.);
#4599=ORIENTED_EDGE('',*,*,#6981,.T.);
#4600=ORIENTED_EDGE('',*,*,#6982,.T.);
#4601=ORIENTED_EDGE('',*,*,#6983,.F.);
#4602=ORIENTED_EDGE('',*,*,#6984,.T.);
#4603=ORIENTED_EDGE('',*,*,#6985,.F.);
#4604=ORIENTED_EDGE('',*,*,#6986,.F.);
#4605=ORIENTED_EDGE('',*,*,#6987,.F.);
#4606=ORIENTED_EDGE('',*,*,#6988,.F.);
#4607=ORIENTED_EDGE('',*,*,#6989,.F.);
#4608=ORIENTED_EDGE('',*,*,#6990,.F.);
#4609=ORIENTED_EDGE('',*,*,#6991,.F.);
#4610=ORIENTED_EDGE('',*,*,#6973,.F.);
#4611=ORIENTED_EDGE('',*,*,#6992,.F.);
#4612=ORIENTED_EDGE('',*,*,#6993,.F.);
#4613=ORIENTED_EDGE('',*,*,#6994,.F.);
#4614=ORIENTED_EDGE('',*,*,#6995,.T.);
#4615=ORIENTED_EDGE('',*,*,#6981,.F.);
#4616=ORIENTED_EDGE('',*,*,#6995,.F.);
#4617=ORIENTED_EDGE('',*,*,#6996,.F.);
#4618=ORIENTED_EDGE('',*,*,#6984,.F.);
#4619=ORIENTED_EDGE('',*,*,#6997,.F.);
#4620=ORIENTED_EDGE('',*,*,#6982,.F.);
#4621=ORIENTED_EDGE('',*,*,#6998,.F.);
#4622=ORIENTED_EDGE('',*,*,#6976,.T.);
#4623=ORIENTED_EDGE('',*,*,#6999,.T.);
#4624=ORIENTED_EDGE('',*,*,#6978,.T.);
#4625=ORIENTED_EDGE('',*,*,#7000,.F.);
#4626=ORIENTED_EDGE('',*,*,#7001,.T.);
#4627=ORIENTED_EDGE('',*,*,#7002,.T.);
#4628=ORIENTED_EDGE('',*,*,#7003,.F.);
#4629=ORIENTED_EDGE('',*,*,#7004,.T.);
#4630=ORIENTED_EDGE('',*,*,#7005,.T.);
#4631=ORIENTED_EDGE('',*,*,#7006,.T.);
#4632=ORIENTED_EDGE('',*,*,#7007,.T.);
#4633=ORIENTED_EDGE('',*,*,#7008,.T.);
#4634=ORIENTED_EDGE('',*,*,#7009,.T.);
#4635=ORIENTED_EDGE('',*,*,#7006,.F.);
#4636=ORIENTED_EDGE('',*,*,#7010,.F.);
#4637=ORIENTED_EDGE('',*,*,#6941,.F.);
#4638=ORIENTED_EDGE('',*,*,#6940,.F.);
#4639=ORIENTED_EDGE('',*,*,#6939,.F.);
#4640=ORIENTED_EDGE('',*,*,#6938,.F.);
#4641=ORIENTED_EDGE('',*,*,#6937,.F.);
#4642=ORIENTED_EDGE('',*,*,#6936,.F.);
#4643=ORIENTED_EDGE('',*,*,#6935,.F.);
#4644=ORIENTED_EDGE('',*,*,#6934,.F.);
#4645=ORIENTED_EDGE('',*,*,#6958,.T.);
#4646=ORIENTED_EDGE('',*,*,#6959,.T.);
#4647=ORIENTED_EDGE('',*,*,#6954,.T.);
#4648=ORIENTED_EDGE('',*,*,#6953,.T.);
#4649=ORIENTED_EDGE('',*,*,#6952,.T.);
#4650=ORIENTED_EDGE('',*,*,#6951,.T.);
#4651=ORIENTED_EDGE('',*,*,#6950,.T.);
#4652=ORIENTED_EDGE('',*,*,#6949,.T.);
#4653=ORIENTED_EDGE('',*,*,#6948,.T.);
#4654=ORIENTED_EDGE('',*,*,#6947,.T.);
#4655=ORIENTED_EDGE('',*,*,#6957,.T.);
#4656=ORIENTED_EDGE('',*,*,#7007,.F.);
#4657=ORIENTED_EDGE('',*,*,#7010,.T.);
#4658=ORIENTED_EDGE('',*,*,#6967,.T.);
#4659=ORIENTED_EDGE('',*,*,#6966,.T.);
#4660=ORIENTED_EDGE('',*,*,#6965,.T.);
#4661=ORIENTED_EDGE('',*,*,#6974,.T.);
#4662=ORIENTED_EDGE('',*,*,#6991,.T.);
#4663=ORIENTED_EDGE('',*,*,#6990,.T.);
#4664=ORIENTED_EDGE('',*,*,#6989,.T.);
#4665=ORIENTED_EDGE('',*,*,#6988,.T.);
#4666=ORIENTED_EDGE('',*,*,#6987,.T.);
#4667=ORIENTED_EDGE('',*,*,#6986,.T.);
#4668=ORIENTED_EDGE('',*,*,#6985,.T.);
#4669=ORIENTED_EDGE('',*,*,#7011,.T.);
#4670=ORIENTED_EDGE('',*,*,#6980,.T.);
#4671=ORIENTED_EDGE('',*,*,#6971,.T.);
#4672=ORIENTED_EDGE('',*,*,#6970,.T.);
#4673=ORIENTED_EDGE('',*,*,#6969,.T.);
#4674=ORIENTED_EDGE('',*,*,#6968,.T.);
#4675=ORIENTED_EDGE('',*,*,#7012,.T.);
#4676=ORIENTED_EDGE('',*,*,#7013,.T.);
#4677=ORIENTED_EDGE('',*,*,#7014,.T.);
#4678=ORIENTED_EDGE('',*,*,#7015,.T.);
#4679=ORIENTED_EDGE('',*,*,#7016,.T.);
#4680=ORIENTED_EDGE('',*,*,#7017,.T.);
#4681=ORIENTED_EDGE('',*,*,#7018,.T.);
#4682=ORIENTED_EDGE('',*,*,#7000,.T.);
#4683=ORIENTED_EDGE('',*,*,#7017,.F.);
#4684=ORIENTED_EDGE('',*,*,#6998,.T.);
#4685=ORIENTED_EDGE('',*,*,#6975,.T.);
#4686=ORIENTED_EDGE('',*,*,#6963,.T.);
#4687=ORIENTED_EDGE('',*,*,#6962,.T.);
#4688=ORIENTED_EDGE('',*,*,#6961,.T.);
#4689=ORIENTED_EDGE('',*,*,#6979,.T.);
#4690=ORIENTED_EDGE('',*,*,#6999,.F.);
#4691=ORIENTED_EDGE('',*,*,#6983,.T.);
#4692=ORIENTED_EDGE('',*,*,#6997,.T.);
#4693=ORIENTED_EDGE('',*,*,#6993,.T.);
#4694=ORIENTED_EDGE('',*,*,#6992,.T.);
#4695=ORIENTED_EDGE('',*,*,#6977,.T.);
#4696=ORIENTED_EDGE('',*,*,#7008,.F.);
#4697=ORIENTED_EDGE('',*,*,#7011,.F.);
#4698=ORIENTED_EDGE('',*,*,#6996,.T.);
#4699=ORIENTED_EDGE('',*,*,#6994,.T.);
#4700=ORIENTED_EDGE('',*,*,#7001,.F.);
#4701=ORIENTED_EDGE('',*,*,#7012,.F.);
#4702=ORIENTED_EDGE('',*,*,#7013,.F.);
#4703=ORIENTED_EDGE('',*,*,#7019,.T.);
#4704=ORIENTED_EDGE('',*,*,#7014,.F.);
#4705=ORIENTED_EDGE('',*,*,#7002,.F.);
#4706=ORIENTED_EDGE('',*,*,#7020,.T.);
#4707=ORIENTED_EDGE('',*,*,#7003,.T.);
#4708=ORIENTED_EDGE('',*,*,#7021,.T.);
#4709=ORIENTED_EDGE('',*,*,#6960,.F.);
#4710=ORIENTED_EDGE('',*,*,#7021,.F.);
#4711=ORIENTED_EDGE('',*,*,#7016,.F.);
#4712=ORIENTED_EDGE('',*,*,#7019,.F.);
#4713=ORIENTED_EDGE('',*,*,#7015,.F.);
#4714=ORIENTED_EDGE('',*,*,#7005,.F.);
#4715=ORIENTED_EDGE('',*,*,#7018,.F.);
#4716=ORIENTED_EDGE('',*,*,#7004,.F.);
#4717=ORIENTED_EDGE('',*,*,#7020,.F.);
#4718=ORIENTED_EDGE('',*,*,#6932,.F.);
#4719=ORIENTED_EDGE('',*,*,#7022,.T.);
#4720=ORIENTED_EDGE('',*,*,#6892,.F.);
#4721=ORIENTED_EDGE('',*,*,#6904,.T.);
#4722=ORIENTED_EDGE('',*,*,#6874,.F.);
#4723=ORIENTED_EDGE('',*,*,#6883,.T.);
#4724=ORIENTED_EDGE('',*,*,#6852,.F.);
#4725=ORIENTED_EDGE('',*,*,#6864,.T.);
#4726=ORIENTED_EDGE('',*,*,#6834,.F.);
#4727=ORIENTED_EDGE('',*,*,#6845,.T.);
#4728=ORIENTED_EDGE('',*,*,#7022,.F.);
#4729=ORIENTED_EDGE('',*,*,#6829,.F.);
#4730=ORIENTED_EDGE('',*,*,#6881,.F.);
#4731=ORIENTED_EDGE('',*,*,#7023,.F.);
#4732=ORIENTED_EDGE('',*,*,#6886,.F.);
#4733=ORIENTED_EDGE('',*,*,#6927,.F.);
#4734=ORIENTED_EDGE('',*,*,#6879,.F.);
#4735=ORIENTED_EDGE('',*,*,#6926,.F.);
#4736=ORIENTED_EDGE('',*,*,#6888,.F.);
#4737=ORIENTED_EDGE('',*,*,#7024,.F.);
#4738=ORIENTED_EDGE('',*,*,#6880,.T.);
#4739=ORIENTED_EDGE('',*,*,#7024,.T.);
#4740=ORIENTED_EDGE('',*,*,#6887,.F.);
#4741=ORIENTED_EDGE('',*,*,#7023,.T.);
#4742=ORIENTED_EDGE('',*,*,#7009,.F.);
#4743=ORIENTED_EDGE('',*,*,#6828,.T.);
#4744=ORIENTED_EDGE('',*,*,#6848,.F.);
#4745=ORIENTED_EDGE('',*,*,#6833,.T.);
#4746=ORIENTED_EDGE('',*,*,#6840,.T.);
#4747=ORIENTED_EDGE('',*,*,#6843,.T.);
#4748=ORIENTED_EDGE('',*,*,#6898,.T.);
#4749=ORIENTED_EDGE('',*,*,#6902,.T.);
#4750=ORIENTED_EDGE('',*,*,#6908,.F.);
#4751=ORIENTED_EDGE('',*,*,#6913,.T.);
#4752=ORIENTED_EDGE('',*,*,#6858,.T.);
#4753=ORIENTED_EDGE('',*,*,#6862,.T.);
#4754=ORIENTED_EDGE('',*,*,#6868,.F.);
#4755=ORIENTED_EDGE('',*,*,#6873,.T.);
#6828=EDGE_CURVE('',#8319,#8319,#848,.T.);
#6829=EDGE_CURVE('',#8320,#8320,#849,.T.);
#6830=EDGE_CURVE('',#8321,#8322,#850,.T.);
#6831=EDGE_CURVE('',#8323,#8321,#9327,.T.);
#6832=EDGE_CURVE('',#8324,#8323,#851,.T.);
#6833=EDGE_CURVE('',#8322,#8324,#9328,.T.);
#6834=EDGE_CURVE('',#8325,#8325,#852,.T.);
#6835=EDGE_CURVE('',#8326,#8327,#853,.T.);
#6836=EDGE_CURVE('',#8326,#8328,#9329,.T.);
#6837=EDGE_CURVE('',#8329,#8328,#854,.T.);
#6838=EDGE_CURVE('',#8330,#8329,#9330,.T.);
#6839=EDGE_CURVE('',#8330,#8331,#855,.T.);
#6840=EDGE_CURVE('',#8324,#8331,#856,.T.);
#6841=EDGE_CURVE('',#8323,#8327,#9331,.T.);
#6842=EDGE_CURVE('',#8332,#8333,#857,.T.);
#6843=EDGE_CURVE('',#8331,#8332,#9332,.T.);
#6844=EDGE_CURVE('',#8333,#8330,#9333,.T.);
#6845=EDGE_CURVE('',#8334,#8334,#858,.T.);
#6846=EDGE_CURVE('',#8335,#8336,#859,.T.);
#6847=EDGE_CURVE('',#8321,#8336,#9334,.T.);
#6848=EDGE_CURVE('',#8322,#8332,#860,.T.);
#6849=EDGE_CURVE('',#8333,#8337,#9335,.T.);
#6850=EDGE_CURVE('',#8337,#8338,#861,.T.);
#6851=EDGE_CURVE('',#8335,#8338,#9336,.T.);
#6852=EDGE_CURVE('',#8339,#8339,#862,.T.);
#6853=EDGE_CURVE('',#8340,#8341,#863,.T.);
#6854=EDGE_CURVE('',#8340,#8342,#9337,.T.);
#6855=EDGE_CURVE('',#8343,#8342,#864,.T.);
#6856=EDGE_CURVE('',#8344,#8343,#9338,.T.);
#6857=EDGE_CURVE('',#8344,#8345,#865,.T.);
#6858=EDGE_CURVE('',#8346,#8345,#866,.T.);
#6859=EDGE_CURVE('',#8346,#8347,#867,.T.);
#6860=EDGE_CURVE('',#8347,#8341,#9339,.T.);
#6861=EDGE_CURVE('',#8348,#8349,#868,.T.);
#6862=EDGE_CURVE('',#8345,#8348,#9340,.T.);
#6863=EDGE_CURVE('',#8349,#8344,#9341,.T.);
#6864=EDGE_CURVE('',#8350,#8350,#869,.T.);
#6865=EDGE_CURVE('',#8351,#8352,#870,.T.);
#6866=EDGE_CURVE('',#8353,#8352,#9342,.T.);
#6867=EDGE_CURVE('',#8353,#8354,#871,.T.);
#6868=EDGE_CURVE('',#8354,#8348,#872,.T.);
#6869=EDGE_CURVE('',#8349,#8355,#9343,.T.);
#6870=EDGE_CURVE('',#8355,#8356,#873,.T.);
#6871=EDGE_CURVE('',#8351,#8356,#9344,.T.);
#6872=EDGE_CURVE('',#8347,#8353,#9345,.T.);
#6873=EDGE_CURVE('',#8354,#8346,#9346,.T.);
#6874=EDGE_CURVE('',#8357,#8357,#874,.T.);
#6875=EDGE_CURVE('',#8358,#8359,#875,.T.);
#6876=EDGE_CURVE('',#8358,#8360,#9347,.T.);
#6877=EDGE_CURVE('',#8361,#8360,#876,.T.);
#6878=EDGE_CURVE('',#8362,#8361,#9348,.T.);
#6879=EDGE_CURVE('',#8362,#8363,#877,.T.);
#6880=EDGE_CURVE('',#8364,#8363,#878,.T.);
#6881=EDGE_CURVE('',#8364,#8365,#879,.T.);
#6882=EDGE_CURVE('',#8365,#8359,#9349,.T.);
#6883=EDGE_CURVE('',#8366,#8366,#880,.T.);
#6884=EDGE_CURVE('',#8367,#8368,#881,.T.);
#6885=EDGE_CURVE('',#8369,#8368,#9350,.T.);
#6886=EDGE_CURVE('',#8369,#8370,#882,.T.);
#6887=EDGE_CURVE('',#8370,#8371,#883,.T.);
#6888=EDGE_CURVE('',#8371,#8372,#884,.T.);
#6889=EDGE_CURVE('',#8372,#8373,#9351,.T.);
#6890=EDGE_CURVE('',#8373,#8374,#885,.T.);
#6891=EDGE_CURVE('',#8367,#8374,#9352,.T.);
#6892=EDGE_CURVE('',#8375,#8375,#886,.T.);
#6893=EDGE_CURVE('',#8376,#8377,#887,.T.);
#6894=EDGE_CURVE('',#8376,#8378,#9353,.T.);
#6895=EDGE_CURVE('',#8379,#8378,#888,.T.);
#6896=EDGE_CURVE('',#8380,#8379,#9354,.T.);
#6897=EDGE_CURVE('',#8380,#8381,#889,.T.);
#6898=EDGE_CURVE('',#8382,#8381,#890,.T.);
#6899=EDGE_CURVE('',#8382,#8383,#891,.T.);
#6900=EDGE_CURVE('',#8383,#8377,#9355,.T.);
#6901=EDGE_CURVE('',#8384,#8385,#892,.T.);
#6902=EDGE_CURVE('',#8381,#8384,#9356,.T.);
#6903=EDGE_CURVE('',#8385,#8380,#9357,.T.);
#6904=EDGE_CURVE('',#8386,#8386,#893,.T.);
#6905=EDGE_CURVE('',#8387,#8388,#894,.T.);
#6906=EDGE_CURVE('',#8389,#8388,#9358,.T.);
#6907=EDGE_CURVE('',#8389,#8390,#895,.T.);
#6908=EDGE_CURVE('',#8390,#8384,#896,.T.);
#6909=EDGE_CURVE('',#8385,#8391,#9359,.T.);
#6910=EDGE_CURVE('',#8391,#8392,#897,.T.);
#6911=EDGE_CURVE('',#8387,#8392,#9360,.T.);
#6912=EDGE_CURVE('',#8383,#8389,#9361,.T.);
#6913=EDGE_CURVE('',#8390,#8382,#9362,.T.);
#6914=EDGE_CURVE('',#8336,#8327,#9363,.T.);
#6915=EDGE_CURVE('',#8335,#8326,#9364,.T.);
#6916=EDGE_CURVE('',#8338,#8328,#9365,.T.);
#6917=EDGE_CURVE('',#8337,#8329,#9366,.T.);
#6918=EDGE_CURVE('',#8352,#8341,#9367,.T.);
#6919=EDGE_CURVE('',#8351,#8340,#9368,.T.);
#6920=EDGE_CURVE('',#8356,#8342,#9369,.T.);
#6921=EDGE_CURVE('',#8355,#8343,#9370,.T.);
#6922=EDGE_CURVE('',#8368,#8359,#9371,.T.);
#6923=EDGE_CURVE('',#8367,#8358,#9372,.T.);
#6924=EDGE_CURVE('',#8374,#8360,#9373,.T.);
#6925=EDGE_CURVE('',#8373,#8361,#9374,.T.);
#6926=EDGE_CURVE('',#8372,#8362,#9375,.T.);
#6927=EDGE_CURVE('',#8365,#8369,#9376,.T.);
#6928=EDGE_CURVE('',#8388,#8377,#9377,.T.);
#6929=EDGE_CURVE('',#8387,#8376,#9378,.T.);
#6930=EDGE_CURVE('',#8392,#8378,#9379,.T.);
#6931=EDGE_CURVE('',#8391,#8379,#9380,.T.);
#6932=EDGE_CURVE('',#8393,#8393,#898,.T.);
#6933=EDGE_CURVE('',#8394,#8395,#9381,.T.);
#6934=EDGE_CURVE('',#8395,#8396,#1911,.T.);
#6935=EDGE_CURVE('',#8396,#8397,#1912,.T.);
#6936=EDGE_CURVE('',#8397,#8398,#1913,.T.);
#6937=EDGE_CURVE('',#8398,#8399,#1914,.T.);
#6938=EDGE_CURVE('',#8399,#8400,#1915,.T.);
#6939=EDGE_CURVE('',#8400,#8401,#1916,.T.);
#6940=EDGE_CURVE('',#8401,#8402,#1917,.T.);
#6941=EDGE_CURVE('',#8402,#8403,#1918,.T.);
#6942=EDGE_CURVE('',#8403,#8404,#9382,.T.);
#6943=EDGE_CURVE('',#8394,#8404,#1919,.T.);
#6944=EDGE_CURVE('',#8405,#8406,#9383,.T.);
#6945=EDGE_CURVE('',#8406,#8407,#1920,.T.);
#6946=EDGE_CURVE('',#8407,#8408,#9384,.T.);
#6947=EDGE_CURVE('',#8409,#8408,#1921,.T.);
#6948=EDGE_CURVE('',#8410,#8409,#1922,.T.);
#6949=EDGE_CURVE('',#8411,#8410,#1923,.T.);
#6950=EDGE_CURVE('',#8412,#8411,#1924,.T.);
#6951=EDGE_CURVE('',#8413,#8412,#1925,.T.);
#6952=EDGE_CURVE('',#8414,#8413,#1926,.T.);
#6953=EDGE_CURVE('',#8415,#8414,#1927,.T.);
#6954=EDGE_CURVE('',#8405,#8415,#1928,.T.);
#6955=EDGE_CURVE('',#8406,#8394,#9385,.T.);
#6956=EDGE_CURVE('',#8404,#8407,#9386,.T.);
#6957=EDGE_CURVE('',#8408,#8403,#9387,.T.);
#6958=EDGE_CURVE('',#8395,#8405,#9388,.T.);
#6959=EDGE_CURVE('',#8405,#8405,#899,.T.);
#6960=EDGE_CURVE('',#8416,#8416,#900,.T.);
#6961=EDGE_CURVE('',#8417,#8418,#1110,.F.);
#6962=EDGE_CURVE('',#8419,#8417,#1111,.F.);
#6963=EDGE_CURVE('',#8420,#8419,#1112,.F.);
#6964=EDGE_CURVE('',#8420,#8421,#1113,.F.);
#6965=EDGE_CURVE('',#8422,#8421,#1114,.T.);
#6966=EDGE_CURVE('',#8423,#8422,#1115,.T.);
#6967=EDGE_CURVE('',#8424,#8423,#1116,.T.);
#6968=EDGE_CURVE('',#8425,#8424,#1117,.T.);
#6969=EDGE_CURVE('',#8426,#8425,#1118,.T.);
#6970=EDGE_CURVE('',#8427,#8426,#1119,.T.);
#6971=EDGE_CURVE('',#8428,#8427,#1120,.T.);
#6972=EDGE_CURVE('',#8428,#8418,#1121,.F.);
#6973=EDGE_CURVE('',#8429,#8430,#1122,.T.);
#6974=EDGE_CURVE('',#8421,#8430,#1123,.F.);
#6975=EDGE_CURVE('',#8431,#8420,#1124,.F.);
#6976=EDGE_CURVE('',#8432,#8431,#1125,.T.);
#6977=EDGE_CURVE('',#8429,#8432,#901,.T.);
#6978=EDGE_CURVE('',#8433,#8434,#1126,.T.);
#6979=EDGE_CURVE('',#8418,#8433,#1127,.F.);
#6980=EDGE_CURVE('',#8435,#8428,#1128,.F.);
#6981=EDGE_CURVE('',#8435,#8436,#1129,.T.);
#6982=EDGE_CURVE('',#8436,#8437,#1130,.T.);
#6983=EDGE_CURVE('',#8434,#8437,#1131,.F.);
#6984=EDGE_CURVE('',#8438,#8439,#902,.T.);
#6985=EDGE_CURVE('',#8440,#8439,#1132,.T.);
#6986=EDGE_CURVE('',#8441,#8440,#1133,.T.);
#6987=EDGE_CURVE('',#8442,#8441,#1134,.T.);
#6988=EDGE_CURVE('',#8443,#8442,#1135,.T.);
#6989=EDGE_CURVE('',#8444,#8443,#1136,.T.);
#6990=EDGE_CURVE('',#8445,#8444,#1137,.T.);
#6991=EDGE_CURVE('',#8430,#8445,#1138,.T.);
#6992=EDGE_CURVE('',#8446,#8429,#1139,.F.);
#6993=EDGE_CURVE('',#8438,#8446,#1140,.F.);
#6994=EDGE_CURVE('',#8447,#8435,#1141,.T.);
#6995=EDGE_CURVE('',#8447,#8436,#1142,.T.);
#6996=EDGE_CURVE('',#8439,#8447,#1143,.T.);
#6997=EDGE_CURVE('',#8437,#8438,#1144,.F.);
#6998=EDGE_CURVE('',#8432,#8431,#903,.T.);
#6999=EDGE_CURVE('',#8434,#8433,#904,.T.);
#7000=EDGE_CURVE('',#8448,#8448,#905,.T.);
#7001=EDGE_CURVE('',#8449,#8449,#906,.T.);
#7002=EDGE_CURVE('',#8450,#8450,#907,.T.);
#7003=EDGE_CURVE('',#8451,#8452,#908,.T.);
#7004=EDGE_CURVE('',#8451,#8452,#909,.T.);
#7005=EDGE_CURVE('',#8453,#8453,#910,.T.);
#7006=EDGE_CURVE('',#8454,#8455,#911,.T.);
#7007=EDGE_CURVE('',#8455,#8454,#912,.T.);
#7008=EDGE_CURVE('',#8456,#8456,#913,.T.);
#7009=EDGE_CURVE('',#8457,#8457,#914,.T.);
#7010=EDGE_CURVE('',#8455,#8454,#1145,.T.);
#7011=EDGE_CURVE('',#8439,#8435,#915,.T.);
#7012=EDGE_CURVE('',#8458,#8458,#916,.T.);
#7013=EDGE_CURVE('',#8459,#8459,#917,.T.);
#7014=EDGE_CURVE('',#8460,#8460,#918,.T.);
#7015=EDGE_CURVE('',#8461,#8461,#919,.T.);
#7016=EDGE_CURVE('',#8462,#8462,#920,.T.);
#7017=EDGE_CURVE('',#8463,#8463,#921,.T.);
#7018=EDGE_CURVE('',#8464,#8464,#922,.T.);
#7019=EDGE_CURVE('',#8465,#8465,#923,.T.);
#7020=EDGE_CURVE('',#8452,#8451,#1146,.T.);
#7021=EDGE_CURVE('',#8466,#8466,#924,.T.);
#7022=EDGE_CURVE('',#8467,#8467,#925,.T.);
#7023=EDGE_CURVE('',#8370,#8364,#9389,.T.);
#7024=EDGE_CURVE('',#8363,#8371,#9390,.T.);
#8319=VERTEX_POINT('',#35379);
#8320=VERTEX_POINT('',#35381);
#8321=VERTEX_POINT('',#35384);
#8322=VERTEX_POINT('',#35385);
#8323=VERTEX_POINT('',#35387);
#8324=VERTEX_POINT('',#35389);
#8325=VERTEX_POINT('',#35393);
#8326=VERTEX_POINT('',#35395);
#8327=VERTEX_POINT('',#35396);
#8328=VERTEX_POINT('',#35398);
#8329=VERTEX_POINT('',#35400);
#8330=VERTEX_POINT('',#35402);
#8331=VERTEX_POINT('',#35404);
#8332=VERTEX_POINT('',#35409);
#8333=VERTEX_POINT('',#35410);
#8334=VERTEX_POINT('',#35415);
#8335=VERTEX_POINT('',#35417);
#8336=VERTEX_POINT('',#35418);
#8337=VERTEX_POINT('',#35422);
#8338=VERTEX_POINT('',#35424);
#8339=VERTEX_POINT('',#35428);
#8340=VERTEX_POINT('',#35430);
#8341=VERTEX_POINT('',#35431);
#8342=VERTEX_POINT('',#35433);
#8343=VERTEX_POINT('',#35435);
#8344=VERTEX_POINT('',#35437);
#8345=VERTEX_POINT('',#35439);
#8346=VERTEX_POINT('',#35441);
#8347=VERTEX_POINT('',#35443);
#8348=VERTEX_POINT('',#35447);
#8349=VERTEX_POINT('',#35448);
#8350=VERTEX_POINT('',#35453);
#8351=VERTEX_POINT('',#35455);
#8352=VERTEX_POINT('',#35456);
#8353=VERTEX_POINT('',#35458);
#8354=VERTEX_POINT('',#35460);
#8355=VERTEX_POINT('',#35463);
#8356=VERTEX_POINT('',#35465);
#8357=VERTEX_POINT('',#35472);
#8358=VERTEX_POINT('',#35474);
#8359=VERTEX_POINT('',#35475);
#8360=VERTEX_POINT('',#35477);
#8361=VERTEX_POINT('',#35479);
#8362=VERTEX_POINT('',#35481);
#8363=VERTEX_POINT('',#35483);
#8364=VERTEX_POINT('',#35485);
#8365=VERTEX_POINT('',#35487);
#8366=VERTEX_POINT('',#35491);
#8367=VERTEX_POINT('',#35493);
#8368=VERTEX_POINT('',#35494);
#8369=VERTEX_POINT('',#35496);
#8370=VERTEX_POINT('',#35498);
#8371=VERTEX_POINT('',#35500);
#8372=VERTEX_POINT('',#35502);
#8373=VERTEX_POINT('',#35504);
#8374=VERTEX_POINT('',#35506);
#8375=VERTEX_POINT('',#35510);
#8376=VERTEX_POINT('',#35512);
#8377=VERTEX_POINT('',#35513);
#8378=VERTEX_POINT('',#35515);
#8379=VERTEX_POINT('',#35517);
#8380=VERTEX_POINT('',#35519);
#8381=VERTEX_POINT('',#35521);
#8382=VERTEX_POINT('',#35523);
#8383=VERTEX_POINT('',#35525);
#8384=VERTEX_POINT('',#35529);
#8385=VERTEX_POINT('',#35530);
#8386=VERTEX_POINT('',#35535);
#8387=VERTEX_POINT('',#35537);
#8388=VERTEX_POINT('',#35538);
#8389=VERTEX_POINT('',#35540);
#8390=VERTEX_POINT('',#35542);
#8391=VERTEX_POINT('',#35545);
#8392=VERTEX_POINT('',#35547);
#8393=VERTEX_POINT('',#35592);
#8394=VERTEX_POINT('',#35724);
#8395=VERTEX_POINT('',#35725);
#8396=VERTEX_POINT('',#35735);
#8397=VERTEX_POINT('',#35745);
#8398=VERTEX_POINT('',#35755);
#8399=VERTEX_POINT('',#35765);
#8400=VERTEX_POINT('',#35775);
#8401=VERTEX_POINT('',#35785);
#8402=VERTEX_POINT('',#35795);
#8403=VERTEX_POINT('',#35805);
#8404=VERTEX_POINT('',#35807);
#8405=VERTEX_POINT('',#36004);
#8406=VERTEX_POINT('',#36005);
#8407=VERTEX_POINT('',#36071);
#8408=VERTEX_POINT('',#36073);
#8409=VERTEX_POINT('',#36083);
#8410=VERTEX_POINT('',#36093);
#8411=VERTEX_POINT('',#36103);
#8412=VERTEX_POINT('',#36113);
#8413=VERTEX_POINT('',#36123);
#8414=VERTEX_POINT('',#36133);
#8415=VERTEX_POINT('',#36143);
#8416=VERTEX_POINT('',#36163);
#8417=VERTEX_POINT('',#37218);
#8418=VERTEX_POINT('',#37219);
#8419=VERTEX_POINT('',#37334);
#8420=VERTEX_POINT('',#37339);
#8421=VERTEX_POINT('',#37345);
#8422=VERTEX_POINT('',#37351);
#8423=VERTEX_POINT('',#37363);
#8424=VERTEX_POINT('',#37375);
#8425=VERTEX_POINT('',#37387);
#8426=VERTEX_POINT('',#37399);
#8427=VERTEX_POINT('',#37411);
#8428=VERTEX_POINT('',#37419);
#8429=VERTEX_POINT('',#37431);
#8430=VERTEX_POINT('',#37432);
#8431=VERTEX_POINT('',#37441);
#8432=VERTEX_POINT('',#37446);
#8433=VERTEX_POINT('',#37453);
#8434=VERTEX_POINT('',#37454);
#8435=VERTEX_POINT('',#37463);
#8436=VERTEX_POINT('',#37468);
#8437=VERTEX_POINT('',#37473);
#8438=VERTEX_POINT('',#38517);
#8439=VERTEX_POINT('',#38518);
#8440=VERTEX_POINT('',#38526);
#8441=VERTEX_POINT('',#38538);
#8442=VERTEX_POINT('',#38550);
#8443=VERTEX_POINT('',#38562);
#8444=VERTEX_POINT('',#38574);
#8445=VERTEX_POINT('',#38586);
#8446=VERTEX_POINT('',#38596);
#8447=VERTEX_POINT('',#38723);
#8448=VERTEX_POINT('',#38775);
#8449=VERTEX_POINT('',#38778);
#8450=VERTEX_POINT('',#38780);
#8451=VERTEX_POINT('',#38783);
#8452=VERTEX_POINT('',#38784);
#8453=VERTEX_POINT('',#38787);
#8454=VERTEX_POINT('',#38790);
#8455=VERTEX_POINT('',#38791);
#8456=VERTEX_POINT('',#38794);
#8457=VERTEX_POINT('',#38797);
#8458=VERTEX_POINT('',#38809);
#8459=VERTEX_POINT('',#38812);
#8460=VERTEX_POINT('',#38814);
#8461=VERTEX_POINT('',#38817);
#8462=VERTEX_POINT('',#38819);
#8463=VERTEX_POINT('',#38822);
#8464=VERTEX_POINT('',#38824);
#8465=VERTEX_POINT('',#39432);
#8466=VERTEX_POINT('',#39443);
#8467=VERTEX_POINT('',#39450);
#9327=LINE('',#35386,#10155);
#9328=LINE('',#35390,#10156);
#9329=LINE('',#35397,#10157);
#9330=LINE('',#35401,#10158);
#9331=LINE('',#35406,#10159);
#9332=LINE('',#35411,#10160);
#9333=LINE('',#35412,#10161);
#9334=LINE('',#35419,#10162);
#9335=LINE('',#35421,#10163);
#9336=LINE('',#35425,#10164);
#9337=LINE('',#35432,#10165);
#9338=LINE('',#35436,#10166);
#9339=LINE('',#35444,#10167);
#9340=LINE('',#35449,#10168);
#9341=LINE('',#35450,#10169);
#9342=LINE('',#35457,#10170);
#9343=LINE('',#35462,#10171);
#9344=LINE('',#35466,#10172);
#9345=LINE('',#35468,#10173);
#9346=LINE('',#35469,#10174);
#9347=LINE('',#35476,#10175);
#9348=LINE('',#35480,#10176);
#9349=LINE('',#35488,#10177);
#9350=LINE('',#35495,#10178);
#9351=LINE('',#35503,#10179);
#9352=LINE('',#35507,#10180);
#9353=LINE('',#35514,#10181);
#9354=LINE('',#35518,#10182);
#9355=LINE('',#35526,#10183);
#9356=LINE('',#35531,#10184);
#9357=LINE('',#35532,#10185);
#9358=LINE('',#35539,#10186);
#9359=LINE('',#35544,#10187);
#9360=LINE('',#35548,#10188);
#9361=LINE('',#35550,#10189);
#9362=LINE('',#35551,#10190);
#9363=LINE('',#35553,#10191);
#9364=LINE('',#35555,#10192);
#9365=LINE('',#35557,#10193);
#9366=LINE('',#35559,#10194);
#9367=LINE('',#35562,#10195);
#9368=LINE('',#35563,#10196);
#9369=LINE('',#35565,#10197);
#9370=LINE('',#35567,#10198);
#9371=LINE('',#35571,#10199);
#9372=LINE('',#35572,#10200);
#9373=LINE('',#35574,#10201);
#9374=LINE('',#35576,#10202);
#9375=LINE('',#35578,#10203);
#9376=LINE('',#35580,#10204);
#9377=LINE('',#35582,#10205);
#9378=LINE('',#35583,#10206);
#9379=LINE('',#35585,#10207);
#9380=LINE('',#35587,#10208);
#9381=LINE('',#35723,#10209);
#9382=LINE('',#35806,#10210);
#9383=LINE('',#36003,#10211);
#9384=LINE('',#36072,#10212);
#9385=LINE('',#36154,#10213);
#9386=LINE('',#36155,#10214);
#9387=LINE('',#36157,#10215);
#9388=LINE('',#36159,#10216);
#9389=LINE('',#39457,#10217);
#9390=LINE('',#39459,#10218);
#10155=VECTOR('',#17951,1.);
#10156=VECTOR('',#17954,1.);
#10157=VECTOR('',#17961,1.);
#10158=VECTOR('',#17964,1.);
#10159=VECTOR('',#17969,1.);
#10160=VECTOR('',#17974,1.);
#10161=VECTOR('',#17975,1.);
#10162=VECTOR('',#17982,1.);
#10163=VECTOR('',#17985,1.);
#10164=VECTOR('',#17988,1.);
#10165=VECTOR('',#17995,1.);
#10166=VECTOR('',#17998,1.);
#10167=VECTOR('',#18005,1.);
#10168=VECTOR('',#18010,1.);
#10169=VECTOR('',#18011,1.);
#10170=VECTOR('',#18018,1.);
#10171=VECTOR('',#18023,1.);
#10172=VECTOR('',#18026,1.);
#10173=VECTOR('',#18029,1.);
#10174=VECTOR('',#18030,1.);
#10175=VECTOR('',#18037,1.);
#10176=VECTOR('',#18040,1.);
#10177=VECTOR('',#18047,1.);
#10178=VECTOR('',#18054,1.);
#10179=VECTOR('',#18061,1.);
#10180=VECTOR('',#18064,1.);
#10181=VECTOR('',#18071,1.);
#10182=VECTOR('',#18074,1.);
#10183=VECTOR('',#18081,1.);
#10184=VECTOR('',#18086,1.);
#10185=VECTOR('',#18087,1.);
#10186=VECTOR('',#18094,1.);
#10187=VECTOR('',#18099,1.);
#10188=VECTOR('',#18102,1.);
#10189=VECTOR('',#18105,1.);
#10190=VECTOR('',#18106,1.);
#10191=VECTOR('',#18109,1.);
#10192=VECTOR('',#18112,1.);
#10193=VECTOR('',#18115,1.);
#10194=VECTOR('',#18118,1.);
#10195=VECTOR('',#18123,1.);
#10196=VECTOR('',#18124,1.);
#10197=VECTOR('',#18127,1.);
#10198=VECTOR('',#18130,1.);
#10199=VECTOR('',#18137,1.);
#10200=VECTOR('',#18138,1.);
#10201=VECTOR('',#18141,1.);
#10202=VECTOR('',#18144,1.);
#10203=VECTOR('',#18147,1.);
#10204=VECTOR('',#18150,1.);
#10205=VECTOR('',#18153,1.);
#10206=VECTOR('',#18154,1.);
#10207=VECTOR('',#18157,1.);
#10208=VECTOR('',#18160,1.);
#10209=VECTOR('',#18169,1.);
#10210=VECTOR('',#18170,1.);
#10211=VECTOR('',#18171,1.);
#10212=VECTOR('',#18172,1.);
#10213=VECTOR('',#18175,1.);
#10214=VECTOR('',#18176,1.);
#10215=VECTOR('',#18179,1.);
#10216=VECTOR('',#18182,1.);
#10217=VECTOR('',#18301,1.);
#10218=VECTOR('',#18304,1.);
#11200=EDGE_LOOP('',(#4362));
#11201=EDGE_LOOP('',(#4363));
#11202=EDGE_LOOP('',(#4364,#4365,#4366,#4367));
#11203=EDGE_LOOP('',(#4368));
#11204=EDGE_LOOP('',(#4369,#4370,#4371,#4372,#4373,#4374,#4375,#4376));
#11205=EDGE_LOOP('',(#4377,#4378,#4379,#4380));
#11206=EDGE_LOOP('',(#4381));
#11207=EDGE_LOOP('',(#4382,#4383,#4384,#4385,#4386,#4387,#4388,#4389));
#11208=EDGE_LOOP('',(#4390));
#11209=EDGE_LOOP('',(#4391,#4392,#4393,#4394,#4395,#4396,#4397,#4398));
#11210=EDGE_LOOP('',(#4399,#4400,#4401,#4402));
#11211=EDGE_LOOP('',(#4403));
#11212=EDGE_LOOP('',(#4404,#4405,#4406,#4407,#4408,#4409,#4410,#4411));
#11213=EDGE_LOOP('',(#4412,#4413,#4414,#4415));
#11214=EDGE_LOOP('',(#4416));
#11215=EDGE_LOOP('',(#4417,#4418,#4419,#4420,#4421,#4422,#4423,#4424));
#11216=EDGE_LOOP('',(#4425));
#11217=EDGE_LOOP('',(#4426,#4427,#4428,#4429,#4430,#4431,#4432,#4433));
#11218=EDGE_LOOP('',(#4434));
#11219=EDGE_LOOP('',(#4435,#4436,#4437,#4438,#4439,#4440,#4441,#4442));
#11220=EDGE_LOOP('',(#4443,#4444,#4445,#4446));
#11221=EDGE_LOOP('',(#4447));
#11222=EDGE_LOOP('',(#4448,#4449,#4450,#4451,#4452,#4453,#4454,#4455));
#11223=EDGE_LOOP('',(#4456,#4457,#4458,#4459));
#11224=EDGE_LOOP('',(#4460,#4461,#4462,#4463));
#11225=EDGE_LOOP('',(#4464,#4465,#4466,#4467));
#11226=EDGE_LOOP('',(#4468,#4469,#4470,#4471));
#11227=EDGE_LOOP('',(#4472,#4473,#4474,#4475));
#11228=EDGE_LOOP('',(#4476,#4477,#4478,#4479));
#11229=EDGE_LOOP('',(#4480,#4481,#4482,#4483));
#11230=EDGE_LOOP('',(#4484,#4485,#4486,#4487));
#11231=EDGE_LOOP('',(#4488,#4489,#4490,#4491));
#11232=EDGE_LOOP('',(#4492,#4493,#4494,#4495));
#11233=EDGE_LOOP('',(#4496,#4497,#4498,#4499));
#11234=EDGE_LOOP('',(#4500,#4501,#4502,#4503));
#11235=EDGE_LOOP('',(#4504,#4505,#4506,#4507));
#11236=EDGE_LOOP('',(#4508,#4509,#4510,#4511));
#11237=EDGE_LOOP('',(#4512,#4513,#4514,#4515));
#11238=EDGE_LOOP('',(#4516,#4517,#4518,#4519));
#11239=EDGE_LOOP('',(#4520,#4521,#4522,#4523));
#11240=EDGE_LOOP('',(#4524,#4525,#4526,#4527));
#11241=EDGE_LOOP('',(#4528,#4529,#4530,#4531));
#11242=EDGE_LOOP('',(#4532,#4533,#4534,#4535));
#11243=EDGE_LOOP('',(#4536,#4537,#4538,#4539));
#11244=EDGE_LOOP('',(#4540));
#11245=EDGE_LOOP('',(#4541,#4542,#4543,#4544,#4545,#4546,#4547,#4548,#4549,
#4550,#4551));
#11246=EDGE_LOOP('',(#4552,#4553,#4554,#4555,#4556,#4557,#4558,#4559,#4560,
#4561,#4562));
#11247=EDGE_LOOP('',(#4563,#4564,#4565,#4566));
#11248=EDGE_LOOP('',(#4567,#4568,#4569,#4570));
#11249=EDGE_LOOP('',(#4571,#4572,#4573,#4574));
#11250=EDGE_LOOP('',(#4575));
#11251=EDGE_LOOP('',(#4576));
#11252=EDGE_LOOP('',(#4577,#4578,#4579,#4580,#4581,#4582,#4583,#4584,#4585,
#4586,#4587,#4588));
#11253=EDGE_LOOP('',(#4589,#4590,#4591,#4592,#4593,#4594));
#11254=EDGE_LOOP('',(#4595,#4596,#4597,#4598,#4599,#4600,#4601));
#11255=EDGE_LOOP('',(#4602,#4603,#4604,#4605,#4606,#4607,#4608,#4609,#4610,
#4611,#4612));
#11256=EDGE_LOOP('',(#4613,#4614,#4615));
#11257=EDGE_LOOP('',(#4616,#4617,#4618,#4619,#4620));
#11258=EDGE_LOOP('',(#4621,#4622));
#11259=EDGE_LOOP('',(#4623,#4624));
#11260=EDGE_LOOP('',(#4625));
#11261=EDGE_LOOP('',(#4626));
#11262=EDGE_LOOP('',(#4627));
#11263=EDGE_LOOP('',(#4628,#4629));
#11264=EDGE_LOOP('',(#4630));
#11265=EDGE_LOOP('',(#4631,#4632));
#11266=EDGE_LOOP('',(#4633));
#11267=EDGE_LOOP('',(#4634));
#11268=EDGE_LOOP('',(#4635,#4636));
#11269=EDGE_LOOP('',(#4637,#4638,#4639,#4640,#4641,#4642,#4643,#4644,#4645,
#4646,#4647,#4648,#4649,#4650,#4651,#4652,#4653,#4654,#4655));
#11270=EDGE_LOOP('',(#4656,#4657));
#11271=EDGE_LOOP('',(#4658,#4659,#4660,#4661,#4662,#4663,#4664,#4665,#4666,
#4667,#4668,#4669,#4670,#4671,#4672,#4673,#4674));
#11272=EDGE_LOOP('',(#4675));
#11273=EDGE_LOOP('',(#4676));
#11274=EDGE_LOOP('',(#4677));
#11275=EDGE_LOOP('',(#4678));
#11276=EDGE_LOOP('',(#4679));
#11277=EDGE_LOOP('',(#4680));
#11278=EDGE_LOOP('',(#4681));
#11279=EDGE_LOOP('',(#4682));
#11280=EDGE_LOOP('',(#4683));
#11281=EDGE_LOOP('',(#4684,#4685,#4686,#4687,#4688,#4689,#4690,#4691,#4692,
#4693,#4694,#4695));
#11282=EDGE_LOOP('',(#4696));
#11283=EDGE_LOOP('',(#4697,#4698,#4699));
#11284=EDGE_LOOP('',(#4700));
#11285=EDGE_LOOP('',(#4701));
#11286=EDGE_LOOP('',(#4702));
#11287=EDGE_LOOP('',(#4703));
#11288=EDGE_LOOP('',(#4704));
#11289=EDGE_LOOP('',(#4705));
#11290=EDGE_LOOP('',(#4706,#4707));
#11291=EDGE_LOOP('',(#4708));
#11292=EDGE_LOOP('',(#4709));
#11293=EDGE_LOOP('',(#4710));
#11294=EDGE_LOOP('',(#4711));
#11295=EDGE_LOOP('',(#4712));
#11296=EDGE_LOOP('',(#4713));
#11297=EDGE_LOOP('',(#4714));
#11298=EDGE_LOOP('',(#4715));
#11299=EDGE_LOOP('',(#4716,#4717));
#11300=EDGE_LOOP('',(#4718));
#11301=EDGE_LOOP('',(#4719));
#11302=EDGE_LOOP('',(#4720));
#11303=EDGE_LOOP('',(#4721));
#11304=EDGE_LOOP('',(#4722));
#11305=EDGE_LOOP('',(#4723));
#11306=EDGE_LOOP('',(#4724));
#11307=EDGE_LOOP('',(#4725));
#11308=EDGE_LOOP('',(#4726));
#11309=EDGE_LOOP('',(#4727));
#11310=EDGE_LOOP('',(#4728));
#11311=EDGE_LOOP('',(#4729));
#11312=EDGE_LOOP('',(#4730,#4731,#4732,#4733));
#11313=EDGE_LOOP('',(#4734,#4735,#4736,#4737));
#11314=EDGE_LOOP('',(#4738,#4739,#4740,#4741));
#11315=EDGE_LOOP('',(#4742));
#11316=EDGE_LOOP('',(#4743));
#11317=EDGE_LOOP('',(#4744,#4745,#4746,#4747));
#11318=EDGE_LOOP('',(#4748,#4749,#4750,#4751));
#11319=EDGE_LOOP('',(#4752,#4753,#4754,#4755));
#12319=FACE_BOUND('',#11200,.T.);
#12320=FACE_BOUND('',#11201,.T.);
#12321=FACE_BOUND('',#11202,.T.);
#12322=FACE_BOUND('',#11203,.T.);
#12323=FACE_BOUND('',#11204,.T.);
#12324=FACE_BOUND('',#11205,.T.);
#12325=FACE_BOUND('',#11206,.T.);
#12326=FACE_BOUND('',#11207,.T.);
#12327=FACE_BOUND('',#11208,.T.);
#12328=FACE_BOUND('',#11209,.T.);
#12329=FACE_BOUND('',#11210,.T.);
#12330=FACE_BOUND('',#11211,.T.);
#12331=FACE_BOUND('',#11212,.T.);
#12332=FACE_BOUND('',#11213,.T.);
#12333=FACE_BOUND('',#11214,.T.);
#12334=FACE_BOUND('',#11215,.T.);
#12335=FACE_BOUND('',#11216,.T.);
#12336=FACE_BOUND('',#11217,.T.);
#12337=FACE_BOUND('',#11218,.T.);
#12338=FACE_BOUND('',#11219,.T.);
#12339=FACE_BOUND('',#11220,.T.);
#12340=FACE_BOUND('',#11221,.T.);
#12341=FACE_BOUND('',#11222,.T.);
#12342=FACE_BOUND('',#11223,.T.);
#12343=FACE_BOUND('',#11224,.T.);
#12344=FACE_BOUND('',#11225,.T.);
#12345=FACE_BOUND('',#11226,.T.);
#12346=FACE_BOUND('',#11227,.T.);
#12347=FACE_BOUND('',#11228,.T.);
#12348=FACE_BOUND('',#11229,.T.);
#12349=FACE_BOUND('',#11230,.T.);
#12350=FACE_BOUND('',#11231,.T.);
#12351=FACE_BOUND('',#11232,.T.);
#12352=FACE_BOUND('',#11233,.T.);
#12353=FACE_BOUND('',#11234,.T.);
#12354=FACE_BOUND('',#11235,.T.);
#12355=FACE_BOUND('',#11236,.T.);
#12356=FACE_BOUND('',#11237,.T.);
#12357=FACE_BOUND('',#11238,.T.);
#12358=FACE_BOUND('',#11239,.T.);
#12359=FACE_BOUND('',#11240,.T.);
#12360=FACE_BOUND('',#11241,.T.);
#12361=FACE_BOUND('',#11242,.T.);
#12362=FACE_BOUND('',#11243,.T.);
#12363=FACE_BOUND('',#11244,.T.);
#12364=FACE_BOUND('',#11245,.T.);
#12365=FACE_BOUND('',#11246,.T.);
#12366=FACE_BOUND('',#11247,.T.);
#12367=FACE_BOUND('',#11248,.T.);
#12368=FACE_BOUND('',#11249,.T.);
#12369=FACE_BOUND('',#11250,.T.);
#12370=FACE_BOUND('',#11251,.T.);
#12371=FACE_BOUND('',#11252,.T.);
#12372=FACE_BOUND('',#11253,.T.);
#12373=FACE_BOUND('',#11254,.T.);
#12374=FACE_BOUND('',#11255,.T.);
#12375=FACE_BOUND('',#11256,.T.);
#12376=FACE_BOUND('',#11257,.T.);
#12377=FACE_BOUND('',#11258,.T.);
#12378=FACE_BOUND('',#11259,.T.);
#12379=FACE_BOUND('',#11260,.T.);
#12380=FACE_BOUND('',#11261,.T.);
#12381=FACE_BOUND('',#11262,.T.);
#12382=FACE_BOUND('',#11263,.T.);
#12383=FACE_BOUND('',#11264,.T.);
#12384=FACE_BOUND('',#11265,.T.);
#12385=FACE_BOUND('',#11266,.T.);
#12386=FACE_BOUND('',#11267,.T.);
#12387=FACE_BOUND('',#11268,.T.);
#12388=FACE_BOUND('',#11269,.T.);
#12389=FACE_BOUND('',#11270,.T.);
#12390=FACE_BOUND('',#11271,.T.);
#12391=FACE_BOUND('',#11272,.T.);
#12392=FACE_BOUND('',#11273,.T.);
#12393=FACE_BOUND('',#11274,.T.);
#12394=FACE_BOUND('',#11275,.T.);
#12395=FACE_BOUND('',#11276,.T.);
#12396=FACE_BOUND('',#11277,.T.);
#12397=FACE_BOUND('',#11278,.T.);
#12398=FACE_BOUND('',#11279,.T.);
#12399=FACE_BOUND('',#11280,.T.);
#12400=FACE_BOUND('',#11281,.T.);
#12401=FACE_BOUND('',#11282,.T.);
#12402=FACE_BOUND('',#11283,.T.);
#12403=FACE_BOUND('',#11284,.T.);
#12404=FACE_BOUND('',#11285,.T.);
#12405=FACE_BOUND('',#11286,.T.);
#12406=FACE_BOUND('',#11287,.T.);
#12407=FACE_BOUND('',#11288,.T.);
#12408=FACE_BOUND('',#11289,.T.);
#12409=FACE_BOUND('',#11290,.T.);
#12410=FACE_BOUND('',#11291,.T.);
#12411=FACE_BOUND('',#11292,.T.);
#12412=FACE_BOUND('',#11293,.T.);
#12413=FACE_BOUND('',#11294,.T.);
#12414=FACE_BOUND('',#11295,.T.);
#12415=FACE_BOUND('',#11296,.T.);
#12416=FACE_BOUND('',#11297,.T.);
#12417=FACE_BOUND('',#11298,.T.);
#12418=FACE_BOUND('',#11299,.T.);
#12419=FACE_BOUND('',#11300,.T.);
#12420=FACE_BOUND('',#11301,.T.);
#12421=FACE_BOUND('',#11302,.T.);
#12422=FACE_BOUND('',#11303,.T.);
#12423=FACE_BOUND('',#11304,.T.);
#12424=FACE_BOUND('',#11305,.T.);
#12425=FACE_BOUND('',#11306,.T.);
#12426=FACE_BOUND('',#11307,.T.);
#12427=FACE_BOUND('',#11308,.T.);
#12428=FACE_BOUND('',#11309,.T.);
#12429=FACE_BOUND('',#11310,.T.);
#12430=FACE_BOUND('',#11311,.T.);
#12431=FACE_BOUND('',#11312,.T.);
#12432=FACE_BOUND('',#11313,.T.);
#12433=FACE_BOUND('',#11314,.T.);
#12434=FACE_BOUND('',#11315,.T.);
#12435=FACE_BOUND('',#11316,.T.);
#12436=FACE_BOUND('',#11317,.T.);
#12437=FACE_BOUND('',#11318,.T.);
#12438=FACE_BOUND('',#11319,.T.);
#12686=(
BOUNDED_SURFACE()
B_SPLINE_SURFACE(1,2,((#35593,#35594,#35595,#35596,#35597,#35598,#35599,
#35600,#35601,#35602,#35603,#35604,#35605,#35606,#35607,#35608,#35609,#35610,
#35611,#35612,#35613,#35614,#35615,#35616,#35617,#35618,#35619,#35620,#35621,
#35622,#35623,#35624,#35625,#35626,#35627,#35628,#35629,#35630,#35631,#35632,
#35633,#35634,#35635,#35636,#35637,#35638,#35639,#35640,#35641,#35642,#35643,
#35644,#35645,#35646,#35647,#35648,#35649,#35650,#35651,#35652,#35653,#35654,
#35655,#35656,#35657),(#35658,#35659,#35660,#35661,#35662,#35663,#35664,
#35665,#35666,#35667,#35668,#35669,#35670,#35671,#35672,#35673,#35674,#35675,
#35676,#35677,#35678,#35679,#35680,#35681,#35682,#35683,#35684,#35685,#35686,
#35687,#35688,#35689,#35690,#35691,#35692,#35693,#35694,#35695,#35696,#35697,
#35698,#35699,#35700,#35701,#35702,#35703,#35704,#35705,#35706,#35707,#35708,
#35709,#35710,#35711,#35712,#35713,#35714,#35715,#35716,#35717,#35718,#35719,
#35720,#35721,#35722)),.RULED_SURF.,.F.,.F.,.F.)
B_SPLINE_SURFACE_WITH_KNOTS((2,2),(3,2,2,2,2,2,2,2,2,2,2,2,2,2,2,2,2,2,
2,2,2,2,2,2,2,2,2,2,2,2,2,2,3),(0.,1.),(0.,0.03125,0.0625,0.09375,0.125,
0.15625,0.1875,0.21875,0.25,0.28125,0.3125,0.34375,0.375,0.40625,0.4375,
0.46875,0.5,0.53125,0.5625,0.59375,0.625,0.65625,0.6875,0.71875,0.75,0.78125,
0.8125,0.84375,0.875,0.90625,0.9375,0.96875,1.),.UNSPECIFIED.)
GEOMETRIC_REPRESENTATION_ITEM()
RATIONAL_B_SPLINE_SURFACE(((1.,0.923879532511287,1.,0.923879532511287,1.,
0.923879532511287,1.,0.923879532511287,1.,0.923879532511287,1.,0.923879532511287,
1.,0.923879532511287,1.,0.923879532511287,1.,0.923879532511287,1.,0.923879532511287,
1.,0.923879532511287,1.,0.923879532511287,1.,0.923879532511287,1.,0.923879532511287,
1.,0.923879532511287,1.,0.923879532511287,1.,0.923879532511287,1.,0.923879532511287,
1.,0.923879532511287,1.,0.923879532511287,1.,0.923879532511287,1.,0.923879532511287,
1.,0.923879532511287,1.,0.923879532511287,1.,0.923879532511287,1.,0.923879532511287,
1.,0.923879532511287,1.,0.923879532511287,1.,0.923879532511287,1.,0.923879532511287,
1.,0.923879532511287,1.,0.923879532511287,1.),(1.,0.923879532511287,1.,
0.923879532511287,1.,0.923879532511287,1.,0.923879532511287,1.,0.923879532511287,
1.,0.923879532511287,1.,0.923879532511287,1.,0.923879532511287,1.,0.923879532511287,
1.,0.923879532511287,1.,0.923879532511287,1.,0.923879532511287,1.,0.923879532511287,
1.,0.923879532511287,1.,0.923879532511287,1.,0.923879532511287,1.,0.923879532511287,
1.,0.923879532511287,1.,0.923879532511287,1.,0.923879532511287,1.,0.923879532511287,
1.,0.923879532511287,1.,0.923879532511287,1.,0.923879532511287,1.,0.923879532511287,
1.,0.923879532511287,1.,0.923879532511287,1.,0.923879532511287,1.,0.923879532511287,
1.,0.923879532511287,1.,0.923879532511287,1.,0.923879532511287,1.)))
REPRESENTATION_ITEM('')
SURFACE()
);
#12687=(
BOUNDED_SURFACE()
B_SPLINE_SURFACE(1,2,((#35873,#35874,#35875,#35876,#35877,#35878,#35879,
#35880,#35881,#35882,#35883,#35884,#35885,#35886,#35887,#35888,#35889,#35890,
#35891,#35892,#35893,#35894,#35895,#35896,#35897,#35898,#35899,#35900,#35901,
#35902,#35903,#35904,#35905,#35906,#35907,#35908,#35909,#35910,#35911,#35912,
#35913,#35914,#35915,#35916,#35917,#35918,#35919,#35920,#35921,#35922,#35923,
#35924,#35925,#35926,#35927,#35928,#35929,#35930,#35931,#35932,#35933,#35934,
#35935,#35936,#35937),(#35938,#35939,#35940,#35941,#35942,#35943,#35944,
#35945,#35946,#35947,#35948,#35949,#35950,#35951,#35952,#35953,#35954,#35955,
#35956,#35957,#35958,#35959,#35960,#35961,#35962,#35963,#35964,#35965,#35966,
#35967,#35968,#35969,#35970,#35971,#35972,#35973,#35974,#35975,#35976,#35977,
#35978,#35979,#35980,#35981,#35982,#35983,#35984,#35985,#35986,#35987,#35988,
#35989,#35990,#35991,#35992,#35993,#35994,#35995,#35996,#35997,#35998,#35999,
#36000,#36001,#36002)),.RULED_SURF.,.F.,.F.,.F.)
B_SPLINE_SURFACE_WITH_KNOTS((2,2),(3,2,2,2,2,2,2,2,2,2,2,2,2,2,2,2,2,2,
2,2,2,2,2,2,2,2,2,2,2,2,2,2,3),(0.,1.),(0.,0.03125,0.0625,0.09375,0.125,
0.15625,0.1875,0.21875,0.25,0.28125,0.3125,0.34375,0.375,0.40625,0.4375,
0.46875,0.5,0.53125,0.5625,0.59375,0.625,0.65625,0.6875,0.71875,0.75,0.78125,
0.8125,0.84375,0.875,0.90625,0.9375,0.96875,1.),.UNSPECIFIED.)
GEOMETRIC_REPRESENTATION_ITEM()
RATIONAL_B_SPLINE_SURFACE(((1.,0.923879532511287,1.,0.923879532511287,1.,
0.923879532511287,1.,0.923879532511287,1.,0.923879532511287,1.,0.923879532511287,
1.,0.923879532511287,1.,0.923879532511287,1.,0.923879532511287,1.,0.923879532511287,
1.,0.923879532511287,1.,0.923879532511287,1.,0.923879532511287,1.,0.923879532511287,
1.,0.923879532511287,1.,0.923879532511287,1.,0.923879532511287,1.,0.923879532511287,
1.,0.923879532511287,1.,0.923879532511287,1.,0.923879532511287,1.,0.923879532511287,
1.,0.923879532511287,1.,0.923879532511287,1.,0.923879532511287,1.,0.923879532511287,
1.,0.923879532511287,1.,0.923879532511287,1.,0.923879532511287,1.,0.923879532511287,
1.,0.923879532511287,1.,0.923879532511287,1.),(1.,0.923879532511287,1.,
0.923879532511287,1.,0.923879532511287,1.,0.923879532511287,1.,0.923879532511287,
1.,0.923879532511287,1.,0.923879532511287,1.,0.923879532511287,1.,0.923879532511287,
1.,0.923879532511287,1.,0.923879532511287,1.,0.923879532511287,1.,0.923879532511287,
1.,0.923879532511287,1.,0.923879532511287,1.,0.923879532511287,1.,0.923879532511287,
1.,0.923879532511287,1.,0.923879532511287,1.,0.923879532511287,1.,0.923879532511287,
1.,0.923879532511287,1.,0.923879532511287,1.,0.923879532511287,1.,0.923879532511287,
1.,0.923879532511287,1.,0.923879532511287,1.,0.923879532511287,1.,0.923879532511287,
1.,0.923879532511287,1.,0.923879532511287,1.,0.923879532511287,1.)))
REPRESENTATION_ITEM('')
SURFACE()
);
#12688=(
BOUNDED_SURFACE()
B_SPLINE_SURFACE(3,2,((#36164,#36165,#36166),(#36167,#36168,#36169),(#36170,
#36171,#36172),(#36173,#36174,#36175),(#36176,#36177,#36178),(#36179,#36180,
#36181),(#36182,#36183,#36184),(#36185,#36186,#36187),(#36188,#36189,#36190),
(#36191,#36192,#36193),(#36194,#36195,#36196),(#36197,#36198,#36199),(#36200,
#36201,#36202),(#36203,#36204,#36205),(#36206,#36207,#36208),(#36209,#36210,
#36211),(#36212,#36213,#36214),(#36215,#36216,#36217),(#36218,#36219,#36220),
(#36221,#36222,#36223),(#36224,#36225,#36226),(#36227,#36228,#36229),(#36230,
#36231,#36232),(#36233,#36234,#36235),(#36236,#36237,#36238),(#36239,#36240,
#36241),(#36242,#36243,#36244),(#36245,#36246,#36247),(#36248,#36249,#36250),
(#36251,#36252,#36253),(#36254,#36255,#36256),(#36257,#36258,#36259),(#36260,
#36261,#36262),(#36263,#36264,#36265),(#36266,#36267,#36268),(#36269,#36270,
#36271),(#36272,#36273,#36274),(#36275,#36276,#36277),(#36278,#36279,#36280),
(#36281,#36282,#36283),(#36284,#36285,#36286),(#36287,#36288,#36289),(#36290,
#36291,#36292),(#36293,#36294,#36295),(#36296,#36297,#36298),(#36299,#36300,
#36301),(#36302,#36303,#36304),(#36305,#36306,#36307),(#36308,#36309,#36310),
(#36311,#36312,#36313),(#36314,#36315,#36316),(#36317,#36318,#36319),(#36320,
#36321,#36322),(#36323,#36324,#36325),(#36326,#36327,#36328),(#36329,#36330,
#36331),(#36332,#36333,#36334),(#36335,#36336,#36337),(#36338,#36339,#36340),
(#36341,#36342,#36343),(#36344,#36345,#36346),(#36347,#36348,#36349),(#36350,
#36351,#36352),(#36353,#36354,#36355),(#36356,#36357,#36358),(#36359,#36360,
#36361),(#36362,#36363,#36364),(#36365,#36366,#36367),(#36368,#36369,#36370),
(#36371,#36372,#36373),(#36374,#36375,#36376),(#36377,#36378,#36379),(#36380,
#36381,#36382),(#36383,#36384,#36385),(#36386,#36387,#36388),(#36389,#36390,
#36391),(#36392,#36393,#36394),(#36395,#36396,#36397),(#36398,#36399,#36400),
(#36401,#36402,#36403),(#36404,#36405,#36406),(#36407,#36408,#36409),(#36410,
#36411,#36412),(#36413,#36414,#36415),(#36416,#36417,#36418),(#36419,#36420,
#36421),(#36422,#36423,#36424),(#36425,#36426,#36427),(#36428,#36429,#36430),
(#36431,#36432,#36433),(#36434,#36435,#36436),(#36437,#36438,#36439),(#36440,
#36441,#36442),(#36443,#36444,#36445),(#36446,#36447,#36448),(#36449,#36450,
#36451),(#36452,#36453,#36454),(#36455,#36456,#36457),(#36458,#36459,#36460),
(#36461,#36462,#36463),(#36464,#36465,#36466),(#36467,#36468,#36469),(#36470,
#36471,#36472),(#36473,#36474,#36475),(#36476,#36477,#36478),(#36479,#36480,
#36481),(#36482,#36483,#36484),(#36485,#36486,#36487),(#36488,#36489,#36490),
(#36491,#36492,#36493),(#36494,#36495,#36496),(#36497,#36498,#36499),(#36500,
#36501,#36502),(#36503,#36504,#36505),(#36506,#36507,#36508),(#36509,#36510,
#36511),(#36512,#36513,#36514),(#36515,#36516,#36517),(#36518,#36519,#36520),
(#36521,#36522,#36523),(#36524,#36525,#36526),(#36527,#36528,#36529),(#36530,
#36531,#36532),(#36533,#36534,#36535),(#36536,#36537,#36538),(#36539,#36540,
#36541),(#36542,#36543,#36544),(#36545,#36546,#36547),(#36548,#36549,#36550),
(#36551,#36552,#36553),(#36554,#36555,#36556),(#36557,#36558,#36559),(#36560,
#36561,#36562),(#36563,#36564,#36565),(#36566,#36567,#36568),(#36569,#36570,
#36571),(#36572,#36573,#36574),(#36575,#36576,#36577),(#36578,#36579,#36580),
(#36581,#36582,#36583),(#36584,#36585,#36586),(#36587,#36588,#36589),(#36590,
#36591,#36592),(#36593,#36594,#36595),(#36596,#36597,#36598),(#36599,#36600,
#36601),(#36602,#36603,#36604),(#36605,#36606,#36607),(#36608,#36609,#36610),
(#36611,#36612,#36613),(#36614,#36615,#36616),(#36617,#36618,#36619),(#36620,
#36621,#36622),(#36623,#36624,#36625),(#36626,#36627,#36628),(#36629,#36630,
#36631),(#36632,#36633,#36634),(#36635,#36636,#36637),(#36638,#36639,#36640),
(#36641,#36642,#36643),(#36644,#36645,#36646),(#36647,#36648,#36649),(#36650,
#36651,#36652),(#36653,#36654,#36655),(#36656,#36657,#36658),(#36659,#36660,
#36661),(#36662,#36663,#36664),(#36665,#36666,#36667),(#36668,#36669,#36670),
(#36671,#36672,#36673),(#36674,#36675,#36676),(#36677,#36678,#36679),(#36680,
#36681,#36682),(#36683,#36684,#36685),(#36686,#36687,#36688),(#36689,#36690,
#36691),(#36692,#36693,#36694),(#36695,#36696,#36697),(#36698,#36699,#36700),
(#36701,#36702,#36703),(#36704,#36705,#36706),(#36707,#36708,#36709),(#36710,
#36711,#36712),(#36713,#36714,#36715),(#36716,#36717,#36718),(#36719,#36720,
#36721),(#36722,#36723,#36724),(#36725,#36726,#36727),(#36728,#36729,#36730),
(#36731,#36732,#36733),(#36734,#36735,#36736),(#36737,#36738,#36739),(#36740,
#36741,#36742),(#36743,#36744,#36745),(#36746,#36747,#36748),(#36749,#36750,
#36751),(#36752,#36753,#36754),(#36755,#36756,#36757),(#36758,#36759,#36760),
(#36761,#36762,#36763),(#36764,#36765,#36766),(#36767,#36768,#36769),(#36770,
#36771,#36772),(#36773,#36774,#36775),(#36776,#36777,#36778),(#36779,#36780,
#36781),(#36782,#36783,#36784),(#36785,#36786,#36787),(#36788,#36789,#36790),
(#36791,#36792,#36793),(#36794,#36795,#36796),(#36797,#36798,#36799),(#36800,
#36801,#36802),(#36803,#36804,#36805),(#36806,#36807,#36808),(#36809,#36810,
#36811),(#36812,#36813,#36814),(#36815,#36816,#36817),(#36818,#36819,#36820),
(#36821,#36822,#36823),(#36824,#36825,#36826),(#36827,#36828,#36829),(#36830,
#36831,#36832),(#36833,#36834,#36835),(#36836,#36837,#36838),(#36839,#36840,
#36841),(#36842,#36843,#36844),(#36845,#36846,#36847),(#36848,#36849,#36850),
(#36851,#36852,#36853),(#36854,#36855,#36856),(#36857,#36858,#36859),(#36860,
#36861,#36862),(#36863,#36864,#36865),(#36866,#36867,#36868),(#36869,#36870,
#36871),(#36872,#36873,#36874),(#36875,#36876,#36877),(#36878,#36879,#36880),
(#36881,#36882,#36883),(#36884,#36885,#36886),(#36887,#36888,#36889),(#36890,
#36891,#36892),(#36893,#36894,#36895),(#36896,#36897,#36898),(#36899,#36900,
#36901),(#36902,#36903,#36904),(#36905,#36906,#36907),(#36908,#36909,#36910),
(#36911,#36912,#36913),(#36914,#36915,#36916),(#36917,#36918,#36919),(#36920,
#36921,#36922),(#36923,#36924,#36925),(#36926,#36927,#36928),(#36929,#36930,
#36931),(#36932,#36933,#36934),(#36935,#36936,#36937),(#36938,#36939,#36940),
(#36941,#36942,#36943),(#36944,#36945,#36946),(#36947,#36948,#36949),(#36950,
#36951,#36952),(#36953,#36954,#36955),(#36956,#36957,#36958),(#36959,#36960,
#36961),(#36962,#36963,#36964),(#36965,#36966,#36967),(#36968,#36969,#36970),
(#36971,#36972,#36973),(#36974,#36975,#36976),(#36977,#36978,#36979),(#36980,
#36981,#36982),(#36983,#36984,#36985),(#36986,#36987,#36988),(#36989,#36990,
#36991),(#36992,#36993,#36994),(#36995,#36996,#36997),(#36998,#36999,#37000),
(#37001,#37002,#37003),(#37004,#37005,#37006),(#37007,#37008,#37009),(#37010,
#37011,#37012),(#37013,#37014,#37015),(#37016,#37017,#37018),(#37019,#37020,
#37021),(#37022,#37023,#37024),(#37025,#37026,#37027),(#37028,#37029,#37030),
(#37031,#37032,#37033),(#37034,#37035,#37036),(#37037,#37038,#37039),(#37040,
#37041,#37042),(#37043,#37044,#37045),(#37046,#37047,#37048),(#37049,#37050,
#37051),(#37052,#37053,#37054),(#37055,#37056,#37057),(#37058,#37059,#37060),
(#37061,#37062,#37063),(#37064,#37065,#37066),(#37067,#37068,#37069),(#37070,
#37071,#37072),(#37073,#37074,#37075),(#37076,#37077,#37078),(#37079,#37080,
#37081),(#37082,#37083,#37084),(#37085,#37086,#37087),(#37088,#37089,#37090),
(#37091,#37092,#37093),(#37094,#37095,#37096),(#37097,#37098,#37099),(#37100,
#37101,#37102),(#37103,#37104,#37105),(#37106,#37107,#37108),(#37109,#37110,
#37111),(#37112,#37113,#37114),(#37115,#37116,#37117),(#37118,#37119,#37120),
(#37121,#37122,#37123),(#37124,#37125,#37126),(#37127,#37128,#37129),(#37130,
#37131,#37132),(#37133,#37134,#37135),(#37136,#37137,#37138),(#37139,#37140,
#37141),(#37142,#37143,#37144),(#37145,#37146,#37147),(#37148,#37149,#37150),
(#37151,#37152,#37153),(#37154,#37155,#37156),(#37157,#37158,#37159),(#37160,
#37161,#37162),(#37163,#37164,#37165),(#37166,#37167,#37168),(#37169,#37170,
#37171),(#37172,#37173,#37174),(#37175,#37176,#37177),(#37178,#37179,#37180),
(#37181,#37182,#37183),(#37184,#37185,#37186),(#37187,#37188,#37189),(#37190,
#37191,#37192),(#37193,#37194,#37195),(#37196,#37197,#37198),(#37199,#37200,
#37201),(#37202,#37203,#37204),(#37205,#37206,#37207),(#37208,#37209,#37210),
(#37211,#37212,#37213)),.UNSPECIFIED.,.F.,.F.,.F.)
B_SPLINE_SURFACE_WITH_KNOTS((4,2,2,2,2,2,2,2,2,2,2,2,2,2,2,2,2,2,2,2,2,
2,2,2,2,2,2,2,2,2,2,2,2,2,2,2,2,2,2,2,2,2,2,2,2,2,2,2,2,2,2,2,2,2,2,2,2,
2,2,2,2,2,2,2,2,2,2,2,2,2,2,2,2,2,2,2,2,2,2,2,2,2,2,2,2,2,2,2,2,2,2,2,2,
2,2,2,2,2,2,2,2,2,2,2,2,2,2,2,2,2,2,2,2,2,2,2,2,2,2,2,2,2,2,2,2,2,2,2,2,
2,2,2,2,2,2,2,2,2,2,2,2,2,2,2,2,2,2,2,2,2,2,2,2,2,2,2,2,2,2,2,2,2,2,2,2,
2,2,2,2,2,2,2,2,2,4),(3,3),(0.193149276135837,0.194573475589254,0.19599767504267,
0.197421874496086,0.198846073949502,0.201694472856334,0.203118672309751,
0.204542871763166,0.207391270669999,0.208815470123415,0.210239669576831,
0.213088068483663,0.21451226793708,0.215936467390495,0.218784866297328,
0.22163326520416,0.223057464657577,0.224481664110992,0.227330063017825,
0.228754262471241,0.230178461924657,0.233026860831489,0.234451060284905,
0.235875259738322,0.238723658645154,0.241572057551987,0.244420456458819,
0.247268855365651,0.248693054819067,0.250117254272483,0.252965653179316,
0.255814052086148,0.25866245099298,0.260086650446396,0.261510849899812,
0.264359248806645,0.267207647713477,0.27005604662031,0.272904445527142,
0.274328644980558,0.275752844433974,0.278601243340806,0.280025442794223,
0.281449642247639,0.284298041154471,0.285722240607887,0.287146440061304,
0.289994838968135,0.292843237874968,0.294267437328384,0.2956916367818,0.298540035688632,
0.299964235142049,0.301388434595465,0.304236833502297,0.305661032955714,
0.307085232409129,0.309933631315962,0.311357830769378,0.312782030222794,
0.315630429129626,0.318478828036458,0.319903027489875,0.321327226943291,
0.324175625850124,0.32559982530354,0.327024024756956,0.329872423663788,
0.331296623117204,0.33272082257062,0.335569221477452,0.336993420930868,
0.338417620384285,0.341266019291117,0.344114418197949,0.345538617651366,
0.346962817104781,0.349811216011614,0.35123541546503,0.352659614918446,
0.355508013825279,0.356932213278695,0.358356412732111,0.361204811638944,
0.364053210545775,0.366901609452608,0.36975000835944,0.371174207812856,
0.372598407266273,0.375446806173105,0.378295205079937,0.381143603986769,
0.383992002893602,0.385416202347018,0.386840401800434,0.389688800707267,
0.392537199614098,0.395385598520931,0.398233997427763,0.39965819688118,
0.401082396334596,0.403930795241428,0.40677919414826,0.409627593055092,
0.411051792508509,0.412475991961925,0.415324390868757,0.418172789775589,
0.421021188682421,0.423869587589254,0.42529378704267,0.426717986496086,
0.429566385402918,0.432414784309751,0.435263183216583,0.43668738267,0.438111582123415,
0.440959981030248,0.44380837993708,0.446656778843912,0.449505177750745,
0.450929377204161,0.452353576657577,0.455201975564409,0.456626175017826,
0.458050374471242,0.460898773378074,0.46232297283149,0.463747172284906,
0.466595571191739,0.469443970098571,0.470868169551987,0.472292369005403,
0.475140767912236,0.476564967365652,0.477989166819068,0.4808375657259,0.482261765179316,
0.483685964632732,0.486534363539565,0.487958562992981,0.489382762446397,
0.492231161353229,0.495079560260062,0.496503759713478,0.497927959166894,
0.500776358073726,0.502200557527142,0.503624756980559,0.506473155887391,
0.507897355340807,0.509321554794223,0.512169953701055,0.513594153154472,
0.515018352607888,0.51786675151472,0.520715150421552,0.522139349874969,
0.523563549328385,0.526411948235217,0.527836147688633,0.529260347142049,
0.532108746048882,0.533532945502298,0.534957144955714,0.537805543862546,
0.540653942769379,0.543502341676211,0.546350740583043,0.547774940036459,
0.549199139489875,0.552047538396708,0.55489593730354,0.556320136756956,
0.557744336210372),(0.,1.),.UNSPECIFIED.)
GEOMETRIC_REPRESENTATION_ITEM()
RATIONAL_B_SPLINE_SURFACE(((1.,0.722699314797039,1.),(1.,0.739505233921062,
1.),(1.,0.750913931065822,1.),(1.,0.763867107266192,1.),(1.,0.763748327602808,
1.),(1.,0.763840788023146,1.),(1.,0.763934660767682,1.),(1.,0.764075220899086,
1.),(1.,0.764122201658888,1.),(1.,0.764124519516567,1.),(1.,0.763899183527604,
1.),(1.,0.763724776258188,1.),(1.,0.763718186244016,1.),(1.,0.763733433596857,
1.),(1.,0.763753474169701,1.),(1.,0.76378697338056,1.),(1.,0.763752776696806,
1.),(1.,0.763751538604513,1.),(1.,0.763763940574543,1.),(1.,0.76396102079176,
1.),(1.,0.764115220844393,1.),(1.,0.764546159205604,1.),(1.,0.764765645744293,
1.),(1.,0.764727907314652,1.),(1.,0.764660932529331,1.),(1.,0.764455367186594,
1.),(1.,0.764316238910568,1.),(1.,0.763935188171349,1.),(1.,0.763859972893716,
1.),(1.,0.764274012465505,1.),(1.,0.76457343122981,1.),(1.,0.764686738337569,
1.),(1.,0.764674014513268,1.),(1.,0.764551476703936,1.),(1.,0.764442146422493,
1.),(1.,0.764057990860656,1.),(1.,0.763712262722046,1.),(1.,0.763810315046671,
1.),(1.,0.763927911530464,1.),(1.,0.764191701339472,1.),(1.,0.764336047024834,
1.),(1.,0.764669419545292,1.),(1.,0.764732856732067,1.),(1.,0.764530427751721,
1.),(1.,0.764419860629288,1.),(1.,0.764182994716093,1.),(1.,0.764056864941671,
1.),(1.,0.763847972269309,1.),(1.,0.764090105631719,1.),(1.,0.764557854644049,
1.),(1.,0.764727075408901,1.),(1.,0.764592469893156,1.),(1.,0.76429205517341,
1.),(1.,0.763778933821465,1.),(1.,0.763714479620357,1.),(1.,0.764064348110842,
1.),(1.,0.764214432578513,1.),(1.,0.764468330597694,1.),(1.,0.76457255700642,
1.),(1.,0.764738627262064,1.),(1.,0.764627762575867,1.),(1.,0.764184080030961,
1.),(1.,0.763869939463043,1.),(1.,0.764028580212725,1.),(1.,0.764371448031126,
1.),(1.,0.764629675614398,1.),(1.,0.764679319927948,1.),(1.,0.764673366372952,
1.),(1.,0.764617034573576,1.),(1.,0.76432860904734,1.),(1.,0.763955320692206,
1.),(1.,0.763676394380582,1.),(1.,0.763950171983398,1.),(1.,0.764492856603529,
1.),(1.,0.764699044829153,1.),(1.,0.764646790603644,1.),(1.,0.764389512112811,
1.),(1.,0.764047552656364,1.),(1.,0.763947820879635,1.),(1.,0.7639238839966,
1.),(1.,0.764008346032025,1.),(1.,0.764331498413827,1.),(1.,0.764611886319225,
1.),(1.,0.764692272869539,1.),(1.,0.764668655970716,1.),(1.,0.764526003286365,
1.),(1.,0.764407585602509,1.),(1.,0.76401108352945,1.),(1.,0.763691597605849,
1.),(1.,0.763839790873091,1.),(1.,0.763964817595917,1.),(1.,0.764232389234053,
1.),(1.,0.764375097736406,1.),(1.,0.764691651150716,1.),(1.,0.764728274974876,
1.),(1.,0.764425962489577,1.),(1.,0.76408640921874,1.),(1.,0.763910378354219,
1.),(1.,0.763940222092509,1.),(1.,0.764114492355252,1.),(1.,0.764244146959905,
1.),(1.,0.764588972482738,1.),(1.,0.764734205927101,1.),(1.,0.764606540240188,
1.),(1.,0.764512157040054,1.),(1.,0.764269236036256,1.),(1.,0.764121427321446,
1.),(1.,0.763749143028262,1.),(1.,0.763738472511642,1.),(1.,0.764104348255375,
1.),(1.,0.764252603446921,1.),(1.,0.764499401472594,1.),(1.,0.764596727279848,
1.),(1.,0.764735435145248,1.),(1.,0.764599860555111,1.),(1.,0.764258563412971,
1.),(1.,0.764128257509806,1.),(1.,0.763947151915775,1.),(1.,0.763909077799273,
1.),(1.,0.764069787586111,1.),(1.,0.764411198803846,1.),(1.,0.76472602456633,
1.),(1.,0.764699635747033,1.),(1.,0.764390238431946,1.),(1.,0.764249113212434,
1.),(1.,0.76398024343851,1.),(1.,0.76385228181124,1.),(1.,0.763685718677883,
1.),(1.,0.763993094277294,1.),(1.,0.764392354435882,1.),(1.,0.764513634094182,
1.),(1.,0.764662651735703,1.),(1.,0.764690398115232,1.),(1.,0.764621689213982,
1.),(1.,0.764347939142106,1.),(1.,0.764019298699886,1.),(1.,0.76392987954948,
1.),(1.,0.763939856257347,1.),(1.,0.764035977098891,1.),(1.,0.764373733783113,
1.),(1.,0.764638010806738,1.),(1.,0.764689070469253,1.),(1.,0.764655118678298,
1.),(1.,0.764497116908555,1.),(1.,0.764372434889717,1.),(1.,0.763967351373681,
1.),(1.,0.763679332198018,1.),(1.,0.763936049040803,1.),(1.,0.764310708178265,
1.),(1.,0.764607884141716,1.),(1.,0.764667933623475,1.),(1.,0.764681694245897,
1.),(1.,0.764636097985227,1.),(1.,0.764386747051517,1.),(1.,0.764045117651283,
1.),(1.,0.763908872524616,1.),(1.,0.76395754226787,1.),(1.,0.764149013532703,
1.),(1.,0.764280900945993,1.),(1.,0.764617975384813,1.),(1.,0.764738649656064,
1.),(1.,0.764583519945107,1.),(1.,0.764482287442958,1.),(1.,0.764230946224071,
1.),(1.,0.764080793566669,1.),(1.,0.763723362703644,1.),(1.,0.763766722502332,
1.),(1.,0.76427291441918,1.),(1.,0.764580062163821,1.),(1.,0.764729453155635,
1.),(1.,0.764569528540465,1.),(1.,0.764105164381652,1.),(1.,0.763848474045922,
1.),(1.,0.764044371934837,1.),(1.,0.76416925555259,1.),(1.,0.764407167526877,
1.),(1.,0.764520334285805,1.),(1.,0.764733406914302,1.),(1.,0.764680756093071,
1.),(1.,0.764245428286248,1.),(1.,0.763860766458277,1.),(1.,0.763702734210281,
1.),(1.,0.764048836280064,1.),(1.,0.764566623657068,1.),(1.,0.764724834305744,
1.),(1.,0.764625210011228,1.),(1.,0.764542331423941,1.),(1.,0.764326337118295,
1.),(1.,0.764193221628244,1.),(1.,0.763882510299014,1.),(1.,0.763955361792152,
1.),(1.,0.764416713168217,1.),(1.,0.764665129414208,1.),(1.,0.764686940352922,
1.),(1.,0.764460460724398,1.),(1.,0.76392208068725,1.),(1.,0.763672740817721,
1.),(1.,0.763911324525423,1.),(1.,0.764051931517915,1.),(1.,0.764323031146854,
1.),(1.,0.764453731360604,1.),(1.,0.764720907693508,1.),(1.,0.764706351034155,
1.),(1.,0.764343019630522,1.),(1.,0.763994121210039,1.),(1.,0.763887698205184,
1.),(1.,0.764212830355328,1.),(1.,0.764537011123856,1.),(1.,0.764622045143321,
1.),(1.,0.764692681407165,1.),(1.,0.764677599503643,1.),(1.,0.764487344119654,
1.),(1.,0.764144753839761,1.),(1.,0.763702587630224,1.),(1.,0.763799887222974,
1.),(1.,0.764330273475046,1.),(1.,0.764614508454279,1.),(1.,0.76471671542289,
1.),(1.,0.764535560686859,1.),(1.,0.764179665899326,1.),(1.,0.764053667616838,
1.),(1.,0.763916268430484,1.),(1.,0.763926969747539,1.),(1.,0.764161781488297,
1.),(1.,0.764488323704147,1.),(1.,0.764737663853121,1.),(1.,0.76465390164221,
1.),(1.,0.764189010841196,1.),(1.,0.763814890315767,1.),(1.,0.763751197251442,
1.),(1.,0.763833803031666,1.),(1.,0.764068070995748,1.),(1.,0.764218139786203,
1.),(1.,0.764598269472164,1.),(1.,0.764731993944393,1.),(1.,0.764561917625315,
1.),(1.,0.764257407337477,1.),(1.,0.763865858127282,1.),(1.,0.763986854740837,
1.),(1.,0.764456099242501,1.),(1.,0.764684057417691,1.),(1.,0.764672342131847,
1.),(1.,0.764615183579261,1.),(1.,0.764421331097182,1.),(1.,0.764285304332037,
1.),(1.,0.763880849253991,1.),(1.,0.763675921984343,1.),(1.,0.763946650092346,
1.),(1.,0.764089650304982,1.),(1.,0.764360438200807,1.),(1.,0.764486720466232,
1.),(1.,0.764730902773989,1.),(1.,0.76468994788372,1.),(1.,0.764400105207107,
1.),(1.,0.76427192956214,1.),(1.,0.764044803269244,1.),(1.,0.763945914264244,
1.),(1.,0.763914820230933,1.),(1.,0.764254555421925,1.),(1.,0.764667433474705,
1.),(1.,0.764739498660029,1.),(1.,0.76452342410793,1.),(1.,0.764404140660104,
1.),(1.,0.764139137351779,1.),(1.,0.763993333719004,1.),(1.,0.763687184023814,
1.),(1.,0.763834660278889,1.),(1.,0.764236201135504,1.),(1.,0.764378436194924,
1.),(1.,0.764588470001048,1.),(1.,0.764656185266166,1.),(1.,0.764703128203519,
1.),(1.,0.764500442535882,1.),(1.,0.764145398632785,1.),(1.,0.764024978752906,
1.),(1.,0.763910063563777,1.),(1.,0.763941793066124,1.),(1.,0.764205956929848,
1.),(1.,0.764523303545078,1.),(1.,0.764683865095869,1.),(1.,0.764691313612272,
1.),(1.,0.764604453303825,1.),(1.,0.764509476141111,1.),(1.,0.764143354152028,
1.),(1.,0.76377288563184,1.),(1.,0.763764830719989,1.),(1.,0.764133605247446,
1.),(1.,0.764502115195786,1.),(1.,0.76459889368469,1.),(1.,0.764689625425294,
1.),(1.,0.764684310949503,1.),(1.,0.764529245268432,1.),(1.,0.764214503367863,
1.),(1.,0.763945490960164,1.),(1.,0.763909269234188,1.),(1.,0.764018931218163,
1.),(1.,0.764138489117333,1.),(1.,0.764493972977306,1.),(1.,0.764700928871412,
1.),(1.,0.764659938305659,1.),(1.,0.764594156328028,1.),(1.,0.76438685338652,
1.),(1.,0.764245191949504,1.),(1.,0.763842015003482,1.),(1.,0.763684920017492,
1.),(1.,0.763985174574737,1.),(1.,0.764130310945844,1.),(1.,0.764395784805852,
1.),(1.,0.764516186506651,1.),(1.,0.7647374102588,1.),(1.,0.764670099972414,
1.),(1.,0.764261299224288,1.),(1.,0.763920339000742,1.),(1.,0.763939902291723,
1.),(1.,0.764037338315704,1.),(1.,0.764264861871258,1.),(1.,0.764394777042652,
1.),(1.,0.764691836447148,1.),(1.,0.76474026082274,1.),(1.,0.764502444879734,
1.),(1.,0.764377615086339,1.),(1.,0.764105911424375,1.),(1.,0.763960844285112,
1.),(1.,0.763677550033968,1.),(1.,0.763867750516721,1.),(1.,0.764275857523739,
1.),(1.,0.764415362774288,1.),(1.,0.764618984869432,1.),(1.,0.764682548102571,
1.),(1.,0.764714269609273,1.),(1.,0.764500783672347,1.),(1.,0.764050275516554,
1.),(1.,0.763947142258318,1.),(1.,0.764253243543243,1.),(1.,0.76447716836975,
1.),(1.,0.764542829763807,1.),(1.,0.764385405357976,1.),(1.,0.764045762298611,
1.),(1.,0.763921199778699,1.),(1.,0.763756105588418,1.),(1.,0.76372541036921,
1.),(1.,0.763900015681686,1.),(1.,0.764124851617388,1.),(1.,0.764121206660071,
1.),(1.,0.763885915644855,1.),(1.,0.763748500497105,1.),(1.,0.763869356955843,
1.),(1.,0.750994184797527,1.),(1.,0.739646079293118,1.),(1.,0.722895202390289,
1.)))
REPRESENTATION_ITEM('')
SURFACE()
);
#12689=(
BOUNDED_SURFACE()
B_SPLINE_SURFACE(3,2,((#37478,#37479,#37480),(#37481,#37482,#37483),(#37484,
#37485,#37486),(#37487,#37488,#37489),(#37490,#37491,#37492),(#37493,#37494,
#37495),(#37496,#37497,#37498),(#37499,#37500,#37501),(#37502,#37503,#37504),
(#37505,#37506,#37507),(#37508,#37509,#37510),(#37511,#37512,#37513),(#37514,
#37515,#37516),(#37517,#37518,#37519),(#37520,#37521,#37522),(#37523,#37524,
#37525),(#37526,#37527,#37528),(#37529,#37530,#37531),(#37532,#37533,#37534),
(#37535,#37536,#37537),(#37538,#37539,#37540),(#37541,#37542,#37543),(#37544,
#37545,#37546),(#37547,#37548,#37549),(#37550,#37551,#37552),(#37553,#37554,
#37555),(#37556,#37557,#37558),(#37559,#37560,#37561),(#37562,#37563,#37564),
(#37565,#37566,#37567),(#37568,#37569,#37570),(#37571,#37572,#37573),(#37574,
#37575,#37576),(#37577,#37578,#37579),(#37580,#37581,#37582),(#37583,#37584,
#37585),(#37586,#37587,#37588),(#37589,#37590,#37591),(#37592,#37593,#37594),
(#37595,#37596,#37597),(#37598,#37599,#37600),(#37601,#37602,#37603),(#37604,
#37605,#37606),(#37607,#37608,#37609),(#37610,#37611,#37612),(#37613,#37614,
#37615),(#37616,#37617,#37618),(#37619,#37620,#37621),(#37622,#37623,#37624),
(#37625,#37626,#37627),(#37628,#37629,#37630),(#37631,#37632,#37633),(#37634,
#37635,#37636),(#37637,#37638,#37639),(#37640,#37641,#37642),(#37643,#37644,
#37645),(#37646,#37647,#37648),(#37649,#37650,#37651),(#37652,#37653,#37654),
(#37655,#37656,#37657),(#37658,#37659,#37660),(#37661,#37662,#37663),(#37664,
#37665,#37666),(#37667,#37668,#37669),(#37670,#37671,#37672),(#37673,#37674,
#37675),(#37676,#37677,#37678),(#37679,#37680,#37681),(#37682,#37683,#37684),
(#37685,#37686,#37687),(#37688,#37689,#37690),(#37691,#37692,#37693),(#37694,
#37695,#37696),(#37697,#37698,#37699),(#37700,#37701,#37702),(#37703,#37704,
#37705),(#37706,#37707,#37708),(#37709,#37710,#37711),(#37712,#37713,#37714),
(#37715,#37716,#37717),(#37718,#37719,#37720),(#37721,#37722,#37723),(#37724,
#37725,#37726),(#37727,#37728,#37729),(#37730,#37731,#37732),(#37733,#37734,
#37735),(#37736,#37737,#37738),(#37739,#37740,#37741),(#37742,#37743,#37744),
(#37745,#37746,#37747),(#37748,#37749,#37750),(#37751,#37752,#37753),(#37754,
#37755,#37756),(#37757,#37758,#37759),(#37760,#37761,#37762),(#37763,#37764,
#37765),(#37766,#37767,#37768),(#37769,#37770,#37771),(#37772,#37773,#37774),
(#37775,#37776,#37777),(#37778,#37779,#37780),(#37781,#37782,#37783),(#37784,
#37785,#37786),(#37787,#37788,#37789),(#37790,#37791,#37792),(#37793,#37794,
#37795),(#37796,#37797,#37798),(#37799,#37800,#37801),(#37802,#37803,#37804),
(#37805,#37806,#37807),(#37808,#37809,#37810),(#37811,#37812,#37813),(#37814,
#37815,#37816),(#37817,#37818,#37819),(#37820,#37821,#37822),(#37823,#37824,
#37825),(#37826,#37827,#37828),(#37829,#37830,#37831),(#37832,#37833,#37834),
(#37835,#37836,#37837),(#37838,#37839,#37840),(#37841,#37842,#37843),(#37844,
#37845,#37846),(#37847,#37848,#37849),(#37850,#37851,#37852),(#37853,#37854,
#37855),(#37856,#37857,#37858),(#37859,#37860,#37861),(#37862,#37863,#37864),
(#37865,#37866,#37867),(#37868,#37869,#37870),(#37871,#37872,#37873),(#37874,
#37875,#37876),(#37877,#37878,#37879),(#37880,#37881,#37882),(#37883,#37884,
#37885),(#37886,#37887,#37888),(#37889,#37890,#37891),(#37892,#37893,#37894),
(#37895,#37896,#37897),(#37898,#37899,#37900),(#37901,#37902,#37903),(#37904,
#37905,#37906),(#37907,#37908,#37909),(#37910,#37911,#37912),(#37913,#37914,
#37915),(#37916,#37917,#37918),(#37919,#37920,#37921),(#37922,#37923,#37924),
(#37925,#37926,#37927),(#37928,#37929,#37930),(#37931,#37932,#37933),(#37934,
#37935,#37936),(#37937,#37938,#37939),(#37940,#37941,#37942),(#37943,#37944,
#37945),(#37946,#37947,#37948),(#37949,#37950,#37951),(#37952,#37953,#37954),
(#37955,#37956,#37957),(#37958,#37959,#37960),(#37961,#37962,#37963),(#37964,
#37965,#37966),(#37967,#37968,#37969),(#37970,#37971,#37972),(#37973,#37974,
#37975),(#37976,#37977,#37978),(#37979,#37980,#37981),(#37982,#37983,#37984),
(#37985,#37986,#37987),(#37988,#37989,#37990),(#37991,#37992,#37993),(#37994,
#37995,#37996),(#37997,#37998,#37999),(#38000,#38001,#38002),(#38003,#38004,
#38005),(#38006,#38007,#38008),(#38009,#38010,#38011),(#38012,#38013,#38014),
(#38015,#38016,#38017),(#38018,#38019,#38020),(#38021,#38022,#38023),(#38024,
#38025,#38026),(#38027,#38028,#38029),(#38030,#38031,#38032),(#38033,#38034,
#38035),(#38036,#38037,#38038),(#38039,#38040,#38041),(#38042,#38043,#38044),
(#38045,#38046,#38047),(#38048,#38049,#38050),(#38051,#38052,#38053),(#38054,
#38055,#38056),(#38057,#38058,#38059),(#38060,#38061,#38062),(#38063,#38064,
#38065),(#38066,#38067,#38068),(#38069,#38070,#38071),(#38072,#38073,#38074),
(#38075,#38076,#38077),(#38078,#38079,#38080),(#38081,#38082,#38083),(#38084,
#38085,#38086),(#38087,#38088,#38089),(#38090,#38091,#38092),(#38093,#38094,
#38095),(#38096,#38097,#38098),(#38099,#38100,#38101),(#38102,#38103,#38104),
(#38105,#38106,#38107),(#38108,#38109,#38110),(#38111,#38112,#38113),(#38114,
#38115,#38116),(#38117,#38118,#38119),(#38120,#38121,#38122),(#38123,#38124,
#38125),(#38126,#38127,#38128),(#38129,#38130,#38131),(#38132,#38133,#38134),
(#38135,#38136,#38137),(#38138,#38139,#38140),(#38141,#38142,#38143),(#38144,
#38145,#38146),(#38147,#38148,#38149),(#38150,#38151,#38152),(#38153,#38154,
#38155),(#38156,#38157,#38158),(#38159,#38160,#38161),(#38162,#38163,#38164),
(#38165,#38166,#38167),(#38168,#38169,#38170),(#38171,#38172,#38173),(#38174,
#38175,#38176),(#38177,#38178,#38179),(#38180,#38181,#38182),(#38183,#38184,
#38185),(#38186,#38187,#38188),(#38189,#38190,#38191),(#38192,#38193,#38194),
(#38195,#38196,#38197),(#38198,#38199,#38200),(#38201,#38202,#38203),(#38204,
#38205,#38206),(#38207,#38208,#38209),(#38210,#38211,#38212),(#38213,#38214,
#38215),(#38216,#38217,#38218),(#38219,#38220,#38221),(#38222,#38223,#38224),
(#38225,#38226,#38227),(#38228,#38229,#38230),(#38231,#38232,#38233),(#38234,
#38235,#38236),(#38237,#38238,#38239),(#38240,#38241,#38242),(#38243,#38244,
#38245),(#38246,#38247,#38248),(#38249,#38250,#38251),(#38252,#38253,#38254),
(#38255,#38256,#38257),(#38258,#38259,#38260),(#38261,#38262,#38263),(#38264,
#38265,#38266),(#38267,#38268,#38269),(#38270,#38271,#38272),(#38273,#38274,
#38275),(#38276,#38277,#38278),(#38279,#38280,#38281),(#38282,#38283,#38284),
(#38285,#38286,#38287),(#38288,#38289,#38290),(#38291,#38292,#38293),(#38294,
#38295,#38296),(#38297,#38298,#38299),(#38300,#38301,#38302),(#38303,#38304,
#38305),(#38306,#38307,#38308),(#38309,#38310,#38311),(#38312,#38313,#38314),
(#38315,#38316,#38317),(#38318,#38319,#38320),(#38321,#38322,#38323),(#38324,
#38325,#38326),(#38327,#38328,#38329),(#38330,#38331,#38332),(#38333,#38334,
#38335),(#38336,#38337,#38338),(#38339,#38340,#38341),(#38342,#38343,#38344),
(#38345,#38346,#38347),(#38348,#38349,#38350),(#38351,#38352,#38353),(#38354,
#38355,#38356),(#38357,#38358,#38359),(#38360,#38361,#38362),(#38363,#38364,
#38365),(#38366,#38367,#38368),(#38369,#38370,#38371),(#38372,#38373,#38374),
(#38375,#38376,#38377),(#38378,#38379,#38380),(#38381,#38382,#38383),(#38384,
#38385,#38386),(#38387,#38388,#38389),(#38390,#38391,#38392),(#38393,#38394,
#38395),(#38396,#38397,#38398),(#38399,#38400,#38401),(#38402,#38403,#38404),
(#38405,#38406,#38407),(#38408,#38409,#38410),(#38411,#38412,#38413),(#38414,
#38415,#38416),(#38417,#38418,#38419),(#38420,#38421,#38422),(#38423,#38424,
#38425),(#38426,#38427,#38428),(#38429,#38430,#38431),(#38432,#38433,#38434),
(#38435,#38436,#38437),(#38438,#38439,#38440),(#38441,#38442,#38443),(#38444,
#38445,#38446),(#38447,#38448,#38449),(#38450,#38451,#38452),(#38453,#38454,
#38455),(#38456,#38457,#38458),(#38459,#38460,#38461),(#38462,#38463,#38464),
(#38465,#38466,#38467),(#38468,#38469,#38470),(#38471,#38472,#38473),(#38474,
#38475,#38476),(#38477,#38478,#38479),(#38480,#38481,#38482),(#38483,#38484,
#38485),(#38486,#38487,#38488),(#38489,#38490,#38491),(#38492,#38493,#38494),
(#38495,#38496,#38497),(#38498,#38499,#38500),(#38501,#38502,#38503),(#38504,
#38505,#38506),(#38507,#38508,#38509),(#38510,#38511,#38512),(#38513,#38514,
#38515)),.UNSPECIFIED.,.F.,.F.,.F.)
B_SPLINE_SURFACE_WITH_KNOTS((4,2,2,2,2,2,2,2,2,2,2,2,2,2,2,2,2,2,2,2,2,
2,2,2,2,2,2,2,2,2,2,2,2,2,2,2,2,2,2,2,2,2,2,2,2,2,2,2,2,2,2,2,2,2,2,2,2,
2,2,2,2,2,2,2,2,2,2,2,2,2,2,2,2,2,2,2,2,2,2,2,2,2,2,2,2,2,2,2,2,2,2,2,2,
2,2,2,2,2,2,2,2,2,2,2,2,2,2,2,2,2,2,2,2,2,2,2,2,2,2,2,2,2,2,2,2,2,2,2,2,
2,2,2,2,2,2,2,2,2,2,2,2,2,2,2,2,2,2,2,2,2,2,2,2,2,2,2,2,2,2,2,2,2,2,2,2,
2,2,2,2,2,2,2,4),(3,3),(0.193194020715734,0.19458015398761,0.195966287259486,
0.19735242053136,0.198738553803236,0.201510820346987,0.204283086890738,
0.207055353434488,0.208441486706364,0.209827619978239,0.212599886521989,
0.21537215306574,0.216758286337615,0.218144419609491,0.220916686153242,
0.222302819425117,0.223688952696992,0.226461219240743,0.227847352512619,
0.229233485784493,0.232005752328244,0.234778018871995,0.23616415214387,
0.237550285415745,0.240322551959497,0.241708685231372,0.243094818503247,
0.245867085046998,0.247253218318873,0.248639351590749,0.251411618134499,
0.25418388467825,0.255570017950125,0.256956151222,0.259728417765751,0.261114551037626,
0.262500684309502,0.265272950853253,0.266659084125128,0.268045217397003,
0.270817483940754,0.273589750484505,0.276362017028256,0.279134283572006,
0.280520416843882,0.281906550115756,0.284678816659508,0.286064949931383,
0.287451083203258,0.290223349747009,0.29299561629076,0.29576788283451,0.29854014937826,
0.299926282650136,0.301312415922012,0.304084682465762,0.305470815737638,
0.306856949009513,0.309629215553264,0.312401482097014,0.315173748640765,
0.317946015184516,0.319332148456391,0.320718281728266,0.323490548272017,
0.324876681543892,0.326262814815768,0.329035081359519,0.331807347903269,
0.33457961444702,0.337351880990771,0.338738014262645,0.340124147534521,
0.342896414078271,0.344282547350147,0.345668680622022,0.348440947165773,
0.349827080437648,0.351213213709524,0.353985480253275,0.356757746797025,
0.358143880068901,0.359530013340776,0.362302279884527,0.363688413156402,
0.365074546428277,0.367846812972028,0.369232946243904,0.370619079515778,
0.37339134605953,0.37616361260328,0.37893587914703,0.380322012418906,0.381708145690781,
0.384480412234532,0.387252678778283,0.390024945322034,0.391411078593909,
0.392797211865784,0.395569478409534,0.398341744953286,0.399727878225161,
0.401114011497036,0.403886278040787,0.406658544584537,0.409430811128288,
0.410816944400164,0.412203077672039,0.41497534421579,0.41774761075954,0.419133744031415,
0.420519877303291,0.423292143847042,0.426064410390793,0.428836676934543,
0.430222810206419,0.431608943478294,0.434381210022044,0.437153476565795,
0.43853960983767,0.439925743109545,0.442698009653296,0.444084142925172,
0.445470276197047,0.448242542740798,0.449628676012673,0.451014809284549,
0.453787075828299,0.45655934237205,0.457945475643925,0.459331608915801,
0.462103875459551,0.463490008731427,0.464876142003302,0.467648408547053,
0.469034541818928,0.470420675090803,0.473192941634554,0.475965208178305,
0.47735134145018,0.478737474722055,0.481509741265806,0.482895874537681,
0.484282007809557,0.487054274353307,0.488440407625183,0.489826540897058,
0.492598807440809,0.495371073984559,0.49814334052831,0.500915607072061,
0.502301740343936,0.503687873615812,0.506460140159562,0.507846273431438,
0.509232406703313,0.512004673247064,0.514776939790814,0.517549206334565,
0.520321472878316,0.521707606150191,0.523093739422066,0.525866005965817,
0.527252139237692,0.528638272509568,0.531410539053318,0.534182805597069,
0.53695507214082,0.53972733868457,0.541113471956446,0.542499605228321,0.545271871772072,
0.548044138315822),(0.,1.),.UNSPECIFIED.)
GEOMETRIC_REPRESENTATION_ITEM()
RATIONAL_B_SPLINE_SURFACE(((1.,0.724284384183872,1.),(1.,0.740305127237413,
1.),(1.,0.751232954189051,1.),(1.,0.763742821539273,1.),(1.,0.763748825819259,
1.),(1.,0.763834413771316,1.),(1.,0.763924465861183,1.),(1.,0.764064751530991,
1.),(1.,0.764115143190699,1.),(1.,0.764135968375271,1.),(1.,0.76393847009999,
1.),(1.,0.763675888999986,1.),(1.,0.763876016878027,1.),(1.,0.764321026152726,
1.),(1.,0.764509104980298,1.),(1.,0.76451608219454,1.),(1.,0.76447775031199,
1.),(1.,0.764346212201205,1.),(1.,0.764252566231277,1.),(1.,0.764000135558632,
1.),(1.,0.763965766551896,1.),(1.,0.764364555014901,1.),(1.,0.764630270967712,
1.),(1.,0.764711027046936,1.),(1.,0.764689932612344,1.),(1.,0.764558244124265,
1.),(1.,0.764447962391867,1.),(1.,0.764066111419482,1.),(1.,0.763726565682464,
1.),(1.,0.763796776005459,1.),(1.,0.763904914089681,1.),(1.,0.764157901026904,
1.),(1.,0.764300924283023,1.),(1.,0.764645734647822,1.),(1.,0.764739970352618,
1.),(1.,0.764582273953922,1.),(1.,0.764485721950045,1.),(1.,0.764260579879712,
1.),(1.,0.764131679720444,1.),(1.,0.763860735254699,1.),(1.,0.763994368914939,
1.),(1.,0.764451904711763,1.),(1.,0.764675420085065,1.),(1.,0.764676435702143,
1.),(1.,0.764626319914614,1.),(1.,0.764448678783329,1.),(1.,0.764321322928903,
1.),(1.,0.763928094157012,1.),(1.,0.763678648076241,1.),(1.,0.763890075019292,
1.),(1.,0.764021879641345,1.),(1.,0.764286917309977,1.),(1.,0.764418752057724,
1.),(1.,0.764702707473528,1.),(1.,0.764720013103519,1.),(1.,0.764487759524574,
1.),(1.,0.764373147804989,1.),(1.,0.764141505001544,1.),(1.,0.764024512063168,
1.),(1.,0.763855645361392,1.),(1.,0.764113660855987,1.),(1.,0.764565836609295,
1.),(1.,0.764724131926724,1.),(1.,0.764629033790115,1.),(1.,0.764547656618952,
1.),(1.,0.764326190273316,1.),(1.,0.764186143918983,1.),(1.,0.763805229077168,
1.),(1.,0.763699618536614,1.),(1.,0.764013359048112,1.),(1.,0.764157064792652,
1.),(1.,0.764414467893511,1.),(1.,0.764527285422471,1.),(1.,0.764733735803131,
1.),(1.,0.764672147726954,1.),(1.,0.764378491171655,1.),(1.,0.764252882168725,
1.),(1.,0.764034494546627,1.),(1.,0.763942201634753,1.),(1.,0.763920903382263,
1.),(1.,0.764244527340539,1.),(1.,0.764653633517867,1.),(1.,0.764738192767595,
1.),(1.,0.76448908915439,1.),(1.,0.764159736215753,1.),(1.,0.763716715490157,
1.),(1.,0.76377587103168,1.),(1.,0.764149322081957,1.),(1.,0.764292891647004,
1.),(1.,0.764524133102802,1.),(1.,0.764611439973631,1.),(1.,0.764729271281352,
1.),(1.,0.764592564976275,1.),(1.,0.764259450599018,1.),(1.,0.764132866751854,
1.),(1.,0.763952940534743,1.),(1.,0.763909940937905,1.),(1.,0.764047564751732,
1.),(1.,0.764376050918383,1.),(1.,0.764710874387109,1.),(1.,0.764716717096199,
1.),(1.,0.764358367100507,1.),(1.,0.764002110091814,1.),(1.,0.763678666741915,
1.),(1.,0.763890791093845,1.),(1.,0.764286151554894,1.),(1.,0.76441927129705,
1.),(1.,0.764609474764907,1.),(1.,0.764666635980878,1.),(1.,0.764690318511911,
1.),(1.,0.76448601338486,1.),(1.,0.764140706416799,1.),(1.,0.764024893163625,
1.),(1.,0.763911882511275,1.),(1.,0.763938692841781,1.),(1.,0.764187733769396,
1.),(1.,0.764497658159542,1.),(1.,0.764734199223594,1.),(1.,0.764660097132399,
1.),(1.,0.76421324129478,1.),(1.,0.763851792592164,1.),(1.,0.763708665296719,
1.),(1.,0.764029246906871,1.),(1.,0.764413677710061,1.),(1.,0.76452781916181,
1.),(1.,0.7646658134995,1.),(1.,0.764690072542689,1.),(1.,0.764619697565954,
1.),(1.,0.764359052346609,1.),(1.,0.764034028102741,1.),(1.,0.763942399287252,
1.),(1.,0.763927844141164,1.),(1.,0.764011858926398,1.),(1.,0.764328562594867,
1.),(1.,0.764600555208422,1.),(1.,0.764722148145367,1.),(1.,0.764570469279582,
1.),(1.,0.764063816259676,1.),(1.,0.763726910127108,1.),(1.,0.763819983432828,
1.),(1.,0.76417767845136,1.),(1.,0.764523503616313,1.),(1.,0.76461198390526,
1.),(1.,0.764690348954903,1.),(1.,0.764680836895054,1.),(1.,0.76452210843659,
1.),(1.,0.764220072361436,1.),(1.,0.763952836450435,1.),(1.,0.763909765698979,
1.),(1.,0.764001660074815,1.),(1.,0.764114021416086,1.),(1.,0.764459450111386,
1.),(1.,0.764677768912382,1.),(1.,0.764675817192644,1.),(1.,0.764626188605873,
1.),(1.,0.764448334836733,1.),(1.,0.764319649606282,1.),(1.,0.76392144937362,
1.),(1.,0.763678954739498,1.),(1.,0.763966705816651,1.),(1.,0.764324181625799,
1.),(1.,0.764609052799967,1.),(1.,0.764667080350501,1.),(1.,0.764682173323424,
1.),(1.,0.764639909041378,1.),(1.,0.764404109006945,1.),(1.,0.764079253557161,
1.),(1.,0.76391211996651,1.),(1.,0.763938204725637,1.),(1.,0.764104954676349,
1.),(1.,0.764231320468568,1.),(1.,0.764571581565062,1.),(1.,0.764724181309951,
1.),(1.,0.764627747558348,1.),(1.,0.764547299804896,1.),(1.,0.764325646198393,
1.),(1.,0.764183899644622,1.),(1.,0.763799361853443,1.),(1.,0.763703181785222,
1.),(1.,0.764123550653324,1.),(1.,0.764458577730754,1.),(1.,0.764734613928835,
1.),(1.,0.764669103511761,1.),(1.,0.764367907046241,1.),(1.,0.764240302577737,
1.),(1.,0.76402494244893,1.),(1.,0.763937135559565,1.),(1.,0.763929882961757,
1.),(1.,0.764253286273473,1.),(1.,0.764659669769347,1.),(1.,0.764736610859316,
1.),(1.,0.764478373141418,1.),(1.,0.764149224099175,1.),(1.,0.763821487056611,
1.),(1.,0.763748372230787,1.),(1.,0.763801098390883,1.),(1.,0.763911183371908,
1.),(1.,0.764290057432388,1.),(1.,0.764579381227941,1.),(1.,0.764727426427296,
1.),(1.,0.764586296776282,1.),(1.,0.764248306196083,1.),(1.,0.764120922979176,
1.),(1.,0.763946879813119,1.),(1.,0.763910536288566,1.),(1.,0.764057706241362,
1.),(1.,0.76438462516118,1.),(1.,0.76471447438699,1.),(1.,0.764711120531398,
1.),(1.,0.764346703878295,1.),(1.,0.76399170176065,1.),(1.,0.763756582327334,
1.),(1.,0.763752110504806,1.),(1.,0.763901328422942,1.),(1.,0.764035450100222,
1.),(1.,0.76443236193701,1.),(1.,0.764663646141859,1.),(1.,0.764686363906065,
1.),(1.,0.764477694984837,1.),(1.,0.764129890053359,1.),(1.,0.764014977127996,
1.),(1.,0.763910804517628,1.),(1.,0.763943547724003,1.),(1.,0.764197787087454,
1.),(1.,0.764505416587815,1.),(1.,0.764735065981735,1.),(1.,0.764650795813227,
1.),(1.,0.764201499620299,1.),(1.,0.763842254050267,1.),(1.,0.763745729500901,
1.),(1.,0.76381182195424,1.),(1.,0.76402644812972,1.),(1.,0.764171057297587,
1.),(1.,0.764553541563368,1.),(1.,0.764715935999787,1.),(1.,0.764613884843303,
1.),(1.,0.764349088181113,1.),(1.,0.764024757422653,1.),(1.,0.763936087572711,
1.),(1.,0.763933281394626,1.),(1.,0.764019522637573,1.),(1.,0.764337859143539,
1.),(1.,0.764606969286635,1.),(1.,0.764691835149024,1.),(1.,0.764672390149729,
1.),(1.,0.764541959203006,1.),(1.,0.764431856676212,1.),(1.,0.764052655452415,
1.),(1.,0.763720892206212,1.),(1.,0.763802318721878,1.),(1.,0.763911148353123,
1.),(1.,0.764163074576283,1.),(1.,0.76430628255999,1.),(1.,0.764647184874934,
1.),(1.,0.764733604516214,1.),(1.,0.7645148011791,1.),(1.,0.764209006825961,
1.),(1.,0.763946554515086,1.),(1.,0.763910418541632,1.),(1.,0.764010587040542,
1.),(1.,0.764123233796092,1.),(1.,0.764467443928139,1.),(1.,0.764682413968858,
1.),(1.,0.76467328554026,1.),(1.,0.764620305145998,1.),(1.,0.764436387977514,
1.),(1.,0.764306466960175,1.),(1.,0.763911800910976,1.),(1.,0.763678258157877,
1.),(1.,0.763902697590758,1.),(1.,0.764035192882901,1.),(1.,0.764299476715184,
1.),(1.,0.764431141631408,1.),(1.,0.764708752226097,1.),(1.,0.764715902370825,
1.),(1.,0.764395783925963,1.),(1.,0.764067776783428,1.),(1.,0.763910501816556,
1.),(1.,0.763944254604468,1.),(1.,0.764115592875844,1.),(1.,0.764241007152287,
1.),(1.,0.764577846837585,1.),(1.,0.764726738859265,1.),(1.,0.764622633857058,
1.),(1.,0.764538607993317,1.),(1.,0.764312012546189,1.),(1.,0.764170421879028,
1.),(1.,0.763792232864636,1.),(1.,0.76370659012842,1.),(1.,0.764027763125852,
1.),(1.,0.764170621154752,1.),(1.,0.764425646706682,1.),(1.,0.764537442869453,
1.),(1.,0.764735596081267,1.),(1.,0.764663981931681,1.),(1.,0.764265331217681,
1.),(1.,0.763937466031569,1.),(1.,0.763931901903142,1.),(1.,0.764260343346382,
1.),(1.,0.764662203747841,1.),(1.,0.764736820790307,1.),(1.,0.764542417955957,
1.),(1.,0.764431774438024,1.),(1.,0.764176976560631,1.),(1.,0.764033631618057,
1.),(1.,0.763708839179177,1.),(1.,0.76378808686829,1.),(1.,0.764164189211495,
1.),(1.,0.764305748334095,1.),(1.,0.764533380352393,1.),(1.,0.764618865966987,
1.),(1.,0.764727061043886,1.),(1.,0.76458103112283,1.),(1.,0.764133984783778,
1.),(1.,0.763859901665259,1.),(1.,0.76406202396653,1.),(1.,0.764391062212757,
1.),(1.,0.76471420648425,1.),(1.,0.764709508679019,1.),(1.,0.764434815138151,
1.),(1.,0.764303896710659,1.),(1.,0.764039283569035,1.),(1.,0.763906140471446,
1.),(1.,0.763678071029506,1.),(1.,0.763907797434181,1.),(1.,0.764300330435456,
1.),(1.,0.764429809231862,1.),(1.,0.764613336272094,1.),(1.,0.764666656725297,
1.),(1.,0.764675678313187,1.),(1.,0.764459912120916,1.),(1.,0.763994763845434,
1.),(1.,0.763828888332753,1.),(1.,0.764197718857373,1.),(1.,0.764534267618665,
1.),(1.,0.764803818543527,1.),(1.,0.764737840759975,1.),(1.,0.764395415450403,
1.),(1.,0.764246141205225,1.),(1.,0.76396864128702,1.),(1.,0.763840712706475,
1.),(1.,0.763683379268838,1.),(1.,0.763772086503981,1.),(1.,0.763779013551137,
1.),(1.,0.763732611162939,1.),(1.,0.763723138090074,1.)))
REPRESENTATION_ITEM('')
SURFACE()
);
#12690=(
BOUNDED_SURFACE()
B_SPLINE_SURFACE(3,2,((#38707,#38708,#38709),(#38710,#38711,#38712),(#38713,
#38714,#38715),(#38716,#38717,#38718)),.UNSPECIFIED.,.F.,.F.,.F.)
B_SPLINE_SURFACE_WITH_KNOTS((4,4),(3,3),(0.00258460052115835,0.00277094492006339),
(0.188652408414785,1.),.PIECEWISE_BEZIER_KNOTS.)
GEOMETRIC_REPRESENTATION_ITEM()
RATIONAL_B_SPLINE_SURFACE(((0.911321524900829,0.764968611203214,1.),(0.911099518239721,
0.764380209859776,1.),(0.910872217507487,0.763777777232107,1.),(0.910640530053848,
0.763163718139024,1.)))
REPRESENTATION_ITEM('')
SURFACE()
);
#12691=(
BOUNDED_SURFACE()
B_SPLINE_SURFACE(3,2,((#38730,#38731,#38732),(#38733,#38734,#38735),(#38736,
#38737,#38738),(#38739,#38740,#38741),(#38742,#38743,#38744),(#38745,#38746,
#38747),(#38748,#38749,#38750),(#38751,#38752,#38753),(#38754,#38755,#38756),
(#38757,#38758,#38759)),.UNSPECIFIED.,.F.,.F.,.F.)
B_SPLINE_SURFACE_WITH_KNOTS((4,2,2,2,4),(3,3),(0.0442495418135926,0.0460556664569336,
0.0478617911002747,0.0496679157436157,0.0514740403869568),(0.,1.),
 .UNSPECIFIED.)
GEOMETRIC_REPRESENTATION_ITEM()
RATIONAL_B_SPLINE_SURFACE(((1.,0.763723138090958,1.),(1.,0.757306565135894,
1.),(1.,0.751046655980244,1.),(1.,0.738750551500846,1.),(1.,0.732694138219894,
1.),(1.,0.720501130718487,1.),(1.,0.714363531034312,1.),(1.,0.702102216800646,
1.),(1.,0.696457132575243,1.),(1.,0.689508268890299,1.)))
REPRESENTATION_ITEM('')
SURFACE()
);
#12692=(
BOUNDED_SURFACE()
B_SPLINE_SURFACE(3,3,((#38826,#38827,#38828,#38829,#38830,#38831,#38832,
#38833,#38834,#38835,#38836,#38837,#38838,#38839,#38840,#38841,#38842,#38843,
#38844,#38845,#38846,#38847,#38848,#38849,#38850,#38851,#38852,#38853,#38854,
#38855,#38856,#38857,#38858,#38859,#38860,#38861,#38862,#38863,#38864,#38865,
#38866,#38867,#38868,#38869,#38870,#38871,#38872,#38873,#38874,#38875,#38876,
#38877,#38878,#38879,#38880,#38881,#38882,#38883,#38884,#38885,#38886,#38887,
#38888,#38889,#38890,#38891,#38892,#38893,#38894,#38895,#38896,#38897,#38898,
#38899,#38900,#38901,#38902,#38903,#38904,#38905,#38906,#38907,#38908,#38909,
#38910,#38911),(#38912,#38913,#38914,#38915,#38916,#38917,#38918,#38919,
#38920,#38921,#38922,#38923,#38924,#38925,#38926,#38927,#38928,#38929,#38930,
#38931,#38932,#38933,#38934,#38935,#38936,#38937,#38938,#38939,#38940,#38941,
#38942,#38943,#38944,#38945,#38946,#38947,#38948,#38949,#38950,#38951,#38952,
#38953,#38954,#38955,#38956,#38957,#38958,#38959,#38960,#38961,#38962,#38963,
#38964,#38965,#38966,#38967,#38968,#38969,#38970,#38971,#38972,#38973,#38974,
#38975,#38976,#38977,#38978,#38979,#38980,#38981,#38982,#38983,#38984,#38985,
#38986,#38987,#38988,#38989,#38990,#38991,#38992,#38993,#38994,#38995,#38996,
#38997),(#38998,#38999,#39000,#39001,#39002,#39003,#39004,#39005,#39006,
#39007,#39008,#39009,#39010,#39011,#39012,#39013,#39014,#39015,#39016,#39017,
#39018,#39019,#39020,#39021,#39022,#39023,#39024,#39025,#39026,#39027,#39028,
#39029,#39030,#39031,#39032,#39033,#39034,#39035,#39036,#39037,#39038,#39039,
#39040,#39041,#39042,#39043,#39044,#39045,#39046,#39047,#39048,#39049,#39050,
#39051,#39052,#39053,#39054,#39055,#39056,#39057,#39058,#39059,#39060,#39061,
#39062,#39063,#39064,#39065,#39066,#39067,#39068,#39069,#39070,#39071,#39072,
#39073,#39074,#39075,#39076,#39077,#39078,#39079,#39080,#39081,#39082,#39083),
(#39084,#39085,#39086,#39087,#39088,#39089,#39090,#39091,#39092,#39093,
#39094,#39095,#39096,#39097,#39098,#39099,#39100,#39101,#39102,#39103,#39104,
#39105,#39106,#39107,#39108,#39109,#39110,#39111,#39112,#39113,#39114,#39115,
#39116,#39117,#39118,#39119,#39120,#39121,#39122,#39123,#39124,#39125,#39126,
#39127,#39128,#39129,#39130,#39131,#39132,#39133,#39134,#39135,#39136,#39137,
#39138,#39139,#39140,#39141,#39142,#39143,#39144,#39145,#39146,#39147,#39148,
#39149,#39150,#39151,#39152,#39153,#39154,#39155,#39156,#39157,#39158,#39159,
#39160,#39161,#39162,#39163,#39164,#39165,#39166,#39167,#39168,#39169),
(#39170,#39171,#39172,#39173,#39174,#39175,#39176,#39177,#39178,#39179,
#39180,#39181,#39182,#39183,#39184,#39185,#39186,#39187,#39188,#39189,#39190,
#39191,#39192,#39193,#39194,#39195,#39196,#39197,#39198,#39199,#39200,#39201,
#39202,#39203,#39204,#39205,#39206,#39207,#39208,#39209,#39210,#39211,#39212,
#39213,#39214,#39215,#39216,#39217,#39218,#39219,#39220,#39221,#39222,#39223,
#39224,#39225,#39226,#39227,#39228,#39229,#39230,#39231,#39232,#39233,#39234,
#39235,#39236,#39237,#39238,#39239,#39240,#39241,#39242,#39243,#39244,#39245,
#39246,#39247,#39248,#39249,#39250,#39251,#39252,#39253,#39254,#39255),
(#39256,#39257,#39258,#39259,#39260,#39261,#39262,#39263,#39264,#39265,
#39266,#39267,#39268,#39269,#39270,#39271,#39272,#39273,#39274,#39275,#39276,
#39277,#39278,#39279,#39280,#39281,#39282,#39283,#39284,#39285,#39286,#39287,
#39288,#39289,#39290,#39291,#39292,#39293,#39294,#39295,#39296,#39297,#39298,
#39299,#39300,#39301,#39302,#39303,#39304,#39305,#39306,#39307,#39308,#39309,
#39310,#39311,#39312,#39313,#39314,#39315,#39316,#39317,#39318,#39319,#39320,
#39321,#39322,#39323,#39324,#39325,#39326,#39327,#39328,#39329,#39330,#39331,
#39332,#39333,#39334,#39335,#39336,#39337,#39338,#39339,#39340,#39341),
(#39342,#39343,#39344,#39345,#39346,#39347,#39348,#39349,#39350,#39351,
#39352,#39353,#39354,#39355,#39356,#39357,#39358,#39359,#39360,#39361,#39362,
#39363,#39364,#39365,#39366,#39367,#39368,#39369,#39370,#39371,#39372,#39373,
#39374,#39375,#39376,#39377,#39378,#39379,#39380,#39381,#39382,#39383,#39384,
#39385,#39386,#39387,#39388,#39389,#39390,#39391,#39392,#39393,#39394,#39395,
#39396,#39397,#39398,#39399,#39400,#39401,#39402,#39403,#39404,#39405,#39406,
#39407,#39408,#39409,#39410,#39411,#39412,#39413,#39414,#39415,#39416,#39417,
#39418,#39419,#39420,#39421,#39422,#39423,#39424,#39425,#39426,#39427)),
 .UNSPECIFIED.,.F.,.F.,.F.)
B_SPLINE_SURFACE_WITH_KNOTS((4,3,4),(4,3,2,2,2,2,2,2,2,2,2,2,2,2,2,2,2,
2,2,2,2,2,2,2,2,2,2,2,2,2,2,2,2,2,2,2,2,2,2,2,3,4),(0.768207327186719,1.,
1.23184820212984),(-0.00600749857863525,0.,0.0175438596491217,0.0438596491228064,
0.0701754385964912,0.0964912280701754,0.12280701754386,0.149122807017537,
0.175438596491214,0.201754385964905,0.228070175438597,0.25438596491228,
0.280701754385965,0.307017543859649,0.333333333333333,0.359649122807017,
0.385964912280702,0.412280701754386,0.43859649122807,0.464912280701754,
0.491228070175438,0.517543859649124,0.54385964912281,0.570175438596493,
0.596491228070175,0.62280701754386,0.649122807017544,0.675438596491228,
0.701754385964912,0.728070175438596,0.754385964912281,0.780701754385965,
0.807017543859649,0.833333333333333,0.859649122807018,0.885964912280702,
0.912280701754386,0.93859649122807,0.964912280701754,0.982456140350877,
1.,1.00600726704965),.UNSPECIFIED.)
GEOMETRIC_REPRESENTATION_ITEM()
RATIONAL_B_SPLINE_SURFACE(((0.502652054106274,0.502652054106274,0.502652054106274,
0.502652054106274,0.502652054106274,0.502652054106274,0.502652054106274,
0.502652054106274,0.502652054106274,0.502652054106274,0.502652054106274,
0.502652054106274,0.502652054106274,0.502652054106274,0.502652054106274,
0.502652054106274,0.502652054106274,0.502652054106274,0.502652054106274,
0.502652054106274,0.502652054106274,0.502652054106274,0.502652054106274,
0.502652054106274,0.502652054106274,0.502652054106274,0.502652054106274,
0.502652054106274,0.502652054106274,0.502652054106274,0.502652054106274,
0.502652054106274,0.502652054106274,0.502652054106274,0.502652054106274,
0.502652054106274,0.502652054106274,0.502652054106274,0.502652054106274,
0.502652054106274,0.502652054106274,0.502652054106274,0.502652054106274,
0.502652054106274,0.502652054106274,0.502652054106274,0.502652054106274,
0.502652054106274,0.502652054106274,0.502652054106274,0.502652054106274,
0.502652054106274,0.502652054106274,0.502652054106274,0.502652054106274,
0.502652054106274,0.502652054106274,0.502652054106274,0.502652054106274,
0.502652054106274,0.502652054106274,0.502652054106274,0.502652054106274,
0.502652054106274,0.502652054106274,0.502652054106274,0.502652054106274,
0.502652054106274,0.502652054106274,0.502652054106274,0.502652054106274,
0.502652054106274,0.502652054106274,0.502652054106274,0.502652054106274,
0.502652054106274,0.502652054106274,0.502652054106274,0.502652054106274,
0.502652054106274,0.502652054106274,0.502652054106274,0.502652054106274,
0.502652054106274,0.502652054106274,0.502652054106274),(0.525160454284383,
0.525160454284383,0.525160454284383,0.525160454284383,0.525160454284383,
0.525160454284383,0.525160454284383,0.525160454284383,0.525160454284383,
0.525160454284383,0.525160454284383,0.525160454284383,0.525160454284383,
0.525160454284383,0.525160454284383,0.525160454284383,0.525160454284383,
0.525160454284383,0.525160454284383,0.525160454284383,0.525160454284383,
0.525160454284383,0.525160454284383,0.525160454284383,0.525160454284383,
0.525160454284383,0.525160454284383,0.525160454284383,0.525160454284383,
0.525160454284383,0.525160454284383,0.525160454284383,0.525160454284383,
0.525160454284383,0.525160454284383,0.525160454284383,0.525160454284383,
0.525160454284383,0.525160454284383,0.525160454284383,0.525160454284383,
0.525160454284383,0.525160454284383,0.525160454284383,0.525160454284383,
0.525160454284383,0.525160454284383,0.525160454284383,0.525160454284383,
0.525160454284383,0.525160454284383,0.525160454284383,0.525160454284383,
0.525160454284383,0.525160454284383,0.525160454284383,0.525160454284383,
0.525160454284383,0.525160454284383,0.525160454284383,0.525160454284383,
0.525160454284383,0.525160454284383,0.525160454284383,0.525160454284383,
0.525160454284383,0.525160454284383,0.525160454284383,0.525160454284383,
0.525160454284383,0.525160454284383,0.525160454284383,0.525160454284383,
0.525160454284383,0.525160454284383,0.525160454284383,0.525160454284383,
0.525160454284383,0.525160454284383,0.525160454284383,0.525160454284383,
0.525160454284383,0.525160454284383,0.525160454284383,0.525160454284383,
0.525160454284383),(0.690943102915625,0.690943102915625,0.690943102915625,
0.690943102915625,0.690943102915625,0.690943102915625,0.690943102915625,
0.690943102915625,0.690943102915625,0.690943102915625,0.690943102915625,
0.690943102915625,0.690943102915625,0.690943102915625,0.690943102915625,
0.690943102915625,0.690943102915625,0.690943102915625,0.690943102915625,
0.690943102915625,0.690943102915625,0.690943102915625,0.690943102915625,
0.690943102915625,0.690943102915625,0.690943102915625,0.690943102915625,
0.690943102915625,0.690943102915625,0.690943102915625,0.690943102915625,
0.690943102915625,0.690943102915625,0.690943102915625,0.690943102915625,
0.690943102915625,0.690943102915625,0.690943102915625,0.690943102915625,
0.690943102915625,0.690943102915625,0.690943102915625,0.690943102915625,
0.690943102915625,0.690943102915625,0.690943102915625,0.690943102915625,
0.690943102915625,0.690943102915625,0.690943102915625,0.690943102915625,
0.690943102915625,0.690943102915625,0.690943102915625,0.690943102915625,
0.690943102915625,0.690943102915625,0.690943102915625,0.690943102915625,
0.690943102915625,0.690943102915625,0.690943102915625,0.690943102915625,
0.690943102915625,0.690943102915625,0.690943102915625,0.690943102915625,
0.690943102915625,0.690943102915625,0.690943102915625,0.690943102915625,
0.690943102915625,0.690943102915625,0.690943102915625,0.690943102915625,
0.690943102915625,0.690943102915625,0.690943102915625,0.690943102915625,
0.690943102915625,0.690943102915625,0.690943102915625,0.690943102915625,
0.690943102915625,0.690943102915625,0.690943102915625),(1.,1.,1.,1.,1.,
1.,1.,1.,1.,1.,1.,1.,1.,1.,1.,1.,1.,1.,1.,1.,1.,1.,1.,1.,1.,1.,1.,1.,1.,
1.,1.,1.,1.,1.,1.,1.,1.,1.,1.,1.,1.,1.,1.,1.,1.,1.,1.,1.,1.,1.,1.,1.,1.,
1.,1.,1.,1.,1.,1.,1.,1.,1.,1.,1.,1.,1.,1.,1.,1.,1.,1.,1.,1.,1.,1.,1.,1.,
1.,1.,1.,1.,1.,1.,1.,1.,1.),(0.690869063826886,0.690869063826886,0.690869063826886,
0.690869063826886,0.690869063826886,0.690869063826886,0.690869063826886,
0.690869063826886,0.690869063826886,0.690869063826886,0.690869063826886,
0.690869063826886,0.690869063826886,0.690869063826886,0.690869063826886,
0.690869063826886,0.690869063826886,0.690869063826886,0.690869063826886,
0.690869063826886,0.690869063826886,0.690869063826886,0.690869063826886,
0.690869063826886,0.690869063826886,0.690869063826886,0.690869063826886,
0.690869063826886,0.690869063826886,0.690869063826886,0.690869063826886,
0.690869063826886,0.690869063826886,0.690869063826886,0.690869063826886,
0.690869063826886,0.690869063826886,0.690869063826886,0.690869063826886,
0.690869063826886,0.690869063826886,0.690869063826886,0.690869063826886,
0.690869063826886,0.690869063826886,0.690869063826886,0.690869063826886,
0.690869063826886,0.690869063826886,0.690869063826886,0.690869063826886,
0.690869063826886,0.690869063826886,0.690869063826886,0.690869063826886,
0.690869063826886,0.690869063826886,0.690869063826886,0.690869063826886,
0.690869063826886,0.690869063826886,0.690869063826886,0.690869063826886,
0.690869063826886,0.690869063826886,0.690869063826886,0.690869063826886,
0.690869063826886,0.690869063826886,0.690869063826886,0.690869063826886,
0.690869063826886,0.690869063826886,0.690869063826886,0.690869063826886,
0.690869063826886,0.690869063826886,0.690869063826886,0.690869063826886,
0.690869063826886,0.690869063826886,0.690869063826886,0.690869063826886,
0.690869063826886,0.690869063826886,0.690869063826886),(0.525081031202671,
0.525081031202671,0.525081031202671,0.525081031202671,0.525081031202671,
0.525081031202671,0.525081031202671,0.525081031202671,0.525081031202671,
0.525081031202671,0.525081031202671,0.525081031202671,0.525081031202671,
0.525081031202671,0.525081031202671,0.525081031202671,0.525081031202671,
0.525081031202671,0.525081031202671,0.525081031202671,0.525081031202671,
0.525081031202671,0.525081031202671,0.525081031202671,0.525081031202671,
0.525081031202671,0.525081031202671,0.525081031202671,0.525081031202671,
0.525081031202671,0.525081031202671,0.525081031202671,0.525081031202671,
0.525081031202671,0.525081031202671,0.525081031202671,0.525081031202671,
0.525081031202671,0.525081031202671,0.525081031202671,0.525081031202671,
0.525081031202671,0.525081031202671,0.525081031202671,0.525081031202671,
0.525081031202671,0.525081031202671,0.525081031202671,0.525081031202671,
0.525081031202671,0.525081031202671,0.525081031202671,0.525081031202671,
0.525081031202671,0.525081031202671,0.525081031202671,0.525081031202671,
0.525081031202671,0.525081031202671,0.525081031202671,0.525081031202671,
0.525081031202671,0.525081031202671,0.525081031202671,0.525081031202671,
0.525081031202671,0.525081031202671,0.525081031202671,0.525081031202671,
0.525081031202671,0.525081031202671,0.525081031202671,0.525081031202671,
0.525081031202671,0.525081031202671,0.525081031202671,0.525081031202671,
0.525081031202671,0.525081031202671,0.525081031202671,0.525081031202671,
0.525081031202671,0.525081031202671,0.525081031202671,0.525081031202671,
0.525081031202671),(0.502635902127355,0.502635902127355,0.502635902127355,
0.502635902127355,0.502635902127355,0.502635902127355,0.502635902127355,
0.502635902127355,0.502635902127355,0.502635902127355,0.502635902127355,
0.502635902127355,0.502635902127355,0.502635902127355,0.502635902127355,
0.502635902127355,0.502635902127355,0.502635902127355,0.502635902127355,
0.502635902127355,0.502635902127355,0.502635902127355,0.502635902127355,
0.502635902127355,0.502635902127355,0.502635902127355,0.502635902127355,
0.502635902127355,0.502635902127355,0.502635902127355,0.502635902127355,
0.502635902127355,0.502635902127355,0.502635902127355,0.502635902127355,
0.502635902127355,0.502635902127355,0.502635902127355,0.502635902127355,
0.502635902127355,0.502635902127355,0.502635902127355,0.502635902127355,
0.502635902127355,0.502635902127355,0.502635902127355,0.502635902127355,
0.502635902127355,0.502635902127355,0.502635902127355,0.502635902127355,
0.502635902127355,0.502635902127355,0.502635902127355,0.502635902127355,
0.502635902127355,0.502635902127355,0.502635902127355,0.502635902127355,
0.502635902127355,0.502635902127355,0.502635902127355,0.502635902127355,
0.502635902127355,0.502635902127355,0.502635902127355,0.502635902127355,
0.502635902127355,0.502635902127355,0.502635902127355,0.502635902127355,
0.502635902127355,0.502635902127355,0.502635902127355,0.502635902127355,
0.502635902127355,0.502635902127355,0.502635902127355,0.502635902127355,
0.502635902127355,0.502635902127355,0.502635902127355,0.502635902127355,
0.502635902127355,0.502635902127355,0.502635902127355)))
REPRESENTATION_ITEM('')
SURFACE()
);
#13253=ADVANCED_FACE('',(#12319,#12320),#1433,.T.);
#13254=ADVANCED_FACE('',(#12321),#1736,.F.);
#13255=ADVANCED_FACE('',(#12322,#12323),#1434,.F.);
#13256=ADVANCED_FACE('',(#12324),#1737,.F.);
#13257=ADVANCED_FACE('',(#12325,#12326),#1435,.T.);
#13258=ADVANCED_FACE('',(#12327,#12328),#1436,.F.);
#13259=ADVANCED_FACE('',(#12329),#1738,.F.);
#13260=ADVANCED_FACE('',(#12330,#12331),#1437,.T.);
#13261=ADVANCED_FACE('',(#12332),#1739,.F.);
#13262=ADVANCED_FACE('',(#12333,#12334),#1438,.F.);
#13263=ADVANCED_FACE('',(#12335,#12336),#1439,.T.);
#13264=ADVANCED_FACE('',(#12337,#12338),#1440,.F.);
#13265=ADVANCED_FACE('',(#12339),#1740,.F.);
#13266=ADVANCED_FACE('',(#12340,#12341),#1441,.T.);
#13267=ADVANCED_FACE('',(#12342),#1741,.F.);
#13268=ADVANCED_FACE('',(#12343),#1442,.T.);
#13269=ADVANCED_FACE('',(#12344),#1742,.T.);
#13270=ADVANCED_FACE('',(#12345),#1443,.T.);
#13271=ADVANCED_FACE('',(#12346),#1743,.T.);
#13272=ADVANCED_FACE('',(#12347),#1444,.F.);
#13273=ADVANCED_FACE('',(#12348),#1744,.T.);
#13274=ADVANCED_FACE('',(#12349),#1445,.T.);
#13275=ADVANCED_FACE('',(#12350),#1745,.T.);
#13276=ADVANCED_FACE('',(#12351),#1446,.F.);
#13277=ADVANCED_FACE('',(#12352),#1447,.T.);
#13278=ADVANCED_FACE('',(#12353),#1746,.T.);
#13279=ADVANCED_FACE('',(#12354),#1448,.T.);
#13280=ADVANCED_FACE('',(#12355),#1747,.T.);
#13281=ADVANCED_FACE('',(#12356),#1449,.F.);
#13282=ADVANCED_FACE('',(#12357),#1450,.T.);
#13283=ADVANCED_FACE('',(#12358),#1748,.T.);
#13284=ADVANCED_FACE('',(#12359),#1451,.T.);
#13285=ADVANCED_FACE('',(#12360),#1749,.T.);
#13286=ADVANCED_FACE('',(#12361),#1452,.F.);
#13287=ADVANCED_FACE('',(#12362),#1453,.T.);
#13288=ADVANCED_FACE('',(#12363),#1454,.T.);
#13289=ADVANCED_FACE('',(#12364),#12686,.T.);
#13290=ADVANCED_FACE('',(#12365),#12687,.T.);
#13291=ADVANCED_FACE('',(#12366),#1750,.F.);
#13292=ADVANCED_FACE('',(#12367),#1455,.F.);
#13293=ADVANCED_FACE('',(#12368),#1456,.T.);
#13294=ADVANCED_FACE('',(#12369,#12370),#1457,.T.);
#13295=ADVANCED_FACE('',(#12371),#12688,.F.);
#13296=ADVANCED_FACE('',(#12372),#1751,.F.);
#13297=ADVANCED_FACE('',(#12373),#1752,.F.);
#13298=ADVANCED_FACE('',(#12374),#12689,.F.);
#13299=ADVANCED_FACE('',(#12375),#12690,.F.);
#13300=ADVANCED_FACE('',(#12376),#12691,.F.);
#13301=ADVANCED_FACE('',(#12377),#1458,.F.);
#13302=ADVANCED_FACE('',(#12378),#1459,.T.);
#13303=ADVANCED_FACE('',(#12379),#1460,.T.);
#13304=ADVANCED_FACE('',(#12380,#12381),#1461,.T.);
#13305=ADVANCED_FACE('',(#12382,#12383),#1462,.T.);
#13306=ADVANCED_FACE('',(#12384,#12385),#1463,.T.);
#13307=ADVANCED_FACE('',(#12386,#12387),#30,.F.);
#13308=ADVANCED_FACE('',(#12388,#12389),#1753,.F.);
#13309=ADVANCED_FACE('',(#12390,#12391),#1754,.T.);
#13310=ADVANCED_FACE('',(#12392,#12393),#1755,.F.);
#13311=ADVANCED_FACE('',(#12394,#12395),#1756,.F.);
#13312=ADVANCED_FACE('',(#12396,#12397),#1757,.F.);
#13313=ADVANCED_FACE('',(#12398,#12399),#321,.F.);
#13314=ADVANCED_FACE('',(#12400),#12692,.T.);
#13315=ADVANCED_FACE('',(#12401,#12402),#322,.F.);
#13316=ADVANCED_FACE('',(#12403,#12404),#323,.T.);
#13317=ADVANCED_FACE('',(#12405,#12406),#324,.T.);
#13318=ADVANCED_FACE('',(#12407,#12408),#325,.T.);
#13319=ADVANCED_FACE('',(#12409,#12410),#1758,.T.);
#13320=ADVANCED_FACE('',(#12411,#12412),#326,.T.);
#13321=ADVANCED_FACE('',(#12413,#12414),#327,.F.);
#13322=ADVANCED_FACE('',(#12415,#12416),#328,.T.);
#13323=ADVANCED_FACE('',(#12417,#12418),#329,.F.);
#13324=ADVANCED_FACE('',(#12419,#12420),#330,.T.);
#13325=ADVANCED_FACE('',(#12421,#12422),#1759,.F.);
#13326=ADVANCED_FACE('',(#12423,#12424),#1760,.F.);
#13327=ADVANCED_FACE('',(#12425,#12426),#1761,.F.);
#13328=ADVANCED_FACE('',(#12427,#12428),#1762,.F.);
#13329=ADVANCED_FACE('',(#12429,#12430),#1763,.T.);
#13330=ADVANCED_FACE('',(#12431),#1764,.F.);
#13331=ADVANCED_FACE('',(#12432),#1765,.F.);
#13332=ADVANCED_FACE('',(#12433,#12434,#12435,#12436,#12437,#12438),#1766,
 .F.);
#13522=CLOSED_SHELL('',(#13253,#13254,#13255,#13256,#13257,#13258,#13259,
#13260,#13261,#13262,#13263,#13264,#13265,#13266,#13267,#13268,#13269,#13270,
#13271,#13272,#13273,#13274,#13275,#13276,#13277,#13278,#13279,#13280,#13281,
#13282,#13283,#13284,#13285,#13286,#13287,#13288,#13289,#13290,#13291,#13292,
#13293,#13294,#13295,#13296,#13297,#13298,#13299,#13300,#13301,#13302,#13303,
#13304,#13305,#13306,#13307,#13308,#13309,#13310,#13311,#13312,#13313,#13314,
#13315,#13316,#13317,#13318,#13319,#13320,#13321,#13322,#13323,#13324,#13325,
#13326,#13327,#13328,#13329,#13330,#13331,#13332));
#13549=STYLED_ITEM('',(#13576),#13739);
#13576=PRESENTATION_STYLE_ASSIGNMENT((#13603));
#13603=SURFACE_STYLE_USAGE(.BOTH.,#13630);
#13630=SURFACE_SIDE_STYLE('',(#13657));
#13657=SURFACE_STYLE_FILL_AREA(#13684);
#13684=FILL_AREA_STYLE('',(#13711));
#13711=FILL_AREA_STYLE_COLOUR('',#13718);
#13718=COLOUR_RGB('', 0.09019608, 0.27058824, 0.51372549);
#13739=MANIFOLD_SOLID_BREP('Bottle',#13522);
#13767=SHAPE_DEFINITION_REPRESENTATION(#45569,#13795);
#13795=SHAPE_REPRESENTATION('Bottle',(#13802),#45485);
#13802=AXIS2_PLACEMENT_3D('',#19109,#15295,#15296);
#14848=AXIS2_PLACEMENT_3D('',#35377,#17941,#17942);
#14849=AXIS2_PLACEMENT_3D('',#35378,#17943,#17944);
#14850=AXIS2_PLACEMENT_3D('',#35380,#17945,#17946);
#14851=AXIS2_PLACEMENT_3D('',#35382,#17947,#17948);
#14852=AXIS2_PLACEMENT_3D('',#35383,#17949,#17950);
#14853=AXIS2_PLACEMENT_3D('',#35388,#17952,#17953);
#14854=AXIS2_PLACEMENT_3D('',#35391,#17955,#17956);
#14855=AXIS2_PLACEMENT_3D('',#35392,#17957,#17958);
#14856=AXIS2_PLACEMENT_3D('',#35394,#17959,#17960);
#14857=AXIS2_PLACEMENT_3D('',#35399,#17962,#17963);
#14858=AXIS2_PLACEMENT_3D('',#35403,#17965,#17966);
#14859=AXIS2_PLACEMENT_3D('',#35405,#17967,#17968);
#14860=AXIS2_PLACEMENT_3D('',#35407,#17970,#17971);
#14861=AXIS2_PLACEMENT_3D('',#35408,#17972,#17973);
#14862=AXIS2_PLACEMENT_3D('',#35413,#17976,#17977);
#14863=AXIS2_PLACEMENT_3D('',#35414,#17978,#17979);
#14864=AXIS2_PLACEMENT_3D('',#35416,#17980,#17981);
#14865=AXIS2_PLACEMENT_3D('',#35420,#17983,#17984);
#14866=AXIS2_PLACEMENT_3D('',#35423,#17986,#17987);
#14867=AXIS2_PLACEMENT_3D('',#35426,#17989,#17990);
#14868=AXIS2_PLACEMENT_3D('',#35427,#17991,#17992);
#14869=AXIS2_PLACEMENT_3D('',#35429,#17993,#17994);
#14870=AXIS2_PLACEMENT_3D('',#35434,#17996,#17997);
#14871=AXIS2_PLACEMENT_3D('',#35438,#17999,#18000);
#14872=AXIS2_PLACEMENT_3D('',#35440,#18001,#18002);
#14873=AXIS2_PLACEMENT_3D('',#35442,#18003,#18004);
#14874=AXIS2_PLACEMENT_3D('',#35445,#18006,#18007);
#14875=AXIS2_PLACEMENT_3D('',#35446,#18008,#18009);
#14876=AXIS2_PLACEMENT_3D('',#35451,#18012,#18013);
#14877=AXIS2_PLACEMENT_3D('',#35452,#18014,#18015);
#14878=AXIS2_PLACEMENT_3D('',#35454,#18016,#18017);
#14879=AXIS2_PLACEMENT_3D('',#35459,#18019,#18020);
#14880=AXIS2_PLACEMENT_3D('',#35461,#18021,#18022);
#14881=AXIS2_PLACEMENT_3D('',#35464,#18024,#18025);
#14882=AXIS2_PLACEMENT_3D('',#35467,#18027,#18028);
#14883=AXIS2_PLACEMENT_3D('',#35470,#18031,#18032);
#14884=AXIS2_PLACEMENT_3D('',#35471,#18033,#18034);
#14885=AXIS2_PLACEMENT_3D('',#35473,#18035,#18036);
#14886=AXIS2_PLACEMENT_3D('',#35478,#18038,#18039);
#14887=AXIS2_PLACEMENT_3D('',#35482,#18041,#18042);
#14888=AXIS2_PLACEMENT_3D('',#35484,#18043,#18044);
#14889=AXIS2_PLACEMENT_3D('',#35486,#18045,#18046);
#14890=AXIS2_PLACEMENT_3D('',#35489,#18048,#18049);
#14891=AXIS2_PLACEMENT_3D('',#35490,#18050,#18051);
#14892=AXIS2_PLACEMENT_3D('',#35492,#18052,#18053);
#14893=AXIS2_PLACEMENT_3D('',#35497,#18055,#18056);
#14894=AXIS2_PLACEMENT_3D('',#35499,#18057,#18058);
#14895=AXIS2_PLACEMENT_3D('',#35501,#18059,#18060);
#14896=AXIS2_PLACEMENT_3D('',#35505,#18062,#18063);
#14897=AXIS2_PLACEMENT_3D('',#35508,#18065,#18066);
#14898=AXIS2_PLACEMENT_3D('',#35509,#18067,#18068);
#14899=AXIS2_PLACEMENT_3D('',#35511,#18069,#18070);
#14900=AXIS2_PLACEMENT_3D('',#35516,#18072,#18073);
#14901=AXIS2_PLACEMENT_3D('',#35520,#18075,#18076);
#14902=AXIS2_PLACEMENT_3D('',#35522,#18077,#18078);
#14903=AXIS2_PLACEMENT_3D('',#35524,#18079,#18080);
#14904=AXIS2_PLACEMENT_3D('',#35527,#18082,#18083);
#14905=AXIS2_PLACEMENT_3D('',#35528,#18084,#18085);
#14906=AXIS2_PLACEMENT_3D('',#35533,#18088,#18089);
#14907=AXIS2_PLACEMENT_3D('',#35534,#18090,#18091);
#14908=AXIS2_PLACEMENT_3D('',#35536,#18092,#18093);
#14909=AXIS2_PLACEMENT_3D('',#35541,#18095,#18096);
#14910=AXIS2_PLACEMENT_3D('',#35543,#18097,#18098);
#14911=AXIS2_PLACEMENT_3D('',#35546,#18100,#18101);
#14912=AXIS2_PLACEMENT_3D('',#35549,#18103,#18104);
#14913=AXIS2_PLACEMENT_3D('',#35552,#18107,#18108);
#14914=AXIS2_PLACEMENT_3D('',#35554,#18110,#18111);
#14915=AXIS2_PLACEMENT_3D('',#35556,#18113,#18114);
#14916=AXIS2_PLACEMENT_3D('',#35558,#18116,#18117);
#14917=AXIS2_PLACEMENT_3D('',#35560,#18119,#18120);
#14918=AXIS2_PLACEMENT_3D('',#35561,#18121,#18122);
#14919=AXIS2_PLACEMENT_3D('',#35564,#18125,#18126);
#14920=AXIS2_PLACEMENT_3D('',#35566,#18128,#18129);
#14921=AXIS2_PLACEMENT_3D('',#35568,#18131,#18132);
#14922=AXIS2_PLACEMENT_3D('',#35569,#18133,#18134);
#14923=AXIS2_PLACEMENT_3D('',#35570,#18135,#18136);
#14924=AXIS2_PLACEMENT_3D('',#35573,#18139,#18140);
#14925=AXIS2_PLACEMENT_3D('',#35575,#18142,#18143);
#14926=AXIS2_PLACEMENT_3D('',#35577,#18145,#18146);
#14927=AXIS2_PLACEMENT_3D('',#35579,#18148,#18149);
#14928=AXIS2_PLACEMENT_3D('',#35581,#18151,#18152);
#14929=AXIS2_PLACEMENT_3D('',#35584,#18155,#18156);
#14930=AXIS2_PLACEMENT_3D('',#35586,#18158,#18159);
#14931=AXIS2_PLACEMENT_3D('',#35588,#18161,#18162);
#14932=AXIS2_PLACEMENT_3D('',#35589,#18163,#18164);
#14933=AXIS2_PLACEMENT_3D('',#35590,#18165,#18166);
#14934=AXIS2_PLACEMENT_3D('',#35591,#18167,#18168);
#14935=AXIS2_PLACEMENT_3D('',#36153,#18173,#18174);
#14936=AXIS2_PLACEMENT_3D('',#36156,#18177,#18178);
#14937=AXIS2_PLACEMENT_3D('',#36158,#18180,#18181);
#14938=AXIS2_PLACEMENT_3D('',#36160,#18183,#18184);
#14939=AXIS2_PLACEMENT_3D('',#36161,#18185,#18186);
#14940=AXIS2_PLACEMENT_3D('',#36162,#18187,#18188);
#14941=AXIS2_PLACEMENT_3D('',#37425,#18189,#18190);
#14942=AXIS2_PLACEMENT_3D('',#37447,#18191,#18192);
#14943=AXIS2_PLACEMENT_3D('',#37448,#18193,#18194);
#14944=AXIS2_PLACEMENT_3D('',#38516,#18195,#18196);
#14945=AXIS2_PLACEMENT_3D('',#38769,#18197,#18198);
#14946=AXIS2_PLACEMENT_3D('',#38770,#18199,#18200);
#14947=AXIS2_PLACEMENT_3D('',#38771,#18201,#18202);
#14948=AXIS2_PLACEMENT_3D('',#38772,#18203,#18204);
#14949=AXIS2_PLACEMENT_3D('',#38773,#18205,#18206);
#14950=AXIS2_PLACEMENT_3D('',#38774,#18207,#18208);
#14951=AXIS2_PLACEMENT_3D('',#38776,#18209,#18210);
#14952=AXIS2_PLACEMENT_3D('',#38777,#18211,#18212);
#14953=AXIS2_PLACEMENT_3D('',#38779,#18213,#18214);
#14954=AXIS2_PLACEMENT_3D('',#38781,#18215,#18216);
#14955=AXIS2_PLACEMENT_3D('',#38782,#18217,#18218);
#14956=AXIS2_PLACEMENT_3D('',#38785,#18219,#18220);
#14957=AXIS2_PLACEMENT_3D('',#38786,#18221,#18222);
#14958=AXIS2_PLACEMENT_3D('',#38788,#18223,#18224);
#14959=AXIS2_PLACEMENT_3D('',#38789,#18225,#18226);
#14960=AXIS2_PLACEMENT_3D('',#38792,#18227,#18228);
#14961=AXIS2_PLACEMENT_3D('',#38793,#18229,#18230);
#14962=AXIS2_PLACEMENT_3D('',#38795,#18231,#18232);
#14963=AXIS2_PLACEMENT_3D('',#38796,#18233,#18234);
#14964=AXIS2_PLACEMENT_3D('',#38805,#18235,#18236);
#14965=AXIS2_PLACEMENT_3D('',#38806,#18237,#18238);
#14966=AXIS2_PLACEMENT_3D('',#38807,#18239,#18240);
#14967=AXIS2_PLACEMENT_3D('',#38808,#18241,#18242);
#14968=AXIS2_PLACEMENT_3D('',#38810,#18243,#18244);
#14969=AXIS2_PLACEMENT_3D('',#38811,#18245,#18246);
#14970=AXIS2_PLACEMENT_3D('',#38813,#18247,#18248);
#14971=AXIS2_PLACEMENT_3D('',#38815,#18249,#18250);
#14972=AXIS2_PLACEMENT_3D('',#38816,#18251,#18252);
#14973=AXIS2_PLACEMENT_3D('',#38818,#18253,#18254);
#14974=AXIS2_PLACEMENT_3D('',#38820,#18255,#18256);
#14975=AXIS2_PLACEMENT_3D('',#38821,#18257,#18258);
#14976=AXIS2_PLACEMENT_3D('',#38823,#18259,#18260);
#14977=AXIS2_PLACEMENT_3D('',#38825,#18261,#18262);
#14978=AXIS2_PLACEMENT_3D('',#39428,#18263,#18264);
#14979=AXIS2_PLACEMENT_3D('',#39429,#18265,#18266);
#14980=AXIS2_PLACEMENT_3D('',#39430,#18267,#18268);
#14981=AXIS2_PLACEMENT_3D('',#39431,#18269,#18270);
#14982=AXIS2_PLACEMENT_3D('',#39433,#18271,#18272);
#14983=AXIS2_PLACEMENT_3D('',#39434,#18273,#18274);
#14984=AXIS2_PLACEMENT_3D('',#39442,#18275,#18276);
#14985=AXIS2_PLACEMENT_3D('',#39444,#18277,#18278);
#14986=AXIS2_PLACEMENT_3D('',#39445,#18279,#18280);
#14987=AXIS2_PLACEMENT_3D('',#39446,#18281,#18282);
#14988=AXIS2_PLACEMENT_3D('',#39447,#18283,#18284);
#14989=AXIS2_PLACEMENT_3D('',#39448,#18285,#18286);
#14990=AXIS2_PLACEMENT_3D('',#39449,#18287,#18288);
#14991=AXIS2_PLACEMENT_3D('',#39451,#18289,#18290);
#14992=AXIS2_PLACEMENT_3D('',#39452,#18291,#18292);
#14993=AXIS2_PLACEMENT_3D('',#39453,#18293,#18294);
#14994=AXIS2_PLACEMENT_3D('',#39454,#18295,#18296);
#14995=AXIS2_PLACEMENT_3D('',#39455,#18297,#18298);
#14996=AXIS2_PLACEMENT_3D('',#39456,#18299,#18300);
#14997=AXIS2_PLACEMENT_3D('',#39458,#18302,#18303);
#14998=AXIS2_PLACEMENT_3D('',#39460,#18305,#18306);
#15295=DIRECTION('',(0.,0.,1.));
#15296=DIRECTION('',(1.,0.,0.));
#17941=DIRECTION('',(0.,0.,1.));
#17942=DIRECTION('',(1.,0.,0.));
#17943=DIRECTION('',(0.,0.,1.));
#17944=DIRECTION('',(1.,0.,0.));
#17945=DIRECTION('',(0.,0.,1.));
#17946=DIRECTION('',(1.,0.,0.));
#17947=DIRECTION('',(0.,0.,-1.));
#17948=DIRECTION('',(-1.,0.,0.));
#17949=DIRECTION('',(0.,0.,1.));
#17950=DIRECTION('',(-1.,0.,0.));
#17951=DIRECTION('',(0.,0.,-1.));
#17952=DIRECTION('',(0.,0.,-1.));
#17953=DIRECTION('',(-1.,0.,0.));
#17954=DIRECTION('',(0.,0.,1.));
#17955=DIRECTION('',(0.,0.,-1.));
#17956=DIRECTION('',(-1.04744440165294E-14,1.,0.));
#17957=DIRECTION('',(0.,0.,-1.));
#17958=DIRECTION('',(-1.,0.,0.));
#17959=DIRECTION('',(0.,0.,-1.));
#17960=DIRECTION('',(-1.,0.,0.));
#17961=DIRECTION('',(0.,-1.,0.));
#17962=DIRECTION('',(0.,0.,-1.));
#17963=DIRECTION('',(-1.,0.,0.));
#17964=DIRECTION('',(-0.998092281178314,0.061739762327613,0.));
#17965=DIRECTION('',(0.,0.,-1.));
#17966=DIRECTION('',(-1.,0.,0.));
#17967=DIRECTION('',(0.,0.,-1.));
#17968=DIRECTION('',(-1.,0.,0.));
#17969=DIRECTION('',(-0.998092281178314,-0.0617397623276126,0.));
#17970=DIRECTION('',(0.,0.,-1.));
#17971=DIRECTION('',(-1.,0.,0.));
#17972=DIRECTION('',(0.,0.,1.));
#17973=DIRECTION('',(-1.,0.,0.));
#17974=DIRECTION('',(0.,0.,-1.));
#17975=DIRECTION('',(0.,0.,1.));
#17976=DIRECTION('',(0.,0.,-1.));
#17977=DIRECTION('',(-1.04744440165294E-14,1.,0.));
#17978=DIRECTION('',(0.,0.,-1.));
#17979=DIRECTION('',(-1.,0.,0.));
#17980=DIRECTION('',(0.,0.,-1.));
#17981=DIRECTION('',(-1.,0.,0.));
#17982=DIRECTION('',(-0.998092281178314,-0.0617397623276126,0.));
#17983=DIRECTION('',(0.,0.,-1.));
#17984=DIRECTION('',(-1.,0.,0.));
#17985=DIRECTION('',(-0.998092281178314,0.061739762327613,0.));
#17986=DIRECTION('',(0.,0.,-1.));
#17987=DIRECTION('',(-1.,0.,0.));
#17988=DIRECTION('',(0.,-1.,0.));
#17989=DIRECTION('',(0.,0.,-1.));
#17990=DIRECTION('',(-1.04744440165294E-14,1.,0.));
#17991=DIRECTION('',(0.,0.,-1.));
#17992=DIRECTION('',(3.49148133884314E-15,-1.,0.));
#17993=DIRECTION('',(0.,0.,-1.));
#17994=DIRECTION('',(3.46944695195361E-15,-1.,0.));
#17995=DIRECTION('',(1.,3.49148133884314E-15,0.));
#17996=DIRECTION('',(0.,0.,-1.));
#17997=DIRECTION('',(3.46944695195361E-15,-1.,0.));
#17998=DIRECTION('',(-0.0617397623276095,-0.998092281178314,0.));
#17999=DIRECTION('',(0.,0.,-1.));
#18000=DIRECTION('',(-1.,0.,0.));
#18001=DIRECTION('',(0.,0.,-1.));
#18002=DIRECTION('',(3.49148133884314E-15,-1.,0.));
#18003=DIRECTION('',(0.,0.,-1.));
#18004=DIRECTION('',(-1.,0.,0.));
#18005=DIRECTION('',(0.0617397623276161,-0.998092281178314,0.));
#18006=DIRECTION('',(0.,0.,-1.));
#18007=DIRECTION('',(-1.,0.,0.));
#18008=DIRECTION('',(0.,0.,1.));
#18009=DIRECTION('',(-1.,-1.38777878078145E-15,0.));
#18010=DIRECTION('',(0.,0.,-1.));
#18011=DIRECTION('',(0.,0.,1.));
#18012=DIRECTION('',(0.,0.,-1.));
#18013=DIRECTION('',(-1.04744440165294E-14,1.,0.));
#18014=DIRECTION('',(0.,0.,-1.));
#18015=DIRECTION('',(3.49148133884314E-15,-1.,0.));
#18016=DIRECTION('',(0.,0.,-1.));
#18017=DIRECTION('',(3.46944695195361E-15,-1.,0.));
#18018=DIRECTION('',(0.0617397623276161,-0.998092281178314,0.));
#18019=DIRECTION('',(0.,0.,1.));
#18020=DIRECTION('',(-1.,0.,0.));
#18021=DIRECTION('',(0.,0.,-1.));
#18022=DIRECTION('',(3.49148133884314E-15,-1.,0.));
#18023=DIRECTION('',(-0.0617397623276095,-0.998092281178314,0.));
#18024=DIRECTION('',(0.,0.,-1.));
#18025=DIRECTION('',(3.46944695195361E-15,-1.,0.));
#18026=DIRECTION('',(1.,3.49148133884314E-15,0.));
#18027=DIRECTION('',(0.,0.,-1.));
#18028=DIRECTION('',(-1.,0.,0.));
#18029=DIRECTION('',(0.,0.,-1.));
#18030=DIRECTION('',(0.,0.,1.));
#18031=DIRECTION('',(0.,0.,-1.));
#18032=DIRECTION('',(-1.04744440165294E-14,1.,0.));
#18033=DIRECTION('',(0.,0.,-1.));
#18034=DIRECTION('',(1.,0.,0.));
#18035=DIRECTION('',(0.,0.,-1.));
#18036=DIRECTION('',(1.,0.,0.));
#18037=DIRECTION('',(0.,1.,0.));
#18038=DIRECTION('',(0.,0.,-1.));
#18039=DIRECTION('',(1.,0.,0.));
#18040=DIRECTION('',(0.998092281178314,-0.061739762327613,0.));
#18041=DIRECTION('',(0.,0.,-1.));
#18042=DIRECTION('',(-1.,0.,0.));
#18043=DIRECTION('',(0.,0.,-1.));
#18044=DIRECTION('',(1.,0.,0.));
#18045=DIRECTION('',(0.,0.,-1.));
#18046=DIRECTION('',(-1.,0.,0.));
#18047=DIRECTION('',(0.998092281178314,0.0617397623276126,0.));
#18048=DIRECTION('',(0.,0.,-1.));
#18049=DIRECTION('',(-1.04744440165294E-14,1.,0.));
#18050=DIRECTION('',(0.,0.,-1.));
#18051=DIRECTION('',(1.,0.,0.));
#18052=DIRECTION('',(0.,0.,-1.));
#18053=DIRECTION('',(1.,0.,0.));
#18054=DIRECTION('',(0.998092281178314,0.0617397623276126,0.));
#18055=DIRECTION('',(0.,0.,1.));
#18056=DIRECTION('',(-1.,0.,0.));
#18057=DIRECTION('',(0.,0.,-1.));
#18058=DIRECTION('',(1.,0.,0.));
#18059=DIRECTION('',(0.,0.,1.));
#18060=DIRECTION('',(-1.,-5.20417042793043E-15,0.));
#18061=DIRECTION('',(0.998092281178314,-0.061739762327613,0.));
#18062=DIRECTION('',(0.,0.,-1.));
#18063=DIRECTION('',(1.,0.,0.));
#18064=DIRECTION('',(0.,1.,0.));
#18065=DIRECTION('',(0.,0.,-1.));
#18066=DIRECTION('',(-1.04744440165294E-14,1.,0.));
#18067=DIRECTION('',(0.,0.,-1.));
#18068=DIRECTION('',(-1.04744440165294E-14,1.,0.));
#18069=DIRECTION('',(0.,0.,-1.));
#18070=DIRECTION('',(-1.04083408558608E-14,1.,0.));
#18071=DIRECTION('',(-1.,-1.04744440165294E-14,0.));
#18072=DIRECTION('',(0.,0.,-1.));
#18073=DIRECTION('',(-1.04083408558608E-14,1.,0.));
#18074=DIRECTION('',(0.0617397623276026,0.998092281178314,0.));
#18075=DIRECTION('',(0.,0.,-1.));
#18076=DIRECTION('',(-1.,0.,0.));
#18077=DIRECTION('',(0.,0.,-1.));
#18078=DIRECTION('',(-1.04744440165294E-14,1.,0.));
#18079=DIRECTION('',(0.,0.,-1.));
#18080=DIRECTION('',(-1.,0.,0.));
#18081=DIRECTION('',(-0.061739762327623,0.998092281178313,0.));
#18082=DIRECTION('',(0.,0.,-1.));
#18083=DIRECTION('',(-1.,0.,0.));
#18084=DIRECTION('',(0.,0.,1.));
#18085=DIRECTION('',(-1.,1.38777878078145E-15,0.));
#18086=DIRECTION('',(0.,0.,-1.));
#18087=DIRECTION('',(0.,0.,1.));
#18088=DIRECTION('',(0.,0.,-1.));
#18089=DIRECTION('',(-1.04744440165294E-14,1.,0.));
#18090=DIRECTION('',(0.,0.,-1.));
#18091=DIRECTION('',(-1.04744440165294E-14,1.,0.));
#18092=DIRECTION('',(0.,0.,-1.));
#18093=DIRECTION('',(-1.04083408558608E-14,1.,0.));
#18094=DIRECTION('',(-0.061739762327623,0.998092281178313,0.));
#18095=DIRECTION('',(0.,0.,1.));
#18096=DIRECTION('',(-1.,0.,0.));
#18097=DIRECTION('',(0.,0.,-1.));
#18098=DIRECTION('',(-1.04744440165294E-14,1.,0.));
#18099=DIRECTION('',(0.0617397623276026,0.998092281178314,0.));
#18100=DIRECTION('',(0.,0.,-1.));
#18101=DIRECTION('',(-1.04083408558608E-14,1.,0.));
#18102=DIRECTION('',(-1.,-1.04744440165294E-14,0.));
#18103=DIRECTION('',(0.,0.,-1.));
#18104=DIRECTION('',(-1.,0.,0.));
#18105=DIRECTION('',(0.,0.,-1.));
#18106=DIRECTION('',(0.,0.,1.));
#18107=DIRECTION('',(-0.0617397623276126,0.998092281178314,0.));
#18108=DIRECTION('',(-0.998092281178314,-0.0617397623276126,0.));
#18109=DIRECTION('',(0.,0.,1.));
#18110=DIRECTION('',(0.,0.,1.));
#18111=DIRECTION('',(1.,0.,0.));
#18112=DIRECTION('',(0.,0.,1.));
#18113=DIRECTION('',(-1.,0.,0.));
#18114=DIRECTION('',(0.,0.,1.));
#18115=DIRECTION('',(0.,0.,1.));
#18116=DIRECTION('',(0.,0.,1.));
#18117=DIRECTION('',(1.,0.,0.));
#18118=DIRECTION('',(0.,0.,1.));
#18119=DIRECTION('',(0.061739762327613,0.998092281178314,0.));
#18120=DIRECTION('',(-0.998092281178314,0.061739762327613,0.));
#18121=DIRECTION('',(0.,0.,1.));
#18122=DIRECTION('',(-3.46944695195361E-15,1.,0.));
#18123=DIRECTION('',(0.,0.,1.));
#18124=DIRECTION('',(0.,0.,1.));
#18125=DIRECTION('',(0.,-1.,0.));
#18126=DIRECTION('',(0.,0.,1.));
#18127=DIRECTION('',(0.,0.,1.));
#18128=DIRECTION('',(0.,0.,1.));
#18129=DIRECTION('',(-3.46944695195361E-15,1.,0.));
#18130=DIRECTION('',(0.,0.,1.));
#18131=DIRECTION('',(-0.998092281178314,0.0617397623276096,0.));
#18132=DIRECTION('',(-0.0617397623276096,-0.998092281178314,0.));
#18133=DIRECTION('',(-0.998092281178314,-0.0617397623276161,0.));
#18134=DIRECTION('',(0.0617397623276161,-0.998092281178314,0.));
#18135=DIRECTION('',(0.,0.,1.));
#18136=DIRECTION('',(-1.,0.,0.));
#18137=DIRECTION('',(0.,0.,1.));
#18138=DIRECTION('',(0.,0.,1.));
#18139=DIRECTION('',(1.,0.,0.));
#18140=DIRECTION('',(0.,0.,1.));
#18141=DIRECTION('',(0.,0.,1.));
#18142=DIRECTION('',(0.,0.,1.));
#18143=DIRECTION('',(-1.,0.,0.));
#18144=DIRECTION('',(0.,0.,1.));
#18145=DIRECTION('',(-0.061739762327613,-0.998092281178314,0.));
#18146=DIRECTION('',(0.998092281178314,-0.061739762327613,0.));
#18147=DIRECTION('',(0.,0.,1.));
#18148=DIRECTION('',(0.0617397623276126,-0.998092281178314,0.));
#18149=DIRECTION('',(0.998092281178314,0.0617397623276126,0.));
#18150=DIRECTION('',(0.,0.,-1.));
#18151=DIRECTION('',(0.,0.,1.));
#18152=DIRECTION('',(1.04083408558608E-14,-1.,0.));
#18153=DIRECTION('',(0.,0.,1.));
#18154=DIRECTION('',(0.,0.,1.));
#18155=DIRECTION('',(0.,1.,0.));
#18156=DIRECTION('',(0.,0.,1.));
#18157=DIRECTION('',(0.,0.,1.));
#18158=DIRECTION('',(0.,0.,1.));
#18159=DIRECTION('',(1.04083408558608E-14,-1.,0.));
#18160=DIRECTION('',(0.,0.,1.));
#18161=DIRECTION('',(0.998092281178314,-0.0617397623276026,0.));
#18162=DIRECTION('',(0.0617397623276026,0.998092281178314,0.));
#18163=DIRECTION('',(0.998092281178313,0.061739762327623,0.));
#18164=DIRECTION('',(-0.061739762327623,0.998092281178313,0.));
#18165=DIRECTION('',(0.,0.,-1.));
#18166=DIRECTION('',(-1.,0.,0.));
#18167=DIRECTION('',(0.,0.,-1.));
#18168=DIRECTION('',(-1.,0.,0.));
#18169=DIRECTION('',(-0.866025403784441,0.,0.5));
#18170=DIRECTION('',(0.866025403784441,0.,-0.5));
#18171=DIRECTION('',(0.866025403784439,0.,0.5));
#18172=DIRECTION('',(-0.866025403784439,0.,-0.5));
#18173=DIRECTION('',(0.,0.,1.));
#18174=DIRECTION('',(1.,0.,0.));
#18175=DIRECTION('',(0.,0.,1.));
#18176=DIRECTION('',(0.,0.,-1.));
#18177=DIRECTION('',(0.,1.,0.));
#18178=DIRECTION('',(0.,0.,1.));
#18179=DIRECTION('',(0.,0.,1.));
#18180=DIRECTION('',(0.,1.,0.));
#18181=DIRECTION('',(0.,0.,1.));
#18182=DIRECTION('',(0.,0.,-1.));
#18183=DIRECTION('',(0.,0.,-1.));
#18184=DIRECTION('',(-1.,0.,0.));
#18185=DIRECTION('',(0.,0.,-1.));
#18186=DIRECTION('',(-1.,0.,0.));
#18187=DIRECTION('',(0.,0.,-1.));
#18188=DIRECTION('',(-1.,0.,0.));
#18189=DIRECTION('',(-0.0179359317491036,0.0175778306283821,-0.999684611376354));
#18190=DIRECTION('',(-0.999839088515442,0.,0.0179387033146474));
#18191=DIRECTION('',(0.0205587778800031,-0.295683717505608,0.955064644856119));
#18192=DIRECTION('',(0.595793945716029,-0.763497654096111,-0.249200534585825));
#18193=DIRECTION('',(-0.0175759874682992,0.0179054946361856,-0.99968518941032));
#18194=DIRECTION('',(0.,0.999839634236857,0.0179082609180536));
#18195=DIRECTION('',(0.920446420278218,-0.390077155728526,-0.0248636275663566));
#18196=DIRECTION('',(0.390197784505042,0.92073106223661,0.));
#18197=DIRECTION('',(0.706883616772413,-0.706883616772409,-0.0251217968606994));
#18198=DIRECTION('',(0.707106781186546,0.707106781186549,0.));
#18199=DIRECTION('',(0.706883616772413,-0.706883616772409,-0.0251217968606994));
#18200=DIRECTION('',(0.707106781186546,0.707106781186549,0.));
#18201=DIRECTION('',(0.706883616772383,-0.706883616772439,-0.0251217968606994));
#18202=DIRECTION('',(0.707106157141816,0.707107404359837,-3.50945448125777E-5));
#18203=DIRECTION('',(0.706883616772383,-0.70688361677244,-0.0251217968606994));
#18204=DIRECTION('',(0.707106157141816,0.707107404359837,-3.50945448118755E-5));
#18205=DIRECTION('',(0.,0.,1.));
#18206=DIRECTION('',(1.,0.,0.));
#18207=DIRECTION('',(0.,0.,-1.));
#18208=DIRECTION('',(-1.,0.,0.));
#18209=DIRECTION('',(0.,0.,1.));
#18210=DIRECTION('',(1.,0.,0.));
#18211=DIRECTION('',(0.,0.,1.));
#18212=DIRECTION('',(1.,0.,0.));
#18213=DIRECTION('',(0.,0.,-1.));
#18214=DIRECTION('',(1.,0.,0.));
#18215=DIRECTION('',(0.,0.,-1.));
#18216=DIRECTION('',(-1.,0.,0.));
#18217=DIRECTION('',(0.,0.,-1.));
#18218=DIRECTION('',(-1.,0.,0.));
#18219=DIRECTION('',(0.,0.,-1.));
#18220=DIRECTION('',(-1.,0.,0.));
#18221=DIRECTION('',(0.,0.,1.));
#18222=DIRECTION('',(-1.,0.,0.));
#18223=DIRECTION('',(0.,0.,1.));
#18224=DIRECTION('',(1.,0.,0.));
#18225=DIRECTION('',(0.,0.,1.));
#18226=DIRECTION('',(1.,0.,0.));
#18227=DIRECTION('',(0.,0.,-1.));
#18228=DIRECTION('',(1.,0.,0.));
#18229=DIRECTION('',(0.,0.,-1.));
#18230=DIRECTION('',(1.,0.,0.));
#18231=DIRECTION('',(0.,0.,1.));
#18232=DIRECTION('',(1.,0.,0.));
#18233=DIRECTION('',(0.,0.,1.));
#18234=DIRECTION('',(1.,0.,0.));
#18235=DIRECTION('',(0.,0.,-1.));
#18236=DIRECTION('',(-1.,0.,0.));
#18237=DIRECTION('',(0.,0.,-1.));
#18238=DIRECTION('',(-1.,0.,0.));
#18239=DIRECTION('',(0.,0.,1.));
#18240=DIRECTION('',(1.,0.,0.));
#18241=DIRECTION('',(0.,0.,-1.));
#18242=DIRECTION('',(1.,0.,0.));
#18243=DIRECTION('',(0.,0.,-1.));
#18244=DIRECTION('',(-1.,0.,0.));
#18245=DIRECTION('',(0.,0.,-1.));
#18246=DIRECTION('',(-1.,0.,0.));
#18247=DIRECTION('',(0.,0.,1.));
#18248=DIRECTION('',(1.,0.,0.));
#18249=DIRECTION('',(0.,0.,-1.));
#18250=DIRECTION('',(-1.,0.,0.));
#18251=DIRECTION('',(0.,0.,-1.));
#18252=DIRECTION('',(-1.,0.,0.));
#18253=DIRECTION('',(0.,0.,1.));
#18254=DIRECTION('',(-1.,0.,0.));
#18255=DIRECTION('',(0.,0.,-1.));
#18256=DIRECTION('',(-1.,0.,0.));
#18257=DIRECTION('',(0.,0.,-1.));
#18258=DIRECTION('',(-1.,0.,0.));
#18259=DIRECTION('',(0.,0.,1.));
#18260=DIRECTION('',(-1.,0.,0.));
#18261=DIRECTION('',(0.,0.,-1.));
#18262=DIRECTION('',(-1.,0.,0.));
#18263=DIRECTION('',(0.,0.,1.));
#18264=DIRECTION('',(1.,0.,0.));
#18265=DIRECTION('',(0.,0.,1.));
#18266=DIRECTION('',(1.,0.,0.));
#18267=DIRECTION('',(0.,0.,-1.));
#18268=DIRECTION('',(-1.,0.,0.));
#18269=DIRECTION('',(0.,0.,-1.));
#18270=DIRECTION('',(1.,0.,0.));
#18271=DIRECTION('',(0.,0.,1.));
#18272=DIRECTION('',(1.,0.,0.));
#18273=DIRECTION('',(0.,0.,1.));
#18274=DIRECTION('',(1.,0.,0.));
#18275=DIRECTION('',(0.,0.,1.));
#18276=DIRECTION('',(-1.,0.,0.));
#18277=DIRECTION('',(0.,0.,-1.));
#18278=DIRECTION('',(-1.,0.,0.));
#18279=DIRECTION('',(0.,0.,-1.));
#18280=DIRECTION('',(-1.,0.,0.));
#18281=DIRECTION('',(0.,0.,-1.));
#18282=DIRECTION('',(-1.,0.,0.));
#18283=DIRECTION('',(0.,0.,-1.));
#18284=DIRECTION('',(-1.,0.,0.));
#18285=DIRECTION('',(0.,0.,-1.));
#18286=DIRECTION('',(-1.,0.,0.));
#18287=DIRECTION('',(0.,0.,-1.));
#18288=DIRECTION('',(-1.,0.,0.));
#18289=DIRECTION('',(0.,0.,1.));
#18290=DIRECTION('',(1.04744440165294E-14,-1.,0.));
#18291=DIRECTION('',(0.,0.,1.));
#18292=DIRECTION('',(-1.,0.,0.));
#18293=DIRECTION('',(0.,0.,1.));
#18294=DIRECTION('',(-3.49148133884314E-15,1.,0.));
#18295=DIRECTION('',(0.,0.,1.));
#18296=DIRECTION('',(1.,0.,0.));
#18297=DIRECTION('',(0.,0.,-1.));
#18298=DIRECTION('',(-1.,0.,0.));
#18299=DIRECTION('',(0.,0.,-1.));
#18300=DIRECTION('',(-1.,0.,0.));
#18301=DIRECTION('',(0.,0.,1.));
#18302=DIRECTION('',(0.,0.,-1.));
#18303=DIRECTION('',(-1.,0.,0.));
#18304=DIRECTION('',(0.,0.,-1.));
#18305=DIRECTION('',(0.,0.,-1.));
#18306=DIRECTION('',(-1.,0.,0.));
#19109=CARTESIAN_POINT('',(0.,0.,0.));
#35377=CARTESIAN_POINT('',(0.,0.,0.0840000001));
#35378=CARTESIAN_POINT('',(0.,0.,0.0840000001));
#35379=CARTESIAN_POINT('',(0.05,0.,0.0840000001));
#35380=CARTESIAN_POINT('',(0.,0.,0.0840000001));
#35381=CARTESIAN_POINT('',(0.053,0.,0.0840000001));
#35382=CARTESIAN_POINT('',(0.04368363807983,0.0108046177216235,0.083));
#35383=CARTESIAN_POINT('',(0.04368363807983,0.0108046177216235,0.071));
#35384=CARTESIAN_POINT('',(0.0439923368914681,0.00581415631573189,0.071));
#35385=CARTESIAN_POINT('',(0.0485373756442556,0.0120051308018038,0.071));
#35386=CARTESIAN_POINT('',(0.0439923368914681,0.00581415631573189,0.071));
#35387=CARTESIAN_POINT('',(0.0439923368914681,0.00581415631573189,0.081));
#35388=CARTESIAN_POINT('',(0.04368363807983,0.0108046177216235,0.081));
#35389=CARTESIAN_POINT('',(0.0485373756442556,0.0120051308018038,0.081));
#35390=CARTESIAN_POINT('',(0.0485373756442556,0.0120051308018038,0.083));
#35391=CARTESIAN_POINT('',(0.00256146516479152,-0.04,0.081));
#35392=CARTESIAN_POINT('',(0.043,-1.7347234759768E-17,0.081));
#35393=CARTESIAN_POINT('',(0.041603,-1.7347234759768E-17,0.081));
#35394=CARTESIAN_POINT('',(0.04,0.0025614651647911,0.081));
#35395=CARTESIAN_POINT('',(0.037,0.0025614651647911,0.081));
#35396=CARTESIAN_POINT('',(0.0398147807130172,0.00555574200832604,0.081));
#35397=CARTESIAN_POINT('',(0.037,0.00256146516479108,0.081));
#35398=CARTESIAN_POINT('',(0.037,-0.00256146516479112,0.081));
#35399=CARTESIAN_POINT('',(0.04,-0.00256146516479113,0.081));
#35400=CARTESIAN_POINT('',(0.0398147807130172,-0.00555574200832608,0.081));
#35401=CARTESIAN_POINT('',(0.049618820174773,-0.00616219802209742,0.081));
#35402=CARTESIAN_POINT('',(0.0439923368914681,-0.00581415631573192,0.081));
#35403=CARTESIAN_POINT('',(0.04368363807983,-0.0108046177216235,0.081));
#35404=CARTESIAN_POINT('',(0.0485373756442556,-0.0120051308018039,0.081));
#35405=CARTESIAN_POINT('',(0.,0.,0.081));
#35406=CARTESIAN_POINT('',(0.049618820174773,0.00616219802209738,0.081));
#35407=CARTESIAN_POINT('',(0.04368363807983,-0.0108046177216235,0.083));
#35408=CARTESIAN_POINT('',(0.04368363807983,-0.0108046177216235,0.071));
#35409=CARTESIAN_POINT('',(0.0485373756442556,-0.0120051308018039,0.071));
#35410=CARTESIAN_POINT('',(0.0439923368914681,-0.00581415631573192,0.071));
#35411=CARTESIAN_POINT('',(0.0485373756442556,-0.0120051308018039,0.083));
#35412=CARTESIAN_POINT('',(0.0439923368914681,-0.00581415631573192,0.071));
#35413=CARTESIAN_POINT('',(0.00256146516479152,-0.04,0.071));
#35414=CARTESIAN_POINT('',(0.043,-1.7347234759768E-17,0.071));
#35415=CARTESIAN_POINT('',(0.041603,-1.7347234759768E-17,0.071));
#35416=CARTESIAN_POINT('',(0.04,0.0025614651647911,0.071));
#35417=CARTESIAN_POINT('',(0.037,0.0025614651647911,0.071));
#35418=CARTESIAN_POINT('',(0.0398147807130172,0.00555574200832604,0.071));
#35419=CARTESIAN_POINT('',(0.049618820174773,0.00616219802209738,0.071));
#35420=CARTESIAN_POINT('',(0.,0.,0.071));
#35421=CARTESIAN_POINT('',(0.049618820174773,-0.00616219802209742,0.071));
#35422=CARTESIAN_POINT('',(0.0398147807130172,-0.00555574200832608,0.071));
#35423=CARTESIAN_POINT('',(0.04,-0.00256146516479113,0.071));
#35424=CARTESIAN_POINT('',(0.037,-0.00256146516479112,0.071));
#35425=CARTESIAN_POINT('',(0.037,0.00256146516479108,0.071));
#35426=CARTESIAN_POINT('',(0.00256146516479152,-0.04,0.081));
#35427=CARTESIAN_POINT('',(-1.32786462810487E-16,0.043,0.081));
#35428=CARTESIAN_POINT('',(-1.27908863380123E-16,0.041603,0.081));
#35429=CARTESIAN_POINT('',(-0.00256146516479124,0.04,0.081));
#35430=CARTESIAN_POINT('',(-0.00256146516479123,0.037,0.081));
#35431=CARTESIAN_POINT('',(-0.00555574200832618,0.0398147807130172,0.081));
#35432=CARTESIAN_POINT('',(-0.00256146516479121,0.037,0.081));
#35433=CARTESIAN_POINT('',(0.002561465164791,0.037,0.081));
#35434=CARTESIAN_POINT('',(0.00256146516479099,0.04,0.081));
#35435=CARTESIAN_POINT('',(0.00555574200832594,0.0398147807130172,0.081));
#35436=CARTESIAN_POINT('',(0.00616219802209724,0.049618820174773,0.081));
#35437=CARTESIAN_POINT('',(0.00581415631573177,0.0439923368914681,0.081));
#35438=CARTESIAN_POINT('',(0.0108046177216233,0.0436836380798301,0.081));
#35439=CARTESIAN_POINT('',(0.0120051308018037,0.0485373756442557,0.081));
#35440=CARTESIAN_POINT('',(0.,0.,0.081));
#35441=CARTESIAN_POINT('',(-0.012005130801804,0.0485373756442556,0.081));
#35442=CARTESIAN_POINT('',(-0.0108046177216236,0.04368363807983,0.081));
#35443=CARTESIAN_POINT('',(-0.00581415631573204,0.0439923368914681,0.081));
#35444=CARTESIAN_POINT('',(-0.00616219802209755,0.049618820174773,0.081));
#35445=CARTESIAN_POINT('',(0.0108046177216233,0.0436836380798301,0.083));
#35446=CARTESIAN_POINT('',(0.0108046177216233,0.0436836380798301,0.071));
#35447=CARTESIAN_POINT('',(0.0120051308018037,0.0485373756442557,0.071));
#35448=CARTESIAN_POINT('',(0.00581415631573177,0.0439923368914681,0.071));
#35449=CARTESIAN_POINT('',(0.0120051308018037,0.0485373756442557,0.083));
#35450=CARTESIAN_POINT('',(0.00581415631573177,0.0439923368914681,0.071));
#35451=CARTESIAN_POINT('',(0.00256146516479152,-0.04,0.071));
#35452=CARTESIAN_POINT('',(-1.32786462810487E-16,0.043,0.071));
#35453=CARTESIAN_POINT('',(-1.27908863380123E-16,0.041603,0.071));
#35454=CARTESIAN_POINT('',(-0.00256146516479124,0.04,0.071));
#35455=CARTESIAN_POINT('',(-0.00256146516479123,0.037,0.071));
#35456=CARTESIAN_POINT('',(-0.00555574200832618,0.0398147807130172,0.071));
#35457=CARTESIAN_POINT('',(-0.00616219802209755,0.049618820174773,0.071));
#35458=CARTESIAN_POINT('',(-0.00581415631573204,0.0439923368914681,0.071));
#35459=CARTESIAN_POINT('',(-0.0108046177216236,0.04368363807983,0.071));
#35460=CARTESIAN_POINT('',(-0.012005130801804,0.0485373756442556,0.071));
#35461=CARTESIAN_POINT('',(0.,0.,0.071));
#35462=CARTESIAN_POINT('',(0.00616219802209724,0.049618820174773,0.071));
#35463=CARTESIAN_POINT('',(0.00555574200832594,0.0398147807130172,0.071));
#35464=CARTESIAN_POINT('',(0.00256146516479099,0.04,0.071));
#35465=CARTESIAN_POINT('',(0.002561465164791,0.037,0.071));
#35466=CARTESIAN_POINT('',(-0.00256146516479121,0.037,0.071));
#35467=CARTESIAN_POINT('',(-0.0108046177216236,0.04368363807983,0.083));
#35468=CARTESIAN_POINT('',(-0.00581415631573204,0.0439923368914681,0.071));
#35469=CARTESIAN_POINT('',(-0.012005130801804,0.0485373756442556,0.083));
#35470=CARTESIAN_POINT('',(0.00256146516479152,-0.04,0.081));
#35471=CARTESIAN_POINT('',(-0.043,1.7347234759768E-17,0.081));
#35472=CARTESIAN_POINT('',(-0.041603,1.7347234759768E-17,0.081));
#35473=CARTESIAN_POINT('',(-0.04,-0.0025614651647911,0.081));
#35474=CARTESIAN_POINT('',(-0.037,-0.0025614651647911,0.081));
#35475=CARTESIAN_POINT('',(-0.0398147807130172,-0.00555574200832604,0.081));
#35476=CARTESIAN_POINT('',(-0.037,-0.00256146516479108,0.081));
#35477=CARTESIAN_POINT('',(-0.037,0.00256146516479112,0.081));
#35478=CARTESIAN_POINT('',(-0.04,0.00256146516479113,0.081));
#35479=CARTESIAN_POINT('',(-0.0398147807130172,0.00555574200832608,0.081));
#35480=CARTESIAN_POINT('',(-0.049618820174773,0.00616219802209742,0.081));
#35481=CARTESIAN_POINT('',(-0.0439923368914681,0.00581415631573192,0.081));
#35482=CARTESIAN_POINT('',(-0.04368363807983,0.0108046177216235,0.081));
#35483=CARTESIAN_POINT('',(-0.0485373756442556,0.0120051308018039,0.081));
#35484=CARTESIAN_POINT('',(0.,0.,0.081));
#35485=CARTESIAN_POINT('',(-0.0485373756442556,-0.0120051308018038,0.081));
#35486=CARTESIAN_POINT('',(-0.04368363807983,-0.0108046177216235,0.081));
#35487=CARTESIAN_POINT('',(-0.0439923368914681,-0.00581415631573189,0.081));
#35488=CARTESIAN_POINT('',(-0.049618820174773,-0.00616219802209738,0.081));
#35489=CARTESIAN_POINT('',(0.00256146516479152,-0.04,0.071));
#35490=CARTESIAN_POINT('',(-0.043,1.7347234759768E-17,0.071));
#35491=CARTESIAN_POINT('',(-0.041603,1.7347234759768E-17,0.071));
#35492=CARTESIAN_POINT('',(-0.04,-0.0025614651647911,0.071));
#35493=CARTESIAN_POINT('',(-0.037,-0.0025614651647911,0.071));
#35494=CARTESIAN_POINT('',(-0.0398147807130172,-0.00555574200832604,0.071));
#35495=CARTESIAN_POINT('',(-0.049618820174773,-0.00616219802209738,0.071));
#35496=CARTESIAN_POINT('',(-0.0439923368914681,-0.00581415631573189,0.071));
#35497=CARTESIAN_POINT('',(-0.04368363807983,-0.0108046177216235,0.071));
#35498=CARTESIAN_POINT('',(-0.0485373756442556,-0.0120051308018038,0.071));
#35499=CARTESIAN_POINT('',(0.,0.,0.071));
#35500=CARTESIAN_POINT('',(-0.0485373756442556,0.0120051308018039,0.071));
#35501=CARTESIAN_POINT('',(-0.04368363807983,0.0108046177216235,0.071));
#35502=CARTESIAN_POINT('',(-0.0439923368914681,0.00581415631573192,0.071));
#35503=CARTESIAN_POINT('',(-0.049618820174773,0.00616219802209742,0.071));
#35504=CARTESIAN_POINT('',(-0.0398147807130172,0.00555574200832608,0.071));
#35505=CARTESIAN_POINT('',(-0.04,0.00256146516479113,0.071));
#35506=CARTESIAN_POINT('',(-0.037,0.00256146516479112,0.071));
#35507=CARTESIAN_POINT('',(-0.037,-0.00256146516479108,0.071));
#35508=CARTESIAN_POINT('',(0.00256146516479152,-0.04,0.081));
#35509=CARTESIAN_POINT('',(4.33053857950996E-16,-0.043,0.081));
#35510=CARTESIAN_POINT('',(4.18421059659904E-16,-0.041603,0.081));
#35511=CARTESIAN_POINT('',(0.00256146516479152,-0.04,0.081));
#35512=CARTESIAN_POINT('',(0.00256146516479148,-0.037,0.081));
#35513=CARTESIAN_POINT('',(0.00555574200832646,-0.0398147807130171,0.081));
#35514=CARTESIAN_POINT('',(0.00256146516479147,-0.037,0.081));
#35515=CARTESIAN_POINT('',(-0.00256146516479074,-0.037,0.081));
#35516=CARTESIAN_POINT('',(-0.00256146516479072,-0.04,0.081));
#35517=CARTESIAN_POINT('',(-0.00555574200832566,-0.0398147807130173,0.081));
#35518=CARTESIAN_POINT('',(-0.0061621980220969,-0.049618820174773,0.081));
#35519=CARTESIAN_POINT('',(-0.00581415631573146,-0.0439923368914682,0.081));
#35520=CARTESIAN_POINT('',(-0.010804617721623,-0.0436836380798302,0.081));
#35521=CARTESIAN_POINT('',(-0.0120051308018034,-0.0485373756442558,0.081));
#35522=CARTESIAN_POINT('',(0.,0.,0.081));
#35523=CARTESIAN_POINT('',(0.0120051308018043,-0.0485373756442555,0.081));
#35524=CARTESIAN_POINT('',(0.0108046177216239,-0.0436836380798299,0.081));
#35525=CARTESIAN_POINT('',(0.00581415631573235,-0.043992336891468,0.081));
#35526=CARTESIAN_POINT('',(0.0061621980220979,-0.0496188201747729,0.081));
#35527=CARTESIAN_POINT('',(-0.010804617721623,-0.0436836380798302,0.083));
#35528=CARTESIAN_POINT('',(-0.010804617721623,-0.0436836380798302,0.071));
#35529=CARTESIAN_POINT('',(-0.0120051308018034,-0.0485373756442558,0.071));
#35530=CARTESIAN_POINT('',(-0.00581415631573146,-0.0439923368914682,0.071));
#35531=CARTESIAN_POINT('',(-0.0120051308018034,-0.0485373756442558,0.083));
#35532=CARTESIAN_POINT('',(-0.00581415631573146,-0.0439923368914682,0.071));
#35533=CARTESIAN_POINT('',(0.00256146516479152,-0.04,0.071));
#35534=CARTESIAN_POINT('',(4.33053857950996E-16,-0.043,0.071));
#35535=CARTESIAN_POINT('',(4.18421059659904E-16,-0.041603,0.071));
#35536=CARTESIAN_POINT('',(0.00256146516479152,-0.04,0.071));
#35537=CARTESIAN_POINT('',(0.00256146516479148,-0.037,0.071));
#35538=CARTESIAN_POINT('',(0.00555574200832646,-0.0398147807130171,0.071));
#35539=CARTESIAN_POINT('',(0.0061621980220979,-0.0496188201747729,0.071));
#35540=CARTESIAN_POINT('',(0.00581415631573235,-0.043992336891468,0.071));
#35541=CARTESIAN_POINT('',(0.0108046177216239,-0.0436836380798299,0.071));
#35542=CARTESIAN_POINT('',(0.0120051308018043,-0.0485373756442555,0.071));
#35543=CARTESIAN_POINT('',(0.,0.,0.071));
#35544=CARTESIAN_POINT('',(-0.0061621980220969,-0.049618820174773,0.071));
#35545=CARTESIAN_POINT('',(-0.00555574200832566,-0.0398147807130173,0.071));
#35546=CARTESIAN_POINT('',(-0.00256146516479072,-0.04,0.071));
#35547=CARTESIAN_POINT('',(-0.00256146516479074,-0.037,0.071));
#35548=CARTESIAN_POINT('',(0.00256146516479147,-0.037,0.071));
#35549=CARTESIAN_POINT('',(0.0108046177216239,-0.0436836380798299,0.083));
#35550=CARTESIAN_POINT('',(0.00581415631573235,-0.043992336891468,0.071));
#35551=CARTESIAN_POINT('',(0.0120051308018043,-0.0485373756442555,0.083));
#35552=CARTESIAN_POINT('',(0.049618820174773,0.00616219802209738,0.071));
#35553=CARTESIAN_POINT('',(0.0398147807130172,0.00555574200832604,0.071));
#35554=CARTESIAN_POINT('',(0.04,0.0025614651647911,0.071));
#35555=CARTESIAN_POINT('',(0.037,0.00256146516479108,0.071));
#35556=CARTESIAN_POINT('',(0.037,0.00256146516479108,0.071));
#35557=CARTESIAN_POINT('',(0.037,-0.00256146516479111,0.071));
#35558=CARTESIAN_POINT('',(0.04,-0.00256146516479113,0.071));
#35559=CARTESIAN_POINT('',(0.0398147807130172,-0.00555574200832608,0.071));
#35560=CARTESIAN_POINT('',(0.049618820174773,-0.00616219802209742,0.071));
#35561=CARTESIAN_POINT('',(-0.00256146516479124,0.04,0.071));
#35562=CARTESIAN_POINT('',(-0.00555574200832618,0.0398147807130172,0.071));
#35563=CARTESIAN_POINT('',(-0.00256146516479121,0.037,0.071));
#35564=CARTESIAN_POINT('',(-0.00256146516479121,0.037,0.071));
#35565=CARTESIAN_POINT('',(0.00256146516479098,0.037,0.071));
#35566=CARTESIAN_POINT('',(0.00256146516479099,0.04,0.071));
#35567=CARTESIAN_POINT('',(0.00555574200832594,0.0398147807130172,0.071));
#35568=CARTESIAN_POINT('',(0.00616219802209724,0.049618820174773,0.071));
#35569=CARTESIAN_POINT('',(-0.00616219802209755,0.049618820174773,0.071));
#35570=CARTESIAN_POINT('',(-0.04,-0.0025614651647911,0.071));
#35571=CARTESIAN_POINT('',(-0.0398147807130172,-0.00555574200832604,0.071));
#35572=CARTESIAN_POINT('',(-0.037,-0.00256146516479108,0.071));
#35573=CARTESIAN_POINT('',(-0.037,-0.00256146516479108,0.071));
#35574=CARTESIAN_POINT('',(-0.037,0.00256146516479111,0.071));
#35575=CARTESIAN_POINT('',(-0.04,0.00256146516479113,0.071));
#35576=CARTESIAN_POINT('',(-0.0398147807130172,0.00555574200832608,0.071));
#35577=CARTESIAN_POINT('',(-0.049618820174773,0.00616219802209742,0.071));
#35578=CARTESIAN_POINT('',(-0.0439923368914681,0.00581415631573192,0.071));
#35579=CARTESIAN_POINT('',(-0.049618820174773,-0.00616219802209738,0.071));
#35580=CARTESIAN_POINT('',(-0.0439923368914681,-0.00581415631573189,0.071));
#35581=CARTESIAN_POINT('',(0.00256146516479152,-0.04,0.071));
#35582=CARTESIAN_POINT('',(0.00555574200832646,-0.0398147807130171,0.071));
#35583=CARTESIAN_POINT('',(0.00256146516479147,-0.037,0.071));
#35584=CARTESIAN_POINT('',(0.00256146516479147,-0.037,0.071));
#35585=CARTESIAN_POINT('',(-0.00256146516479073,-0.037,0.071));
#35586=CARTESIAN_POINT('',(-0.00256146516479072,-0.04,0.071));
#35587=CARTESIAN_POINT('',(-0.00555574200832566,-0.0398147807130173,0.071));
#35588=CARTESIAN_POINT('',(-0.0061621980220969,-0.049618820174773,0.071));
#35589=CARTESIAN_POINT('',(0.0061621980220979,-0.0496188201747729,0.071));
#35590=CARTESIAN_POINT('',(-0.043,0.,-0.043));
#35591=CARTESIAN_POINT('',(0.,0.,-0.043));
#35592=CARTESIAN_POINT('',(-0.043,0.,-0.043));
#35593=CARTESIAN_POINT('',(-0.00668810118750004,0.0303108891324553,0.0216562499979517));
#35594=CARTESIAN_POINT('',(-0.00668810118750004,0.0347893242555984,0.0217499999979516));
#35595=CARTESIAN_POINT('',(-0.00985483303217851,0.0379560561002769,0.0218437499979517));
#35596=CARTESIAN_POINT('',(-0.013021564876857,0.0411227879449553,0.0219374999979516));
#35597=CARTESIAN_POINT('',(-0.0175,0.0411227879449554,0.0220312499979517));
#35598=CARTESIAN_POINT('',(-0.0219784351231431,0.0411227879449553,0.0221249999979516));
#35599=CARTESIAN_POINT('',(-0.0251451669678216,0.0379560561002769,0.0222187499979517));
#35600=CARTESIAN_POINT('',(-0.0283118988125,0.0347893242555984,0.0223124999979516));
#35601=CARTESIAN_POINT('',(-0.0283118988125,0.0303108891324553,0.0224062499979517));
#35602=CARTESIAN_POINT('',(-0.0283118988125,0.0258324540093123,0.0224999999979516));
#35603=CARTESIAN_POINT('',(-0.0251451669678216,0.0226657221646338,0.0225937499979517));
#35604=CARTESIAN_POINT('',(-0.0219784351231431,0.0194989903199553,0.0226874999979516));
#35605=CARTESIAN_POINT('',(-0.0175,0.0194989903199553,0.0227812499979517));
#35606=CARTESIAN_POINT('',(-0.013021564876857,0.0194989903199553,0.0228749999979516));
#35607=CARTESIAN_POINT('',(-0.00985483303217851,0.0226657221646338,0.0229687499979517));
#35608=CARTESIAN_POINT('',(-0.00668810118750004,0.0258324540093123,0.0230624999979516));
#35609=CARTESIAN_POINT('',(-0.00668810118750004,0.0303108891324553,0.0231562499979516));
#35610=CARTESIAN_POINT('',(-0.00668810118750004,0.0347893242555984,0.0232499999979516));
#35611=CARTESIAN_POINT('',(-0.00985483303217851,0.0379560561002769,0.0233437499979516));
#35612=CARTESIAN_POINT('',(-0.013021564876857,0.0411227879449553,0.0234374999979516));
#35613=CARTESIAN_POINT('',(-0.0175,0.0411227879449554,0.0235312499979516));
#35614=CARTESIAN_POINT('',(-0.0219784351231431,0.0411227879449553,0.0236249999979516));
#35615=CARTESIAN_POINT('',(-0.0251451669678216,0.0379560561002769,0.0237187499979516));
#35616=CARTESIAN_POINT('',(-0.0283118988125,0.0347893242555984,0.0238124999979517));
#35617=CARTESIAN_POINT('',(-0.0283118988125,0.0303108891324553,0.0239062499979516));
#35618=CARTESIAN_POINT('',(-0.0283118988125,0.0258324540093123,0.0239999999979516));
#35619=CARTESIAN_POINT('',(-0.0251451669678216,0.0226657221646338,0.0240937499979516));
#35620=CARTESIAN_POINT('',(-0.0219784351231431,0.0194989903199553,0.0241874999979516));
#35621=CARTESIAN_POINT('',(-0.0175,0.0194989903199553,0.0242812499979516));
#35622=CARTESIAN_POINT('',(-0.013021564876857,0.0194989903199553,0.0243749999979516));
#35623=CARTESIAN_POINT('',(-0.00985483303217851,0.0226657221646338,0.0244687499979516));
#35624=CARTESIAN_POINT('',(-0.00668810118750004,0.0258324540093123,0.0245624999979516));
#35625=CARTESIAN_POINT('',(-0.00668810118750004,0.0303108891324553,0.0246562499979517));
#35626=CARTESIAN_POINT('',(-0.00668810118750004,0.0347893242555984,0.0247499999979516));
#35627=CARTESIAN_POINT('',(-0.00985483303217851,0.0379560561002769,0.0248437499979517));
#35628=CARTESIAN_POINT('',(-0.013021564876857,0.0411227879449553,0.0249374999979516));
#35629=CARTESIAN_POINT('',(-0.0175,0.0411227879449554,0.0250312499979517));
#35630=CARTESIAN_POINT('',(-0.0219784351231431,0.0411227879449553,0.0251249999979516));
#35631=CARTESIAN_POINT('',(-0.0251451669678216,0.0379560561002769,0.0252187499979517));
#35632=CARTESIAN_POINT('',(-0.0283118988125,0.0347893242555984,0.0253124999979516));
#35633=CARTESIAN_POINT('',(-0.0283118988125,0.0303108891324553,0.0254062499979517));
#35634=CARTESIAN_POINT('',(-0.0283118988125,0.0258324540093123,0.0254999999979516));
#35635=CARTESIAN_POINT('',(-0.0251451669678216,0.0226657221646338,0.0255937499979517));
#35636=CARTESIAN_POINT('',(-0.0219784351231431,0.0194989903199553,0.0256874999979516));
#35637=CARTESIAN_POINT('',(-0.0175,0.0194989903199553,0.0257812499979517));
#35638=CARTESIAN_POINT('',(-0.013021564876857,0.0194989903199553,0.0258749999979516));
#35639=CARTESIAN_POINT('',(-0.00985483303217851,0.0226657221646338,0.0259687499979517));
#35640=CARTESIAN_POINT('',(-0.00668810118750004,0.0258324540093123,0.0260624999979516));
#35641=CARTESIAN_POINT('',(-0.00668810118750004,0.0303108891324553,0.0261562499979517));
#35642=CARTESIAN_POINT('',(-0.00668810118750004,0.0347893242555984,0.0262499999979516));
#35643=CARTESIAN_POINT('',(-0.00985483303217851,0.0379560561002769,0.0263437499979517));
#35644=CARTESIAN_POINT('',(-0.013021564876857,0.0411227879449553,0.0264374999979516));
#35645=CARTESIAN_POINT('',(-0.0175,0.0411227879449554,0.0265312499979517));
#35646=CARTESIAN_POINT('',(-0.0219784351231431,0.0411227879449553,0.0266249999979516));
#35647=CARTESIAN_POINT('',(-0.0251451669678216,0.0379560561002769,0.0267187499979517));
#35648=CARTESIAN_POINT('',(-0.0283118988125,0.0347893242555984,0.0268124999979516));
#35649=CARTESIAN_POINT('',(-0.0283118988125,0.0303108891324553,0.0269062499979516));
#35650=CARTESIAN_POINT('',(-0.0283118988125,0.0258324540093123,0.0269999999979516));
#35651=CARTESIAN_POINT('',(-0.0251451669678216,0.0226657221646338,0.0270937499979516));
#35652=CARTESIAN_POINT('',(-0.0219784351231431,0.0194989903199553,0.0271874999979516));
#35653=CARTESIAN_POINT('',(-0.0175,0.0194989903199553,0.0272812499979516));
#35654=CARTESIAN_POINT('',(-0.013021564876857,0.0194989903199553,0.0273749999979517));
#35655=CARTESIAN_POINT('',(-0.00985483303217851,0.0226657221646338,0.0274687499979516));
#35656=CARTESIAN_POINT('',(-0.00668810118750004,0.0258324540093123,0.0275624999979516));
#35657=CARTESIAN_POINT('',(-0.00668810118750004,0.0303108891324553,0.0276562499979516));
#35658=CARTESIAN_POINT('',(-0.0075,0.0303108891324553,0.0221249999959033));
#35659=CARTESIAN_POINT('',(-0.00750000000000004,0.0344530247561863,0.0222187499959032));
#35660=CARTESIAN_POINT('',(-0.0104289321881346,0.0373819569443208,0.0223124999959033));
#35661=CARTESIAN_POINT('',(-0.0133578643762691,0.0403108891324553,0.0224062499959032));
#35662=CARTESIAN_POINT('',(-0.0175,0.0403108891324553,0.0224999999959033));
#35663=CARTESIAN_POINT('',(-0.021642135623731,0.0403108891324553,0.0225937499959032));
#35664=CARTESIAN_POINT('',(-0.0245710678118655,0.0373819569443208,0.0226874999959033));
#35665=CARTESIAN_POINT('',(-0.0275000000000001,0.0344530247561863,0.0227812499959032));
#35666=CARTESIAN_POINT('',(-0.0275,0.0303108891324553,0.0228749999959033));
#35667=CARTESIAN_POINT('',(-0.0275000000000001,0.0261687535087244,0.0229687499959032));
#35668=CARTESIAN_POINT('',(-0.0245710678118655,0.0232398213205899,0.0230624999959032));
#35669=CARTESIAN_POINT('',(-0.021642135623731,0.0203108891324553,0.0231562499959032));
#35670=CARTESIAN_POINT('',(-0.0175,0.0203108891324553,0.0232499999959032));
#35671=CARTESIAN_POINT('',(-0.0133578643762691,0.0203108891324553,0.0233437499959032));
#35672=CARTESIAN_POINT('',(-0.0104289321881346,0.0232398213205899,0.0234374999959032));
#35673=CARTESIAN_POINT('',(-0.00750000000000004,0.0261687535087243,0.0235312499959032));
#35674=CARTESIAN_POINT('',(-0.0075,0.0303108891324553,0.0236249999959032));
#35675=CARTESIAN_POINT('',(-0.00750000000000004,0.0344530247561863,0.0237187499959032));
#35676=CARTESIAN_POINT('',(-0.0104289321881346,0.0373819569443208,0.0238124999959032));
#35677=CARTESIAN_POINT('',(-0.0133578643762691,0.0403108891324553,0.0239062499959032));
#35678=CARTESIAN_POINT('',(-0.0175,0.0403108891324553,0.0239999999959032));
#35679=CARTESIAN_POINT('',(-0.021642135623731,0.0403108891324553,0.0240937499959032));
#35680=CARTESIAN_POINT('',(-0.0245710678118655,0.0373819569443208,0.0241874999959032));
#35681=CARTESIAN_POINT('',(-0.0275000000000001,0.0344530247561863,0.0242812499959032));
#35682=CARTESIAN_POINT('',(-0.0275,0.0303108891324553,0.0243749999959033));
#35683=CARTESIAN_POINT('',(-0.0275000000000001,0.0261687535087244,0.0244687499959033));
#35684=CARTESIAN_POINT('',(-0.0245710678118655,0.0232398213205899,0.0245624999959033));
#35685=CARTESIAN_POINT('',(-0.021642135623731,0.0203108891324553,0.0246562499959032));
#35686=CARTESIAN_POINT('',(-0.0175,0.0203108891324553,0.0247499999959033));
#35687=CARTESIAN_POINT('',(-0.0133578643762691,0.0203108891324553,0.0248437499959032));
#35688=CARTESIAN_POINT('',(-0.0104289321881346,0.0232398213205899,0.0249374999959033));
#35689=CARTESIAN_POINT('',(-0.00750000000000004,0.0261687535087243,0.0250312499959033));
#35690=CARTESIAN_POINT('',(-0.0075,0.0303108891324553,0.0251249999959033));
#35691=CARTESIAN_POINT('',(-0.00750000000000004,0.0344530247561863,0.0252187499959032));
#35692=CARTESIAN_POINT('',(-0.0104289321881346,0.0373819569443208,0.0253124999959033));
#35693=CARTESIAN_POINT('',(-0.0133578643762691,0.0403108891324553,0.0254062499959032));
#35694=CARTESIAN_POINT('',(-0.0175,0.0403108891324553,0.0254999999959033));
#35695=CARTESIAN_POINT('',(-0.021642135623731,0.0403108891324553,0.0255937499959033));
#35696=CARTESIAN_POINT('',(-0.0245710678118655,0.0373819569443208,0.0256874999959033));
#35697=CARTESIAN_POINT('',(-0.0275000000000001,0.0344530247561863,0.0257812499959032));
#35698=CARTESIAN_POINT('',(-0.0275,0.0303108891324553,0.0258749999959033));
#35699=CARTESIAN_POINT('',(-0.0275000000000001,0.0261687535087244,0.0259687499959032));
#35700=CARTESIAN_POINT('',(-0.0245710678118655,0.0232398213205899,0.0260624999959033));
#35701=CARTESIAN_POINT('',(-0.021642135623731,0.0203108891324553,0.0261562499959033));
#35702=CARTESIAN_POINT('',(-0.0175,0.0203108891324553,0.0262499999959033));
#35703=CARTESIAN_POINT('',(-0.0133578643762691,0.0203108891324553,0.0263437499959032));
#35704=CARTESIAN_POINT('',(-0.0104289321881346,0.0232398213205899,0.0264374999959033));
#35705=CARTESIAN_POINT('',(-0.00750000000000004,0.0261687535087243,0.0265312499959032));
#35706=CARTESIAN_POINT('',(-0.0075,0.0303108891324553,0.0266249999959033));
#35707=CARTESIAN_POINT('',(-0.00750000000000004,0.0344530247561863,0.0267187499959033));
#35708=CARTESIAN_POINT('',(-0.0104289321881346,0.0373819569443208,0.0268124999959033));
#35709=CARTESIAN_POINT('',(-0.0133578643762691,0.0403108891324553,0.0269062499959032));
#35710=CARTESIAN_POINT('',(-0.0175,0.0403108891324553,0.0269999999959032));
#35711=CARTESIAN_POINT('',(-0.021642135623731,0.0403108891324553,0.0270937499959032));
#35712=CARTESIAN_POINT('',(-0.0245710678118655,0.0373819569443208,0.0271874999959032));
#35713=CARTESIAN_POINT('',(-0.0275000000000001,0.0344530247561863,0.0272812499959033));
#35714=CARTESIAN_POINT('',(-0.0275,0.0303108891324553,0.0273749999959032));
#35715=CARTESIAN_POINT('',(-0.0275000000000001,0.0261687535087244,0.0274687499959032));
#35716=CARTESIAN_POINT('',(-0.0245710678118655,0.0232398213205899,0.0275624999959032));
#35717=CARTESIAN_POINT('',(-0.021642135623731,0.0203108891324553,0.0276562499959032));
#35718=CARTESIAN_POINT('',(-0.0175,0.0203108891324553,0.0277499999959032));
#35719=CARTESIAN_POINT('',(-0.0133578643762691,0.0203108891324553,0.0278437499959033));
#35720=CARTESIAN_POINT('',(-0.0104289321881346,0.0232398213205899,0.0279374999959032));
#35721=CARTESIAN_POINT('',(-0.00750000000000004,0.0261687535087243,0.0280312499959032));
#35722=CARTESIAN_POINT('',(-0.0075,0.0303108891324553,0.0281249999959032));
#35723=CARTESIAN_POINT('',(-0.00709405059375004,0.0303108891324553,0.0218906249969274));
#35724=CARTESIAN_POINT('',(-0.00668810118750004,0.0303108891324553,0.0216562499979517));
#35725=CARTESIAN_POINT('',(-0.0075,0.0303108891324553,0.0221249999959033));
#35726=CARTESIAN_POINT('',(-0.0075,0.0303108891324553,0.0221249999959033));
#35727=CARTESIAN_POINT('',(-0.00750000000000004,0.0344530247561863,0.0222187499959032));
#35728=CARTESIAN_POINT('',(-0.0104289321881346,0.0373819569443208,0.0223124999959033));
#35729=CARTESIAN_POINT('',(-0.0133578643762691,0.0403108891324553,0.0224062499959032));
#35730=CARTESIAN_POINT('',(-0.0175,0.0403108891324553,0.0224999999959033));
#35731=CARTESIAN_POINT('',(-0.021642135623731,0.0403108891324553,0.0225937499959032));
#35732=CARTESIAN_POINT('',(-0.0245710678118655,0.0373819569443208,0.0226874999959033));
#35733=CARTESIAN_POINT('',(-0.0275000000000001,0.0344530247561862,0.0227812499959032));
#35734=CARTESIAN_POINT('',(-0.0275,0.0303108891324553,0.0228749999959033));
#35735=CARTESIAN_POINT('',(-0.0275,0.0303108891324553,0.0228749999959033));
#35736=CARTESIAN_POINT('',(-0.0275,0.0303108891324553,0.0228749999959033));
#35737=CARTESIAN_POINT('',(-0.0275000000000001,0.0261687535087244,0.0229687499959032));
#35738=CARTESIAN_POINT('',(-0.0245710678118655,0.0232398213205899,0.0230624999959032));
#35739=CARTESIAN_POINT('',(-0.021642135623731,0.0203108891324553,0.0231562499959032));
#35740=CARTESIAN_POINT('',(-0.0175,0.0203108891324553,0.0232499999959032));
#35741=CARTESIAN_POINT('',(-0.0133578643762691,0.0203108891324553,0.0233437499959032));
#35742=CARTESIAN_POINT('',(-0.0104289321881346,0.0232398213205899,0.0234374999959032));
#35743=CARTESIAN_POINT('',(-0.00750000000000003,0.0261687535087244,0.0235312499959033));
#35744=CARTESIAN_POINT('',(-0.0075,0.0303108891324553,0.0236249999959032));
#35745=CARTESIAN_POINT('',(-0.0075,0.0303108891324553,0.0236249999959032));
#35746=CARTESIAN_POINT('',(-0.0075,0.0303108891324553,0.0236249999959032));
#35747=CARTESIAN_POINT('',(-0.00750000000000005,0.0344530247561863,0.0237187499959033));
#35748=CARTESIAN_POINT('',(-0.0104289321881346,0.0373819569443208,0.0238124999959032));
#35749=CARTESIAN_POINT('',(-0.0133578643762691,0.0403108891324553,0.0239062499959032));
#35750=CARTESIAN_POINT('',(-0.0175,0.0403108891324553,0.0239999999959032));
#35751=CARTESIAN_POINT('',(-0.021642135623731,0.0403108891324553,0.0240937499959032));
#35752=CARTESIAN_POINT('',(-0.0245710678118655,0.0373819569443208,0.0241874999959032));
#35753=CARTESIAN_POINT('',(-0.0275,0.0344530247561863,0.0242812499959032));
#35754=CARTESIAN_POINT('',(-0.0275,0.0303108891324553,0.0243749999959032));
#35755=CARTESIAN_POINT('',(-0.0275,0.0303108891324553,0.0243749999959033));
#35756=CARTESIAN_POINT('',(-0.0275,0.0303108891324553,0.0243749999959033));
#35757=CARTESIAN_POINT('',(-0.0275000000000001,0.0261687535087244,0.0244687499959032));
#35758=CARTESIAN_POINT('',(-0.0245710678118655,0.0232398213205899,0.0245624999959033));
#35759=CARTESIAN_POINT('',(-0.021642135623731,0.0203108891324553,0.0246562499959032));
#35760=CARTESIAN_POINT('',(-0.0175,0.0203108891324553,0.0247499999959033));
#35761=CARTESIAN_POINT('',(-0.0133578643762691,0.0203108891324553,0.0248437499959032));
#35762=CARTESIAN_POINT('',(-0.0104289321881346,0.0232398213205899,0.0249374999959033));
#35763=CARTESIAN_POINT('',(-0.00750000000000006,0.0261687535087243,0.0250312499959033));
#35764=CARTESIAN_POINT('',(-0.0075,0.0303108891324553,0.0251249999959033));
#35765=CARTESIAN_POINT('',(-0.0075,0.0303108891324553,0.0251249999959033));
#35766=CARTESIAN_POINT('',(-0.0075,0.0303108891324553,0.0251249999959033));
#35767=CARTESIAN_POINT('',(-0.00750000000000002,0.0344530247561863,0.0252187499959033));
#35768=CARTESIAN_POINT('',(-0.0104289321881346,0.0373819569443208,0.0253124999959033));
#35769=CARTESIAN_POINT('',(-0.0133578643762691,0.0403108891324553,0.0254062499959032));
#35770=CARTESIAN_POINT('',(-0.0175,0.0403108891324553,0.0254999999959033));
#35771=CARTESIAN_POINT('',(-0.021642135623731,0.0403108891324553,0.0255937499959033));
#35772=CARTESIAN_POINT('',(-0.0245710678118655,0.0373819569443208,0.0256874999959033));
#35773=CARTESIAN_POINT('',(-0.0275000000000001,0.0344530247561863,0.0257812499959032));
#35774=CARTESIAN_POINT('',(-0.0275,0.0303108891324553,0.0258749999959033));
#35775=CARTESIAN_POINT('',(-0.0275,0.0303108891324553,0.0258749999959033));
#35776=CARTESIAN_POINT('',(-0.0275,0.0303108891324553,0.0258749999959033));
#35777=CARTESIAN_POINT('',(-0.0275000000000001,0.0261687535087244,0.0259687499959032));
#35778=CARTESIAN_POINT('',(-0.0245710678118655,0.0232398213205899,0.0260624999959033));
#35779=CARTESIAN_POINT('',(-0.021642135623731,0.0203108891324553,0.0261562499959033));
#35780=CARTESIAN_POINT('',(-0.0175,0.0203108891324553,0.0262499999959033));
#35781=CARTESIAN_POINT('',(-0.0133578643762691,0.0203108891324553,0.0263437499959032));
#35782=CARTESIAN_POINT('',(-0.0104289321881346,0.0232398213205899,0.0264374999959033));
#35783=CARTESIAN_POINT('',(-0.00750000000000004,0.0261687535087243,0.0265312499959032));
#35784=CARTESIAN_POINT('',(-0.0075,0.0303108891324553,0.0266249999959033));
#35785=CARTESIAN_POINT('',(-0.0075,0.0303108891324553,0.0266249999959033));
#35786=CARTESIAN_POINT('',(-0.0075,0.0303108891324553,0.0266249999959033));
#35787=CARTESIAN_POINT('',(-0.00750000000000004,0.0344530247561863,0.0267187499959033));
#35788=CARTESIAN_POINT('',(-0.0104289321881346,0.0373819569443208,0.0268124999959033));
#35789=CARTESIAN_POINT('',(-0.0133578643762691,0.0403108891324553,0.0269062499959032));
#35790=CARTESIAN_POINT('',(-0.0175,0.0403108891324553,0.0269999999959032));
#35791=CARTESIAN_POINT('',(-0.021642135623731,0.0403108891324553,0.0270937499959032));
#35792=CARTESIAN_POINT('',(-0.0245710678118655,0.0373819569443208,0.0271874999959032));
#35793=CARTESIAN_POINT('',(-0.0275000000000001,0.0344530247561863,0.0272812499959033));
#35794=CARTESIAN_POINT('',(-0.0275,0.0303108891324553,0.0273749999959032));
#35795=CARTESIAN_POINT('',(-0.0275,0.0303108891324553,0.0273749999959032));
#35796=CARTESIAN_POINT('',(-0.0275,0.0303108891324553,0.0273749999959032));
#35797=CARTESIAN_POINT('',(-0.0275000000000001,0.0261687535087244,0.0274687499959032));
#35798=CARTESIAN_POINT('',(-0.0245710678118655,0.0232398213205899,0.0275624999959032));
#35799=CARTESIAN_POINT('',(-0.021642135623731,0.0203108891324553,0.0276562499959032));
#35800=CARTESIAN_POINT('',(-0.0175,0.0203108891324553,0.0277499999959032));
#35801=CARTESIAN_POINT('',(-0.0133578643762691,0.0203108891324553,0.0278437499959033));
#35802=CARTESIAN_POINT('',(-0.0104289321881346,0.0232398213205899,0.0279374999959032));
#35803=CARTESIAN_POINT('',(-0.00750000000000004,0.0261687535087243,0.0280312499959032));
#35804=CARTESIAN_POINT('',(-0.0075,0.0303108891324553,0.0281249999959032));
#35805=CARTESIAN_POINT('',(-0.0075,0.0303108891324553,0.0281249999959032));
#35806=CARTESIAN_POINT('',(-0.00709405059375004,0.0303108891324553,0.0278906249969274));
#35807=CARTESIAN_POINT('',(-0.00668810118750004,0.0303108891324553,0.0276562499979516));
#35808=CARTESIAN_POINT('',(-0.00668810118750004,0.0303108891324553,0.0216562499979517));
#35809=CARTESIAN_POINT('',(-0.00668810118750004,0.0347893242555984,0.0217499999979516));
#35810=CARTESIAN_POINT('',(-0.00985483303217851,0.0379560561002769,0.0218437499979517));
#35811=CARTESIAN_POINT('',(-0.013021564876857,0.0411227879449553,0.0219374999979516));
#35812=CARTESIAN_POINT('',(-0.0175,0.0411227879449554,0.0220312499979517));
#35813=CARTESIAN_POINT('',(-0.0219784351231431,0.0411227879449553,0.0221249999979516));
#35814=CARTESIAN_POINT('',(-0.0251451669678216,0.0379560561002769,0.0222187499979517));
#35815=CARTESIAN_POINT('',(-0.0283118988125,0.0347893242555984,0.0223124999979516));
#35816=CARTESIAN_POINT('',(-0.0283118988125,0.0303108891324553,0.0224062499979517));
#35817=CARTESIAN_POINT('',(-0.0283118988125,0.0258324540093123,0.0224999999979516));
#35818=CARTESIAN_POINT('',(-0.0251451669678216,0.0226657221646338,0.0225937499979517));
#35819=CARTESIAN_POINT('',(-0.0219784351231431,0.0194989903199553,0.0226874999979516));
#35820=CARTESIAN_POINT('',(-0.0175,0.0194989903199553,0.0227812499979517));
#35821=CARTESIAN_POINT('',(-0.013021564876857,0.0194989903199553,0.0228749999979516));
#35822=CARTESIAN_POINT('',(-0.00985483303217851,0.0226657221646338,0.0229687499979517));
#35823=CARTESIAN_POINT('',(-0.00668810118750004,0.0258324540093123,0.0230624999979516));
#35824=CARTESIAN_POINT('',(-0.00668810118750004,0.0303108891324553,0.0231562499979516));
#35825=CARTESIAN_POINT('',(-0.00668810118750004,0.0347893242555984,0.0232499999979516));
#35826=CARTESIAN_POINT('',(-0.00985483303217851,0.0379560561002769,0.0233437499979516));
#35827=CARTESIAN_POINT('',(-0.013021564876857,0.0411227879449553,0.0234374999979516));
#35828=CARTESIAN_POINT('',(-0.0175,0.0411227879449554,0.0235312499979516));
#35829=CARTESIAN_POINT('',(-0.0219784351231431,0.0411227879449553,0.0236249999979516));
#35830=CARTESIAN_POINT('',(-0.0251451669678216,0.0379560561002769,0.0237187499979516));
#35831=CARTESIAN_POINT('',(-0.0283118988125,0.0347893242555984,0.0238124999979517));
#35832=CARTESIAN_POINT('',(-0.0283118988125,0.0303108891324553,0.0239062499979516));
#35833=CARTESIAN_POINT('',(-0.0283118988125,0.0258324540093123,0.0239999999979516));
#35834=CARTESIAN_POINT('',(-0.0251451669678216,0.0226657221646338,0.0240937499979516));
#35835=CARTESIAN_POINT('',(-0.0219784351231431,0.0194989903199553,0.0241874999979516));
#35836=CARTESIAN_POINT('',(-0.0175,0.0194989903199553,0.0242812499979516));
#35837=CARTESIAN_POINT('',(-0.013021564876857,0.0194989903199553,0.0243749999979516));
#35838=CARTESIAN_POINT('',(-0.00985483303217851,0.0226657221646338,0.0244687499979516));
#35839=CARTESIAN_POINT('',(-0.00668810118750004,0.0258324540093123,0.0245624999979516));
#35840=CARTESIAN_POINT('',(-0.00668810118750004,0.0303108891324553,0.0246562499979517));
#35841=CARTESIAN_POINT('',(-0.00668810118750004,0.0347893242555984,0.0247499999979516));
#35842=CARTESIAN_POINT('',(-0.00985483303217851,0.0379560561002769,0.0248437499979517));
#35843=CARTESIAN_POINT('',(-0.013021564876857,0.0411227879449553,0.0249374999979516));
#35844=CARTESIAN_POINT('',(-0.0175,0.0411227879449554,0.0250312499979517));
#35845=CARTESIAN_POINT('',(-0.0219784351231431,0.0411227879449553,0.0251249999979516));
#35846=CARTESIAN_POINT('',(-0.0251451669678216,0.0379560561002769,0.0252187499979517));
#35847=CARTESIAN_POINT('',(-0.0283118988125,0.0347893242555984,0.0253124999979516));
#35848=CARTESIAN_POINT('',(-0.0283118988125,0.0303108891324553,0.0254062499979517));
#35849=CARTESIAN_POINT('',(-0.0283118988125,0.0258324540093123,0.0254999999979516));
#35850=CARTESIAN_POINT('',(-0.0251451669678216,0.0226657221646338,0.0255937499979517));
#35851=CARTESIAN_POINT('',(-0.0219784351231431,0.0194989903199553,0.0256874999979516));
#35852=CARTESIAN_POINT('',(-0.0175,0.0194989903199553,0.0257812499979517));
#35853=CARTESIAN_POINT('',(-0.013021564876857,0.0194989903199553,0.0258749999979516));
#35854=CARTESIAN_POINT('',(-0.00985483303217851,0.0226657221646338,0.0259687499979517));
#35855=CARTESIAN_POINT('',(-0.00668810118750004,0.0258324540093123,0.0260624999979516));
#35856=CARTESIAN_POINT('',(-0.00668810118750004,0.0303108891324553,0.0261562499979517));
#35857=CARTESIAN_POINT('',(-0.00668810118750004,0.0347893242555984,0.0262499999979516));
#35858=CARTESIAN_POINT('',(-0.00985483303217851,0.0379560561002769,0.0263437499979517));
#35859=CARTESIAN_POINT('',(-0.013021564876857,0.0411227879449553,0.0264374999979516));
#35860=CARTESIAN_POINT('',(-0.0175,0.0411227879449554,0.0265312499979517));
#35861=CARTESIAN_POINT('',(-0.0219784351231431,0.0411227879449553,0.0266249999979516));
#35862=CARTESIAN_POINT('',(-0.0251451669678216,0.0379560561002769,0.0267187499979517));
#35863=CARTESIAN_POINT('',(-0.0283118988125,0.0347893242555984,0.0268124999979516));
#35864=CARTESIAN_POINT('',(-0.0283118988125,0.0303108891324553,0.0269062499979516));
#35865=CARTESIAN_POINT('',(-0.0283118988125,0.0258324540093123,0.0269999999979516));
#35866=CARTESIAN_POINT('',(-0.0251451669678216,0.0226657221646338,0.0270937499979516));
#35867=CARTESIAN_POINT('',(-0.0219784351231431,0.0194989903199553,0.0271874999979516));
#35868=CARTESIAN_POINT('',(-0.0175,0.0194989903199553,0.0272812499979516));
#35869=CARTESIAN_POINT('',(-0.013021564876857,0.0194989903199553,0.0273749999979517));
#35870=CARTESIAN_POINT('',(-0.00985483303217851,0.0226657221646338,0.0274687499979516));
#35871=CARTESIAN_POINT('',(-0.00668810118750004,0.0258324540093123,0.0275624999979516));
#35872=CARTESIAN_POINT('',(-0.00668810118750004,0.0303108891324553,0.0276562499979516));
#35873=CARTESIAN_POINT('',(-0.0075,0.0303108891324553,0.021));
#35874=CARTESIAN_POINT('',(-0.00750000000000004,0.0344530247561863,0.02109375));
#35875=CARTESIAN_POINT('',(-0.0104289321881346,0.0373819569443208,0.0211875));
#35876=CARTESIAN_POINT('',(-0.0133578643762691,0.0403108891324553,0.02128125));
#35877=CARTESIAN_POINT('',(-0.0175,0.0403108891324553,0.021375));
#35878=CARTESIAN_POINT('',(-0.021642135623731,0.0403108891324553,0.02146875));
#35879=CARTESIAN_POINT('',(-0.0245710678118655,0.0373819569443208,0.0215625));
#35880=CARTESIAN_POINT('',(-0.0275000000000001,0.0344530247561863,0.02165625));
#35881=CARTESIAN_POINT('',(-0.0275,0.0303108891324553,0.02175));
#35882=CARTESIAN_POINT('',(-0.0275000000000001,0.0261687535087244,0.02184375));
#35883=CARTESIAN_POINT('',(-0.0245710678118655,0.0232398213205899,0.0219375));
#35884=CARTESIAN_POINT('',(-0.021642135623731,0.0203108891324553,0.02203125));
#35885=CARTESIAN_POINT('',(-0.0175,0.0203108891324553,0.022125));
#35886=CARTESIAN_POINT('',(-0.0133578643762691,0.0203108891324553,0.02221875));
#35887=CARTESIAN_POINT('',(-0.0104289321881346,0.0232398213205899,0.0223125));
#35888=CARTESIAN_POINT('',(-0.00750000000000004,0.0261687535087243,0.02240625));
#35889=CARTESIAN_POINT('',(-0.0075,0.0303108891324553,0.0225));
#35890=CARTESIAN_POINT('',(-0.00750000000000004,0.0344530247561863,0.02259375));
#35891=CARTESIAN_POINT('',(-0.0104289321881346,0.0373819569443208,0.0226875));
#35892=CARTESIAN_POINT('',(-0.0133578643762691,0.0403108891324553,0.02278125));
#35893=CARTESIAN_POINT('',(-0.0175,0.0403108891324553,0.022875));
#35894=CARTESIAN_POINT('',(-0.021642135623731,0.0403108891324553,0.02296875));
#35895=CARTESIAN_POINT('',(-0.0245710678118655,0.0373819569443208,0.0230625));
#35896=CARTESIAN_POINT('',(-0.0275000000000001,0.0344530247561863,0.02315625));
#35897=CARTESIAN_POINT('',(-0.0275,0.0303108891324553,0.02325));
#35898=CARTESIAN_POINT('',(-0.0275000000000001,0.0261687535087244,0.02334375));
#35899=CARTESIAN_POINT('',(-0.0245710678118655,0.0232398213205899,0.0234375));
#35900=CARTESIAN_POINT('',(-0.021642135623731,0.0203108891324553,0.02353125));
#35901=CARTESIAN_POINT('',(-0.0175,0.0203108891324553,0.023625));
#35902=CARTESIAN_POINT('',(-0.0133578643762691,0.0203108891324553,0.02371875));
#35903=CARTESIAN_POINT('',(-0.0104289321881346,0.0232398213205899,0.0238125));
#35904=CARTESIAN_POINT('',(-0.00750000000000004,0.0261687535087243,0.02390625));
#35905=CARTESIAN_POINT('',(-0.0075,0.0303108891324553,0.024));
#35906=CARTESIAN_POINT('',(-0.00750000000000004,0.0344530247561863,0.02409375));
#35907=CARTESIAN_POINT('',(-0.0104289321881346,0.0373819569443208,0.0241875));
#35908=CARTESIAN_POINT('',(-0.0133578643762691,0.0403108891324553,0.02428125));
#35909=CARTESIAN_POINT('',(-0.0175,0.0403108891324553,0.024375));
#35910=CARTESIAN_POINT('',(-0.021642135623731,0.0403108891324553,0.02446875));
#35911=CARTESIAN_POINT('',(-0.0245710678118655,0.0373819569443208,0.0245625));
#35912=CARTESIAN_POINT('',(-0.0275000000000001,0.0344530247561863,0.02465625));
#35913=CARTESIAN_POINT('',(-0.0275,0.0303108891324553,0.02475));
#35914=CARTESIAN_POINT('',(-0.0275000000000001,0.0261687535087244,0.02484375));
#35915=CARTESIAN_POINT('',(-0.0245710678118655,0.0232398213205899,0.0249375));
#35916=CARTESIAN_POINT('',(-0.021642135623731,0.0203108891324553,0.02503125));
#35917=CARTESIAN_POINT('',(-0.0175,0.0203108891324553,0.025125));
#35918=CARTESIAN_POINT('',(-0.0133578643762691,0.0203108891324553,0.02521875));
#35919=CARTESIAN_POINT('',(-0.0104289321881346,0.0232398213205899,0.0253125));
#35920=CARTESIAN_POINT('',(-0.00750000000000004,0.0261687535087243,0.02540625));
#35921=CARTESIAN_POINT('',(-0.0075,0.0303108891324553,0.0255));
#35922=CARTESIAN_POINT('',(-0.00750000000000004,0.0344530247561863,0.02559375));
#35923=CARTESIAN_POINT('',(-0.0104289321881346,0.0373819569443208,0.0256875));
#35924=CARTESIAN_POINT('',(-0.0133578643762691,0.0403108891324553,0.02578125));
#35925=CARTESIAN_POINT('',(-0.0175,0.0403108891324553,0.025875));
#35926=CARTESIAN_POINT('',(-0.021642135623731,0.0403108891324553,0.02596875));
#35927=CARTESIAN_POINT('',(-0.0245710678118655,0.0373819569443208,0.0260625));
#35928=CARTESIAN_POINT('',(-0.0275000000000001,0.0344530247561863,0.02615625));
#35929=CARTESIAN_POINT('',(-0.0275,0.0303108891324553,0.02625));
#35930=CARTESIAN_POINT('',(-0.0275000000000001,0.0261687535087244,0.02634375));
#35931=CARTESIAN_POINT('',(-0.0245710678118655,0.0232398213205899,0.0264375));
#35932=CARTESIAN_POINT('',(-0.021642135623731,0.0203108891324553,0.02653125));
#35933=CARTESIAN_POINT('',(-0.0175,0.0203108891324553,0.026625));
#35934=CARTESIAN_POINT('',(-0.0133578643762691,0.0203108891324553,0.02671875));
#35935=CARTESIAN_POINT('',(-0.0104289321881346,0.0232398213205899,0.0268125));
#35936=CARTESIAN_POINT('',(-0.00750000000000004,0.0261687535087243,0.02690625));
#35937=CARTESIAN_POINT('',(-0.0075,0.0303108891324553,0.027));
#35938=CARTESIAN_POINT('',(-0.00668810118750004,0.0303108891324553,0.0214687499979517));
#35939=CARTESIAN_POINT('',(-0.00668810118750004,0.0347893242555984,0.0215624999979517));
#35940=CARTESIAN_POINT('',(-0.00985483303217851,0.0379560561002769,0.0216562499979517));
#35941=CARTESIAN_POINT('',(-0.013021564876857,0.0411227879449553,0.0217499999979516));
#35942=CARTESIAN_POINT('',(-0.0175,0.0411227879449554,0.0218437499979517));
#35943=CARTESIAN_POINT('',(-0.0219784351231431,0.0411227879449553,0.0219374999979516));
#35944=CARTESIAN_POINT('',(-0.0251451669678216,0.0379560561002769,0.0220312499979517));
#35945=CARTESIAN_POINT('',(-0.0283118988125,0.0347893242555984,0.0221249999979516));
#35946=CARTESIAN_POINT('',(-0.0283118988125,0.0303108891324553,0.0222187499979517));
#35947=CARTESIAN_POINT('',(-0.0283118988125,0.0258324540093123,0.0223124999979516));
#35948=CARTESIAN_POINT('',(-0.0251451669678216,0.0226657221646338,0.0224062499979517));
#35949=CARTESIAN_POINT('',(-0.0219784351231431,0.0194989903199553,0.0224999999979516));
#35950=CARTESIAN_POINT('',(-0.0175,0.0194989903199553,0.0225937499979517));
#35951=CARTESIAN_POINT('',(-0.013021564876857,0.0194989903199553,0.0226874999979516));
#35952=CARTESIAN_POINT('',(-0.00985483303217851,0.0226657221646338,0.0227812499979517));
#35953=CARTESIAN_POINT('',(-0.00668810118750004,0.0258324540093123,0.0228749999979516));
#35954=CARTESIAN_POINT('',(-0.00668810118750004,0.0303108891324553,0.0229687499979517));
#35955=CARTESIAN_POINT('',(-0.00668810118750004,0.0347893242555984,0.0230624999979516));
#35956=CARTESIAN_POINT('',(-0.00985483303217851,0.0379560561002769,0.0231562499979516));
#35957=CARTESIAN_POINT('',(-0.013021564876857,0.0411227879449553,0.0232499999979516));
#35958=CARTESIAN_POINT('',(-0.0175,0.0411227879449554,0.0233437499979516));
#35959=CARTESIAN_POINT('',(-0.0219784351231431,0.0411227879449553,0.0234374999979516));
#35960=CARTESIAN_POINT('',(-0.0251451669678216,0.0379560561002769,0.0235312499979516));
#35961=CARTESIAN_POINT('',(-0.0283118988125,0.0347893242555984,0.0236249999979516));
#35962=CARTESIAN_POINT('',(-0.0283118988125,0.0303108891324553,0.0237187499979516));
#35963=CARTESIAN_POINT('',(-0.0283118988125,0.0258324540093123,0.0238124999979517));
#35964=CARTESIAN_POINT('',(-0.0251451669678216,0.0226657221646338,0.0239062499979516));
#35965=CARTESIAN_POINT('',(-0.0219784351231431,0.0194989903199553,0.0239999999979516));
#35966=CARTESIAN_POINT('',(-0.0175,0.0194989903199553,0.0240937499979516));
#35967=CARTESIAN_POINT('',(-0.013021564876857,0.0194989903199553,0.0241874999979516));
#35968=CARTESIAN_POINT('',(-0.00985483303217851,0.0226657221646338,0.0242812499979516));
#35969=CARTESIAN_POINT('',(-0.00668810118750004,0.0258324540093123,0.0243749999979516));
#35970=CARTESIAN_POINT('',(-0.00668810118750004,0.0303108891324553,0.0244687499979516));
#35971=CARTESIAN_POINT('',(-0.00668810118750004,0.0347893242555984,0.0245624999979516));
#35972=CARTESIAN_POINT('',(-0.00985483303217851,0.0379560561002769,0.0246562499979517));
#35973=CARTESIAN_POINT('',(-0.013021564876857,0.0411227879449553,0.0247499999979516));
#35974=CARTESIAN_POINT('',(-0.0175,0.0411227879449554,0.0248437499979517));
#35975=CARTESIAN_POINT('',(-0.0219784351231431,0.0411227879449553,0.0249374999979516));
#35976=CARTESIAN_POINT('',(-0.0251451669678216,0.0379560561002769,0.0250312499979517));
#35977=CARTESIAN_POINT('',(-0.0283118988125,0.0347893242555984,0.0251249999979516));
#35978=CARTESIAN_POINT('',(-0.0283118988125,0.0303108891324553,0.0252187499979517));
#35979=CARTESIAN_POINT('',(-0.0283118988125,0.0258324540093123,0.0253124999979516));
#35980=CARTESIAN_POINT('',(-0.0251451669678216,0.0226657221646338,0.0254062499979517));
#35981=CARTESIAN_POINT('',(-0.0219784351231431,0.0194989903199553,0.0254999999979516));
#35982=CARTESIAN_POINT('',(-0.0175,0.0194989903199553,0.0255937499979517));
#35983=CARTESIAN_POINT('',(-0.013021564876857,0.0194989903199553,0.0256874999979516));
#35984=CARTESIAN_POINT('',(-0.00985483303217851,0.0226657221646338,0.0257812499979517));
#35985=CARTESIAN_POINT('',(-0.00668810118750004,0.0258324540093123,0.0258749999979516));
#35986=CARTESIAN_POINT('',(-0.00668810118750004,0.0303108891324553,0.0259687499979517));
#35987=CARTESIAN_POINT('',(-0.00668810118750004,0.0347893242555984,0.0260624999979516));
#35988=CARTESIAN_POINT('',(-0.00985483303217851,0.0379560561002769,0.0261562499979517));
#35989=CARTESIAN_POINT('',(-0.013021564876857,0.0411227879449553,0.0262499999979516));
#35990=CARTESIAN_POINT('',(-0.0175,0.0411227879449554,0.0263437499979517));
#35991=CARTESIAN_POINT('',(-0.0219784351231431,0.0411227879449553,0.0264374999979516));
#35992=CARTESIAN_POINT('',(-0.0251451669678216,0.0379560561002769,0.0265312499979517));
#35993=CARTESIAN_POINT('',(-0.0283118988125,0.0347893242555984,0.0266249999979516));
#35994=CARTESIAN_POINT('',(-0.0283118988125,0.0303108891324553,0.0267187499979517));
#35995=CARTESIAN_POINT('',(-0.0283118988125,0.0258324540093123,0.0268124999979516));
#35996=CARTESIAN_POINT('',(-0.0251451669678216,0.0226657221646338,0.0269062499979516));
#35997=CARTESIAN_POINT('',(-0.0219784351231431,0.0194989903199553,0.0269999999979516));
#35998=CARTESIAN_POINT('',(-0.0175,0.0194989903199553,0.0270937499979516));
#35999=CARTESIAN_POINT('',(-0.013021564876857,0.0194989903199553,0.0271874999979516));
#36000=CARTESIAN_POINT('',(-0.00985483303217851,0.0226657221646338,0.0272812499979516));
#36001=CARTESIAN_POINT('',(-0.00668810118750004,0.0258324540093123,0.0273749999979517));
#36002=CARTESIAN_POINT('',(-0.00668810118750004,0.0303108891324553,0.0274687499979516));
#36003=CARTESIAN_POINT('',(-0.00709405059375004,0.0303108891324553,0.0212343749989759));
#36004=CARTESIAN_POINT('',(-0.0075,0.0303108891324553,0.021));
#36005=CARTESIAN_POINT('',(-0.00668810118750004,0.0303108891324553,0.0214687499979517));
#36006=CARTESIAN_POINT('',(-0.00668810118750004,0.0303108891324553,0.0214687499979517));
#36007=CARTESIAN_POINT('',(-0.00668810118750004,0.0347893242555984,0.0215624999979517));
#36008=CARTESIAN_POINT('',(-0.00985483303217851,0.0379560561002769,0.0216562499979517));
#36009=CARTESIAN_POINT('',(-0.013021564876857,0.0411227879449553,0.0217499999979516));
#36010=CARTESIAN_POINT('',(-0.0175,0.0411227879449554,0.0218437499979517));
#36011=CARTESIAN_POINT('',(-0.0219784351231431,0.0411227879449553,0.0219374999979516));
#36012=CARTESIAN_POINT('',(-0.0251451669678216,0.0379560561002769,0.0220312499979517));
#36013=CARTESIAN_POINT('',(-0.0283118988125,0.0347893242555984,0.0221249999979516));
#36014=CARTESIAN_POINT('',(-0.0283118988125,0.0303108891324553,0.0222187499979517));
#36015=CARTESIAN_POINT('',(-0.0283118988125,0.0258324540093123,0.0223124999979516));
#36016=CARTESIAN_POINT('',(-0.0251451669678216,0.0226657221646338,0.0224062499979517));
#36017=CARTESIAN_POINT('',(-0.0219784351231431,0.0194989903199553,0.0224999999979516));
#36018=CARTESIAN_POINT('',(-0.0175,0.0194989903199553,0.0225937499979517));
#36019=CARTESIAN_POINT('',(-0.013021564876857,0.0194989903199553,0.0226874999979516));
#36020=CARTESIAN_POINT('',(-0.00985483303217851,0.0226657221646338,0.0227812499979517));
#36021=CARTESIAN_POINT('',(-0.00668810118750004,0.0258324540093123,0.0228749999979516));
#36022=CARTESIAN_POINT('',(-0.00668810118750004,0.0303108891324553,0.0229687499979517));
#36023=CARTESIAN_POINT('',(-0.00668810118750004,0.0347893242555984,0.0230624999979516));
#36024=CARTESIAN_POINT('',(-0.00985483303217851,0.0379560561002769,0.0231562499979516));
#36025=CARTESIAN_POINT('',(-0.013021564876857,0.0411227879449553,0.0232499999979516));
#36026=CARTESIAN_POINT('',(-0.0175,0.0411227879449554,0.0233437499979516));
#36027=CARTESIAN_POINT('',(-0.0219784351231431,0.0411227879449553,0.0234374999979516));
#36028=CARTESIAN_POINT('',(-0.0251451669678216,0.0379560561002769,0.0235312499979516));
#36029=CARTESIAN_POINT('',(-0.0283118988125,0.0347893242555984,0.0236249999979516));
#36030=CARTESIAN_POINT('',(-0.0283118988125,0.0303108891324553,0.0237187499979516));
#36031=CARTESIAN_POINT('',(-0.0283118988125,0.0258324540093123,0.0238124999979517));
#36032=CARTESIAN_POINT('',(-0.0251451669678216,0.0226657221646338,0.0239062499979516));
#36033=CARTESIAN_POINT('',(-0.0219784351231431,0.0194989903199553,0.0239999999979516));
#36034=CARTESIAN_POINT('',(-0.0175,0.0194989903199553,0.0240937499979516));
#36035=CARTESIAN_POINT('',(-0.013021564876857,0.0194989903199553,0.0241874999979516));
#36036=CARTESIAN_POINT('',(-0.00985483303217851,0.0226657221646338,0.0242812499979516));
#36037=CARTESIAN_POINT('',(-0.00668810118750004,0.0258324540093123,0.0243749999979516));
#36038=CARTESIAN_POINT('',(-0.00668810118750004,0.0303108891324553,0.0244687499979516));
#36039=CARTESIAN_POINT('',(-0.00668810118750004,0.0347893242555984,0.0245624999979516));
#36040=CARTESIAN_POINT('',(-0.00985483303217851,0.0379560561002769,0.0246562499979517));
#36041=CARTESIAN_POINT('',(-0.013021564876857,0.0411227879449553,0.0247499999979516));
#36042=CARTESIAN_POINT('',(-0.0175,0.0411227879449554,0.0248437499979517));
#36043=CARTESIAN_POINT('',(-0.0219784351231431,0.0411227879449553,0.0249374999979516));
#36044=CARTESIAN_POINT('',(-0.0251451669678216,0.0379560561002769,0.0250312499979517));
#36045=CARTESIAN_POINT('',(-0.0283118988125,0.0347893242555984,0.0251249999979516));
#36046=CARTESIAN_POINT('',(-0.0283118988125,0.0303108891324553,0.0252187499979517));
#36047=CARTESIAN_POINT('',(-0.0283118988125,0.0258324540093123,0.0253124999979516));
#36048=CARTESIAN_POINT('',(-0.0251451669678216,0.0226657221646338,0.0254062499979517));
#36049=CARTESIAN_POINT('',(-0.0219784351231431,0.0194989903199553,0.0254999999979516));
#36050=CARTESIAN_POINT('',(-0.0175,0.0194989903199553,0.0255937499979517));
#36051=CARTESIAN_POINT('',(-0.013021564876857,0.0194989903199553,0.0256874999979516));
#36052=CARTESIAN_POINT('',(-0.00985483303217851,0.0226657221646338,0.0257812499979517));
#36053=CARTESIAN_POINT('',(-0.00668810118750004,0.0258324540093123,0.0258749999979516));
#36054=CARTESIAN_POINT('',(-0.00668810118750004,0.0303108891324553,0.0259687499979517));
#36055=CARTESIAN_POINT('',(-0.00668810118750004,0.0347893242555984,0.0260624999979516));
#36056=CARTESIAN_POINT('',(-0.00985483303217851,0.0379560561002769,0.0261562499979517));
#36057=CARTESIAN_POINT('',(-0.013021564876857,0.0411227879449553,0.0262499999979516));
#36058=CARTESIAN_POINT('',(-0.0175,0.0411227879449554,0.0263437499979517));
#36059=CARTESIAN_POINT('',(-0.0219784351231431,0.0411227879449553,0.0264374999979516));
#36060=CARTESIAN_POINT('',(-0.0251451669678216,0.0379560561002769,0.0265312499979517));
#36061=CARTESIAN_POINT('',(-0.0283118988125,0.0347893242555984,0.0266249999979516));
#36062=CARTESIAN_POINT('',(-0.0283118988125,0.0303108891324553,0.0267187499979517));
#36063=CARTESIAN_POINT('',(-0.0283118988125,0.0258324540093123,0.0268124999979516));
#36064=CARTESIAN_POINT('',(-0.0251451669678216,0.0226657221646338,0.0269062499979516));
#36065=CARTESIAN_POINT('',(-0.0219784351231431,0.0194989903199553,0.0269999999979516));
#36066=CARTESIAN_POINT('',(-0.0175,0.0194989903199553,0.0270937499979516));
#36067=CARTESIAN_POINT('',(-0.013021564876857,0.0194989903199553,0.0271874999979516));
#36068=CARTESIAN_POINT('',(-0.00985483303217851,0.0226657221646338,0.0272812499979516));
#36069=CARTESIAN_POINT('',(-0.00668810118750004,0.0258324540093123,0.0273749999979517));
#36070=CARTESIAN_POINT('',(-0.00668810118750004,0.0303108891324553,0.0274687499979516));
#36071=CARTESIAN_POINT('',(-0.00668810118750004,0.0303108891324553,0.0274687499979516));
#36072=CARTESIAN_POINT('',(-0.00709405059375004,0.0303108891324553,0.0272343749989758));
#36073=CARTESIAN_POINT('',(-0.0075,0.0303108891324553,0.027));
#36074=CARTESIAN_POINT('',(-0.0275,0.0303108891324553,0.02625));
#36075=CARTESIAN_POINT('',(-0.0275000000000001,0.0261687535087244,0.02634375));
#36076=CARTESIAN_POINT('',(-0.0245710678118655,0.0232398213205899,0.0264375));
#36077=CARTESIAN_POINT('',(-0.021642135623731,0.0203108891324553,0.02653125));
#36078=CARTESIAN_POINT('',(-0.0175,0.0203108891324553,0.026625));
#36079=CARTESIAN_POINT('',(-0.0133578643762691,0.0203108891324553,0.02671875));
#36080=CARTESIAN_POINT('',(-0.0104289321881346,0.0232398213205899,0.0268125));
#36081=CARTESIAN_POINT('',(-0.00750000000000004,0.0261687535087243,0.02690625));
#36082=CARTESIAN_POINT('',(-0.0075,0.0303108891324553,0.027));
#36083=CARTESIAN_POINT('',(-0.0275,0.0303108891324553,0.02625));
#36084=CARTESIAN_POINT('',(-0.0075,0.0303108891324553,0.0255));
#36085=CARTESIAN_POINT('',(-0.00750000000000004,0.0344530247561863,0.02559375));
#36086=CARTESIAN_POINT('',(-0.0104289321881346,0.0373819569443208,0.0256875));
#36087=CARTESIAN_POINT('',(-0.0133578643762691,0.0403108891324553,0.02578125));
#36088=CARTESIAN_POINT('',(-0.0175,0.0403108891324553,0.025875));
#36089=CARTESIAN_POINT('',(-0.021642135623731,0.0403108891324553,0.02596875));
#36090=CARTESIAN_POINT('',(-0.0245710678118655,0.0373819569443208,0.0260625));
#36091=CARTESIAN_POINT('',(-0.0275000000000001,0.0344530247561863,0.02615625));
#36092=CARTESIAN_POINT('',(-0.0275,0.0303108891324553,0.02625));
#36093=CARTESIAN_POINT('',(-0.0075,0.0303108891324553,0.0255));
#36094=CARTESIAN_POINT('',(-0.0275,0.0303108891324553,0.02475));
#36095=CARTESIAN_POINT('',(-0.0275000000000001,0.0261687535087244,0.02484375));
#36096=CARTESIAN_POINT('',(-0.0245710678118655,0.0232398213205899,0.0249375));
#36097=CARTESIAN_POINT('',(-0.021642135623731,0.0203108891324553,0.02503125));
#36098=CARTESIAN_POINT('',(-0.0175,0.0203108891324553,0.025125));
#36099=CARTESIAN_POINT('',(-0.0133578643762691,0.0203108891324553,0.02521875));
#36100=CARTESIAN_POINT('',(-0.0104289321881346,0.0232398213205899,0.0253125));
#36101=CARTESIAN_POINT('',(-0.00750000000000004,0.0261687535087243,0.02540625));
#36102=CARTESIAN_POINT('',(-0.0075,0.0303108891324553,0.0255));
#36103=CARTESIAN_POINT('',(-0.0275,0.0303108891324553,0.02475));
#36104=CARTESIAN_POINT('',(-0.0075,0.0303108891324553,0.024));
#36105=CARTESIAN_POINT('',(-0.00750000000000002,0.0344530247561863,0.02409375));
#36106=CARTESIAN_POINT('',(-0.0104289321881346,0.0373819569443208,0.0241875));
#36107=CARTESIAN_POINT('',(-0.0133578643762691,0.0403108891324553,0.02428125));
#36108=CARTESIAN_POINT('',(-0.0175,0.0403108891324553,0.024375));
#36109=CARTESIAN_POINT('',(-0.021642135623731,0.0403108891324553,0.02446875));
#36110=CARTESIAN_POINT('',(-0.0245710678118655,0.0373819569443208,0.0245625));
#36111=CARTESIAN_POINT('',(-0.0275000000000001,0.0344530247561863,0.02465625));
#36112=CARTESIAN_POINT('',(-0.0275,0.0303108891324553,0.02475));
#36113=CARTESIAN_POINT('',(-0.0075,0.0303108891324553,0.024));
#36114=CARTESIAN_POINT('',(-0.0275,0.0303108891324553,0.02325));
#36115=CARTESIAN_POINT('',(-0.0275000000000001,0.0261687535087243,0.02334375));
#36116=CARTESIAN_POINT('',(-0.0245710678118655,0.0232398213205899,0.0234375));
#36117=CARTESIAN_POINT('',(-0.021642135623731,0.0203108891324553,0.02353125));
#36118=CARTESIAN_POINT('',(-0.0175,0.0203108891324553,0.023625));
#36119=CARTESIAN_POINT('',(-0.0133578643762691,0.0203108891324553,0.02371875));
#36120=CARTESIAN_POINT('',(-0.0104289321881346,0.0232398213205899,0.0238125));
#36121=CARTESIAN_POINT('',(-0.00750000000000006,0.0261687535087243,0.02390625));
#36122=CARTESIAN_POINT('',(-0.0075,0.0303108891324553,0.024));
#36123=CARTESIAN_POINT('',(-0.0275,0.0303108891324553,0.02325));
#36124=CARTESIAN_POINT('',(-0.0075,0.0303108891324553,0.0225));
#36125=CARTESIAN_POINT('',(-0.00750000000000005,0.0344530247561863,0.02259375));
#36126=CARTESIAN_POINT('',(-0.0104289321881346,0.0373819569443208,0.0226875));
#36127=CARTESIAN_POINT('',(-0.0133578643762691,0.0403108891324553,0.02278125));
#36128=CARTESIAN_POINT('',(-0.0175,0.0403108891324553,0.022875));
#36129=CARTESIAN_POINT('',(-0.021642135623731,0.0403108891324553,0.02296875));
#36130=CARTESIAN_POINT('',(-0.0245710678118655,0.0373819569443208,0.0230625));
#36131=CARTESIAN_POINT('',(-0.0275000000000001,0.0344530247561863,0.02315625));
#36132=CARTESIAN_POINT('',(-0.0275,0.0303108891324553,0.02325));
#36133=CARTESIAN_POINT('',(-0.0075,0.0303108891324553,0.0225));
#36134=CARTESIAN_POINT('',(-0.0275,0.0303108891324553,0.02175));
#36135=CARTESIAN_POINT('',(-0.0275000000000001,0.0261687535087244,0.02184375));
#36136=CARTESIAN_POINT('',(-0.0245710678118655,0.0232398213205899,0.0219375));
#36137=CARTESIAN_POINT('',(-0.021642135623731,0.0203108891324553,0.02203125));
#36138=CARTESIAN_POINT('',(-0.0175,0.0203108891324553,0.022125));
#36139=CARTESIAN_POINT('',(-0.0133578643762691,0.0203108891324553,0.02221875));
#36140=CARTESIAN_POINT('',(-0.0104289321881346,0.0232398213205899,0.0223125));
#36141=CARTESIAN_POINT('',(-0.00750000000000003,0.0261687535087244,0.0224062500000001));
#36142=CARTESIAN_POINT('',(-0.0075,0.0303108891324553,0.0225));
#36143=CARTESIAN_POINT('',(-0.0275,0.0303108891324553,0.02175));
#36144=CARTESIAN_POINT('',(-0.0075,0.0303108891324553,0.021));
#36145=CARTESIAN_POINT('',(-0.00750000000000004,0.0344530247561863,0.02109375));
#36146=CARTESIAN_POINT('',(-0.0104289321881346,0.0373819569443208,0.0211875));
#36147=CARTESIAN_POINT('',(-0.0133578643762691,0.0403108891324553,0.02128125));
#36148=CARTESIAN_POINT('',(-0.0175,0.0403108891324553,0.021375));
#36149=CARTESIAN_POINT('',(-0.021642135623731,0.0403108891324553,0.02146875));
#36150=CARTESIAN_POINT('',(-0.0245710678118655,0.0373819569443208,0.0215625));
#36151=CARTESIAN_POINT('',(-0.0275000000000001,0.0344530247561862,0.02165625));
#36152=CARTESIAN_POINT('',(-0.0275,0.0303108891324553,0.02175));
#36153=CARTESIAN_POINT('',(-0.0175,0.0303108891324553,0.0227055389329771));
#36154=CARTESIAN_POINT('',(-0.00668810118750004,0.0303108891324553,0.0215624999979517));
#36155=CARTESIAN_POINT('',(-0.00668810118750004,0.0303108891324553,0.0275624999979516));
#36156=CARTESIAN_POINT('',(-0.00668810118750004,0.0303108891324553,0.0275624999979516));
#36157=CARTESIAN_POINT('',(-0.0075,0.0303108891324553,0.0275624999979516));
#36158=CARTESIAN_POINT('',(-0.00668810118750004,0.0303108891324553,0.0275624999979516));
#36159=CARTESIAN_POINT('',(-0.0075,0.0303108891324553,0.0215624999979517));
#36160=CARTESIAN_POINT('',(-0.0175,0.0303108891324553,0.021));
#36161=CARTESIAN_POINT('',(-0.0175,0.0303108891324553,0.021));
#36162=CARTESIAN_POINT('',(-0.0175,0.0303108891324553,0.021));
#36163=CARTESIAN_POINT('',(-0.0295,0.0303108891324553,0.021));
#36164=CARTESIAN_POINT('',(0.0150054713301403,0.0116548629404355,0.0361391701443907));
#36165=CARTESIAN_POINT('',(0.0150031588763673,0.0116578401919889,0.035947934784466));
#36166=CARTESIAN_POINT('',(0.0151539652239554,0.0117751854584953,0.0359394078676464));
#36167=CARTESIAN_POINT('',(0.0147161665958775,0.0120273386973655,0.036148565230682));
#36168=CARTESIAN_POINT('',(0.0147210398289912,0.0120209153897032,0.0359662072084213));
#36169=CARTESIAN_POINT('',(0.0148546185149646,0.0121445710251608,0.0359492170745093));
#36170=CARTESIAN_POINT('',(0.0144133059896117,0.0123886722824512,0.0361546881596415));
#36171=CARTESIAN_POINT('',(0.0144143214096126,0.0123876620823172,0.0359787226980922));
#36172=CARTESIAN_POINT('',(0.0145436629927643,0.0125047669320259,0.0359563064442854));
#36173=CARTESIAN_POINT('',(0.0137806677531994,0.0130887656693854,0.0361714915612611));
#36174=CARTESIAN_POINT('',(0.0137809942375612,0.0130882928088727,0.0360024592325571));
#36175=CARTESIAN_POINT('',(0.0138987058352324,0.0132065284189183,0.0359742968067866));
#36176=CARTESIAN_POINT('',(0.0134509186271344,0.0134275053033658,0.0361831802396108));
#36177=CARTESIAN_POINT('',(0.0134479713569291,0.0134304584458767,0.0360141932545989));
#36178=CARTESIAN_POINT('',(0.013565452208009,0.0135487654179437,0.0359860369724177));
#36179=CARTESIAN_POINT('',(0.0127639622054845,0.0140821297892993,0.0362069676037666));
#36180=CARTESIAN_POINT('',(0.0127608824316598,0.0140849200425824,0.0360380293351662));
#36181=CARTESIAN_POINT('',(0.0128722761287665,0.0142089014121378,0.036009833448151));
#36182=CARTESIAN_POINT('',(0.0124055409164308,0.0143988762317392,0.0362189194690151));
#36183=CARTESIAN_POINT('',(0.0124024061219934,0.0144015785667605,0.0360500306463481));
#36184=CARTESIAN_POINT('',(0.0125105936649424,0.014528289602461,0.0360217950032614));
#36185=CARTESIAN_POINT('',(0.0116714517710063,0.0150000765239135,0.036242673130302));
#36186=CARTESIAN_POINT('',(0.0116681817468594,0.0150026195968398,0.0360738590671113));
#36187=CARTESIAN_POINT('',(0.0117698571779652,0.0151345076388992,0.0360455634085746));
#36188=CARTESIAN_POINT('',(0.0112948641563,0.0152855569023416,0.0362545093019396));
#36189=CARTESIAN_POINT('',(0.0112914933446839,0.0152880478903352,0.0360857214182595));
#36190=CARTESIAN_POINT('',(0.0113898744880696,0.0154223731515779,0.0360574046522466));
#36191=CARTESIAN_POINT('',(0.0101370220428386,0.016097503179033,0.0362900435294723));
#36192=CARTESIAN_POINT('',(0.010133457137473,0.0160997487415128,0.0361212573242105));
#36193=CARTESIAN_POINT('',(0.0102216604240609,0.0162411455678868,0.0360929396859323));
#36194=CARTESIAN_POINT('',(0.00932784277326136,0.0165797177732773,0.0363137944754649));
#36195=CARTESIAN_POINT('',(0.00932402550068061,0.0165818564949476,0.0361448926543703));
#36196=CARTESIAN_POINT('',(0.00940532350498953,0.0167275004883187,0.0361166676303393));
#36197=CARTESIAN_POINT('',(0.00805749908506388,0.0172133852439097,0.0363495830710199));
#36198=CARTESIAN_POINT('',(0.00805365291654553,0.0172151864437042,0.0361805854510368));
#36199=CARTESIAN_POINT('',(0.00812374034472282,0.017366482829951,0.0361524376560477));
#36200=CARTESIAN_POINT('',(0.00762302277337706,0.0174102228500188,0.0363615663698332));
#36201=CARTESIAN_POINT('',(0.00761917539836762,0.0174119074800385,0.0361925640669859));
#36202=CARTESIAN_POINT('',(0.00768540896722212,0.0175649362904097,0.0361644200944729));
#36203=CARTESIAN_POINT('',(0.0067421348108262,0.0177699171096375,0.0363854684767082));
#36204=CARTESIAN_POINT('',(0.00673821226469986,0.0177714051850552,0.0362164741581558));
#36205=CARTESIAN_POINT('',(0.00679670148073716,0.0179275483463163,0.0361883236436059));
#36206=CARTESIAN_POINT('',(0.00629750019405377,0.0179322032679647,0.0363973418696297));
#36207=CARTESIAN_POINT('',(0.00629354409684533,0.0179335927900506,0.0362283581420782));
#36208=CARTESIAN_POINT('',(0.00634812012471546,0.0180911321687717,0.0362001991088505));
#36209=CARTESIAN_POINT('',(0.00495135232263279,0.0183677380514857,0.0364328740623035));
#36210=CARTESIAN_POINT('',(0.00494731728573729,0.0183688244427915,0.0362639076752442));
#36211=CARTESIAN_POINT('',(0.00499004225783576,0.018530121831357,0.0362357348449958));
#36212=CARTESIAN_POINT('',(0.00403766104134308,0.0185899382196955,0.0364564584641844));
#36213=CARTESIAN_POINT('',(0.00403354391352598,0.0185908321653496,0.0362874747700997));
#36214=CARTESIAN_POINT('',(0.00406827840324674,0.0187540564461923,0.0362593158706682));
#36215=CARTESIAN_POINT('',(0.00264279108803299,0.0188212056651329,0.0364919907042367));
#36216=CARTESIAN_POINT('',(0.0026386301707038,0.0188217898732382,0.0363230061665402));
#36217=CARTESIAN_POINT('',(0.00266112044395212,0.0189869921716713,0.0362948477881039));
#36218=CARTESIAN_POINT('',(0.00217376239730524,0.0188812204022797,0.0365038571823142));
#36219=CARTESIAN_POINT('',(0.00216966039829716,0.0188816939766296,0.0363348774179181));
#36220=CARTESIAN_POINT('',(0.00218797198716229,0.0190474033987819,0.0363067152235105));
#36221=CARTESIAN_POINT('',(0.00122736168079795,0.0189662676914545,0.0365276159903745));
#36222=CARTESIAN_POINT('',(0.00122325978210865,0.0189665313786802,0.0363587404620788));
#36223=CARTESIAN_POINT('',(0.00123325939896185,0.0191328317845803,0.0363304939496865));
#36224=CARTESIAN_POINT('',(0.000750109747437154,0.0189910895629562,0.0365395229269734));
#36225=CARTESIAN_POINT('',(0.000746035312959843,0.0189912527062141,0.0363707284949299));
#36226=CARTESIAN_POINT('',(0.000751817144200152,0.0191576547601785,0.0363424168003708));
#36227=CARTESIAN_POINT('',(-0.000670065907784316,0.0190117753343796,0.0365749488927423));
#36228=CARTESIAN_POINT('',(-0.000673874856843052,0.0190116233381809,0.0364063765575926));
#36229=CARTESIAN_POINT('',(-0.000680804354205267,0.0191778946149216,0.0363778877747587));
#36230=CARTESIAN_POINT('',(-0.00160954297810004,0.0189550625967369,0.0365983944775526));
#36231=CARTESIAN_POINT('',(-0.00161373965550082,0.0189547054858199,0.0364299487070827));
#36232=CARTESIAN_POINT('',(-0.00162848218484478,0.019120310475174,0.0364013569929705));
#36233=CARTESIAN_POINT('',(-0.00300799590936611,0.0187662787272906,0.036633876228612));
#36234=CARTESIAN_POINT('',(-0.00301215150832985,0.0187656130285369,0.0364654104309061));
#36235=CARTESIAN_POINT('',(-0.00303913970831725,0.0189295349129496,0.0364368354483491));
#36236=CARTESIAN_POINT('',(-0.00347234573253729,0.0186859927943862,0.0366457512682207));
#36237=CARTESIAN_POINT('',(-0.0034765462939763,0.018685210758763,0.0364772515256066));
#36238=CARTESIAN_POINT('',(-0.00350754249106109,0.0188484660646857,0.0364487036494823));
#36239=CARTESIAN_POINT('',(-0.00439738683072631,0.0184901730835349,0.0366696406146067));
#36240=CARTESIAN_POINT('',(-0.00440155639190949,0.0184891832393428,0.0365010320369736));
#36241=CARTESIAN_POINT('',(-0.00444066149242716,0.0186508142610025,0.0364725717219389));
#36242=CARTESIAN_POINT('',(-0.00485946183245549,0.0183742272060465,0.0366816913984795));
#36243=CARTESIAN_POINT('',(-0.00486362356602114,0.0183731244670117,0.0365130094368909));
#36244=CARTESIAN_POINT('',(-0.00490677393536493,0.0185338153889762,0.0364846080278259));
#36245=CARTESIAN_POINT('',(-0.00623047589763161,0.017974636268116,0.0367178177623487));
#36246=CARTESIAN_POINT('',(-0.00623477555290467,0.0179731625453613,0.0365489393515267));
#36247=CARTESIAN_POINT('',(-0.0062897509041315,0.0181305941503993,0.0365206945255701));
#36248=CARTESIAN_POINT('',(-0.00711376035248052,0.0176430910751536,0.03674150620782));
#36249=CARTESIAN_POINT('',(-0.00711741722307947,0.0176416296124813,0.0365725725693226));
#36250=CARTESIAN_POINT('',(-0.00718068263463432,0.0177959670518017,0.0365443741266795));
#36251=CARTESIAN_POINT('',(-0.00882110726856891,0.0168544449803335,0.0367885120981666));
#36252=CARTESIAN_POINT('',(-0.00882456908118346,0.0168526183525423,0.0366197978000482));
#36253=CARTESIAN_POINT('',(-0.00890266033648855,0.0169997524596937,0.0365914224896071));
#36254=CARTESIAN_POINT('',(-0.00964516470428283,0.0163973397368115,0.0368119386239966));
#36255=CARTESIAN_POINT('',(-0.00964868426798934,0.0163952756846889,0.0366433874886977));
#36256=CARTESIAN_POINT('',(-0.00973372826951099,0.0165382735779742,0.0366148806443442));
#36257=CARTESIAN_POINT('',(-0.0108354707890685,0.015614674538188,0.0368476617333936));
#36258=CARTESIAN_POINT('',(-0.0108388931283578,0.0156122991685692,0.036679173008154));
#36259=CARTESIAN_POINT('',(-0.0109342223730294,0.0157483876887146,0.0366506162690511));
#36260=CARTESIAN_POINT('',(-0.0112248240896321,0.0153371335655903,0.036859675273099));
#36261=CARTESIAN_POINT('',(-0.01122824158708,0.0153346314501312,0.0366911815412776));
#36262=CARTESIAN_POINT('',(-0.0113269189796164,0.015468321592113,0.0366626287034684));
#36263=CARTESIAN_POINT('',(-0.0119750795926056,0.0147587875722466,0.0368835550330791));
#36264=CARTESIAN_POINT('',(-0.0119783813846664,0.014756109998839,0.0367149966242104));
#36265=CARTESIAN_POINT('',(-0.0120836443668111,0.014884773382102,0.0366864959984767));
#36266=CARTESIAN_POINT('',(-0.0123376991914475,0.0144569261127705,0.0368954714669796));
#36267=CARTESIAN_POINT('',(-0.0123409681507439,0.0144541338985067,0.0367268562151948));
#36268=CARTESIAN_POINT('',(-0.0124494054250222,0.014580224628592,0.0366984011330891));
#36269=CARTESIAN_POINT('',(-0.0133887349763937,0.0135139894778297,0.0369311963220453));
#36270=CARTESIAN_POINT('',(-0.013391980180177,0.0135107968379156,0.0367623833297108));
#36271=CARTESIAN_POINT('',(-0.0135095617900217,0.0136289283784537,0.0367340861153028));
#36272=CARTESIAN_POINT('',(-0.0140405295944604,0.0128357666330661,0.0369549874623704));
#36273=CARTESIAN_POINT('',(-0.0140433284392538,0.0128327092039008,0.0367859805271076));
#36274=CARTESIAN_POINT('',(-0.0141670411795076,0.0129447410817698,0.0367578410680902));
#36275=CARTESIAN_POINT('',(-0.0149439782060546,0.0117431196649284,0.0369905594354358));
#36276=CARTESIAN_POINT('',(-0.0149465501818784,0.0117398453202388,0.0368216051756138));
#36277=CARTESIAN_POINT('',(-0.0150780591810504,0.0118422723622672,0.0367934221024625));
#36278=CARTESIAN_POINT('',(-0.0152333218510672,0.0113654199885582,0.0370024373175107));
#36279=CARTESIAN_POINT('',(-0.0152357712602565,0.0113621402906335,0.0368335437749784));
#36280=CARTESIAN_POINT('',(-0.0153697820207074,0.0114611482845017,0.0368053119406504));
#36281=CARTESIAN_POINT('',(-0.0157836614479193,0.0105878655748921,0.0370262155197047));
#36282=CARTESIAN_POINT('',(-0.0157859353279763,0.0105844719750197,0.0368574618914034));
#36283=CARTESIAN_POINT('',(-0.0159246092661184,0.010676551792807,0.0368291173975656));
#36284=CARTESIAN_POINT('',(-0.0160425585467998,0.0101911239560025,0.0370380229775066));
#36285=CARTESIAN_POINT('',(-0.0160447576605073,0.0101876655110854,0.036869346348945));
#36286=CARTESIAN_POINT('',(-0.0161855984644101,0.0102762207197787,0.0368409399653176));
#36287=CARTESIAN_POINT('',(-0.0167717703580097,0.00897766606165621,0.0370733901805091));
#36288=CARTESIAN_POINT('',(-0.016773601611875,0.00897421684756687,0.0369048856237015));
#36289=CARTESIAN_POINT('',(-0.0169207121015404,0.00905184121412537,0.0368763424308858));
#36290=CARTESIAN_POINT('',(-0.0171948593056475,0.008137841358569,0.0370969116729273));
#36291=CARTESIAN_POINT('',(-0.0171967188294503,0.00813389456074387,0.0369284522952958));
#36292=CARTESIAN_POINT('',(-0.0173472535408609,0.00820453899863601,0.0368998711664753));
#36293=CARTESIAN_POINT('',(-0.0177354059733428,0.00683207780183144,0.0371325488546828));
#36294=CARTESIAN_POINT('',(-0.0177369368253014,0.0068281071831255,0.0369639793819681));
#36295=CARTESIAN_POINT('',(-0.0178923121707994,0.00688724367089204,0.0369354876292107));
#36296=CARTESIAN_POINT('',(-0.0178998432688179,0.00638912086206398,0.0371444827328984));
#36297=CARTESIAN_POINT('',(-0.0179012848831722,0.00638507668266705,0.0369758555020377));
#36298=CARTESIAN_POINT('',(-0.0180581382875847,0.00644038769455516,0.0369474100490041));
#36299=CARTESIAN_POINT('',(-0.0181965136995441,0.00548745329097301,0.0371684840151055));
#36300=CARTESIAN_POINT('',(-0.0181977564942562,0.00548333866730378,0.0369997311055984));
#36301=CARTESIAN_POINT('',(-0.0183573102751423,0.00553079228087688,0.03697138665641));
#36302=CARTESIAN_POINT('',(-0.0183288238059416,0.00502779906232661,0.0371805746899094));
#36303=CARTESIAN_POINT('',(-0.0183299512506326,0.00502368414452842,0.0370117539859255));
#36304=CARTESIAN_POINT('',(-0.0184907334703224,0.00506710051140986,0.0369834641380204));
#36305=CARTESIAN_POINT('',(-0.0186705908881364,0.0036479059704665,0.0372164291814345));
#36306=CARTESIAN_POINT('',(-0.0186714379034367,0.00364361154967467,0.0370475001987006));
#36307=CARTESIAN_POINT('',(-0.0188352556230713,0.0036750836839486,0.0370192962198233));
#36308=CARTESIAN_POINT('',(-0.0188278596473151,0.0027196295348313,0.0372398737540957));
#36309=CARTESIAN_POINT('',(-0.0188284295264619,0.00271578388320857,0.0370710611102305));
#36310=CARTESIAN_POINT('',(-0.0189935157205228,0.00273862512585575,0.0370427651063071));
#36311=CARTESIAN_POINT('',(-0.019004411247759,0.000846780273607725,0.0372868546796072));
#36312=CARTESIAN_POINT('',(-0.0190045699896578,0.000842898100617533,0.0371182903933998));
#36313=CARTESIAN_POINT('',(-0.0191708482586001,0.000849305940358859,0.0370897949811809));
#36314=CARTESIAN_POINT('',(-0.0190236362092071,-9.90864261468875E-5,0.0373104525234818));
#36315=CARTESIAN_POINT('',(-0.0190236105305129,-0.000103356945062465,0.0371419877495273));
#36316=CARTESIAN_POINT('',(-0.0191898952974827,-0.000104847364396079,0.0371134111251529));
#36317=CARTESIAN_POINT('',(-0.0189182036402674,-0.00200252934197603,0.0373584378295551));
#36318=CARTESIAN_POINT('',(-0.01891775574234,-0.00200680794040965,0.037189902370063));
#36319=CARTESIAN_POINT('',(-0.0190831294904098,-0.00202494445874197,0.0371613831443892));
#36320=CARTESIAN_POINT('',(-0.0187949378319753,-0.00293848570417647,0.0373822828591816));
#36321=CARTESIAN_POINT('',(-0.0187942194227897,-0.0029429785958604,0.0372135941292793));
#36322=CARTESIAN_POINT('',(-0.018958722724182,-0.00296909208963992,0.0371851970354613));
#36323=CARTESIAN_POINT('',(-0.0184129004148024,-0.00478011345639779,0.0374298727350032));
#36324=CARTESIAN_POINT('',(-0.0184117730522092,-0.00478451749490607,0.0372609113340795));
#36325=CARTESIAN_POINT('',(-0.0185731684945105,-0.00482681154353278,0.0372327333206625));
#36326=CARTESIAN_POINT('',(-0.0181541175259362,-0.00568578481567748,0.0374535194940516));
#36327=CARTESIAN_POINT('',(-0.0181529639024806,-0.00568951455252184,0.0372845076982008));
#36328=CARTESIAN_POINT('',(-0.0183119271885001,-0.00574034356679125,0.0372563723376181));
#36329=CARTESIAN_POINT('',(-0.0176615722557226,-0.00702096136471443,0.037489071103229));
#36330=CARTESIAN_POINT('',(-0.0176600569045193,-0.00702476800508173,0.0373202501340292));
#36331=CARTESIAN_POINT('',(-0.0178145277596478,-0.00708700619075372,0.037291959760207));
#36332=CARTESIAN_POINT('',(-0.0174792538599267,-0.00746327294783377,0.0375009932518153));
#36333=CARTESIAN_POINT('',(-0.0174776502739044,-0.00746703371040129,0.0373322517824091));
#36334=CARTESIAN_POINT('',(-0.0176304145384798,-0.00753310997641051,0.0373038975062605));
#36335=CARTESIAN_POINT('',(-0.0170852874983177,-0.00832572577577798,0.0375246628185486));
#36336=CARTESIAN_POINT('',(-0.0170834939788836,-0.00832940188153098,0.0373560562349849));
#36337=CARTESIAN_POINT('',(-0.0172326351947694,-0.0084029516129172,0.0373275937443767));
#36338=CARTESIAN_POINT('',(-0.0168731413930909,-0.00874750248588951,0.0375364528956926));
#36339=CARTESIAN_POINT('',(-0.0168712372089865,-0.00875117766036781,0.0373679028797414));
#36340=CARTESIAN_POINT('',(-0.0170184658140329,-0.00882833946261563,0.0373393949243217));
#36341=CARTESIAN_POINT('',(-0.0161921413199236,-0.00998505685127267,0.0375718420432244));
#36342=CARTESIAN_POINT('',(-0.0161900056026684,-0.00998850854585282,0.0374033780835406));
#36343=CARTESIAN_POINT('',(-0.0163310925976824,-0.0100765114087224,0.0373748021053271));
#36344=CARTESIAN_POINT('',(-0.0156789682144187,-0.0107732094813255,0.0375954766575031));
#36345=CARTESIAN_POINT('',(-0.015676415516236,-0.0107769012143963,0.0374269646426421));
#36346=CARTESIAN_POINT('',(-0.0158132800581132,-0.0108714680566263,0.0373984255437832));
#36347=CARTESIAN_POINT('',(-0.0145332214666613,-0.0122750788428526,0.0376432225818568));
#36348=CARTESIAN_POINT('',(-0.0145303248317423,-0.0122785300115987,0.0374744753828116));
#36349=CARTESIAN_POINT('',(-0.0146573239782155,-0.012386359365391,0.0374461253942193));
#36350=CARTESIAN_POINT('',(-0.0138956162084445,-0.0129924510713994,0.0376674711168235));
#36351=CARTESIAN_POINT('',(-0.0138928048172763,-0.0129954634359944,0.0374985473407757));
#36352=CARTESIAN_POINT('',(-0.014014094807802,-0.0131099718199376,0.0374703408547971));
#36353=CARTESIAN_POINT('',(-0.012538686354179,-0.0143064069271994,0.0377148389024716));
#36354=CARTESIAN_POINT('',(-0.0125356171246053,-0.0143090890041745,0.0375459982972597));
#36355=CARTESIAN_POINT('',(-0.0126449003590129,-0.01443499193813,0.0375177238513366));
#36356=CARTESIAN_POINT('',(-0.0118162120710391,-0.014908521985929,0.0377381964997738));
#36357=CARTESIAN_POINT('',(-0.011813116889813,-0.0149109891050472,0.0375695350497656));
#36358=CARTESIAN_POINT('',(-0.0119158089831625,-0.0150420366104124,0.0375411171558609));
#36359=CARTESIAN_POINT('',(-0.0106670601049956,-0.0157300843161944,0.03777353081355));
#36360=CARTESIAN_POINT('',(-0.0106636458051717,-0.0157323982000827,0.0376050107567335));
#36361=CARTESIAN_POINT('',(-0.0107562893339342,-0.0158703711407046,0.0375764789793572));
#36362=CARTESIAN_POINT('',(-0.0102730580316003,-0.0159902811627692,0.0377853551568641));
#36363=CARTESIAN_POINT('',(-0.0102695363870165,-0.0159925438324983,0.0376168629961018));
#36364=CARTESIAN_POINT('',(-0.010358752975961,-0.0161327200913,0.0375883087565455));
#36365=CARTESIAN_POINT('',(-0.00946269352699932,-0.0164827862996255,0.0378091861102951));
#36366=CARTESIAN_POINT('',(-0.00945905047971319,-0.0164848780244409,0.0376406911606725));
#36367=CARTESIAN_POINT('',(-0.00954116381799984,-0.0166293341277074,0.0376121395168345));
#36368=CARTESIAN_POINT('',(-0.00904482220411608,-0.0167157459689924,0.0378212343357241));
#36369=CARTESIAN_POINT('',(-0.00904106866268619,-0.0167177754852218,0.0376527111427666));
#36370=CARTESIAN_POINT('',(-0.00911958859647621,-0.0168642565158397,0.0376241820375386));
#36371=CARTESIAN_POINT('',(-0.00777683698870974,-0.0173614715524598,0.0378571713220989));
#36372=CARTESIAN_POINT('',(-0.00777276210631457,-0.0173633105843053,0.0376884999982028));
#36373=CARTESIAN_POINT('',(-0.00784040585450888,-0.0175154685207172,0.0376600892872526));
#36374=CARTESIAN_POINT('',(-0.00690784591584773,-0.0177247307802204,0.0378810100035085));
#36375=CARTESIAN_POINT('',(-0.00690373178108501,-0.0177263240799465,0.0377121389206075));
#36376=CARTESIAN_POINT('',(-0.00696379007350073,-0.0178818959862885,0.0376838892450103));
#36377=CARTESIAN_POINT('',(-0.00512374411469783,-0.0183202528005343,0.0379284549751914));
#36378=CARTESIAN_POINT('',(-0.00511953167638094,-0.01832143877845,0.0377594348084143));
#36379=CARTESIAN_POINT('',(-0.00516398405082556,-0.0184823260981536,0.037731304237429));
#36380=CARTESIAN_POINT('',(-0.0042086343984728,-0.018552526833146,0.0379519491088865));
#36381=CARTESIAN_POINT('',(-0.00420489696214683,-0.0185533920251016,0.0377830608406211));
#36382=CARTESIAN_POINT('',(-0.00424076685047704,-0.0187162358287406,0.0377548258401882));
#36383=CARTESIAN_POINT('',(-0.00233039814015239,-0.0188806276353035,0.0379995291145493));
#36384=CARTESIAN_POINT('',(-0.00232659312175988,-0.0188810801521881,0.0378309289691186));
#36385=CARTESIAN_POINT('',(-0.00234593999503727,-0.0190464021372848,0.0378024624662963));
#36386=CARTESIAN_POINT('',(-0.00138918386749588,-0.0189724749457313,0.0380230950232191));
#36387=CARTESIAN_POINT('',(-0.00138498020199089,-0.0189727818803281,0.037854613968655));
#36388=CARTESIAN_POINT('',(-0.00139644988445051,-0.0191386865299805,0.0378260505551503));
#36389=CARTESIAN_POINT('',(0.000491394329291348,-0.0190169179678846,0.0380703932917064));
#36390=CARTESIAN_POINT('',(0.000495637576888113,-0.0190168106419338,0.0379018852344002));
#36391=CARTESIAN_POINT('',(0.000500614389251542,-0.0191830655857678,0.037873344175741));
#36392=CARTESIAN_POINT('',(0.00143175034843468,-0.0189696728656897,0.0380941477309837));
#36393=CARTESIAN_POINT('',(0.0014362479032175,-0.0189693191294249,0.0379255097828157));
#36394=CARTESIAN_POINT('',(0.00144920178766854,-0.01913531960882,0.0378970719744518));
#36395=CARTESIAN_POINT('',(0.00284238342400006,-0.0187921647474114,0.0381300899636321));
#36396=CARTESIAN_POINT('',(0.00284662846057186,-0.0187915244138856,0.0379612649815778));
#36397=CARTESIAN_POINT('',(0.0028721631719315,-0.0189560989677983,0.0379329784026332));
#36398=CARTESIAN_POINT('',(0.00331441870834582,-0.0187146954289997,0.0381421650442573));
#36399=CARTESIAN_POINT('',(0.00331857804575343,-0.0187139582770902,0.0379732853469086));
#36400=CARTESIAN_POINT('',(0.00334831904383978,-0.0188778892806443,0.0379450429468843));
#36401=CARTESIAN_POINT('',(0.00424454885795175,-0.0185259008247079,0.0381660293974286));
#36402=CARTESIAN_POINT('',(0.00424864072028103,-0.0185249631732459,0.0379971363307566));
#36403=CARTESIAN_POINT('',(0.00428652689934009,-0.0186872200107699,0.0379689040486078));
#36404=CARTESIAN_POINT('',(0.00470370079483309,-0.0184145889742131,0.0381778419035332));
#36405=CARTESIAN_POINT('',(0.00470768720968842,-0.0184135722921259,0.0380089916051811));
#36406=CARTESIAN_POINT('',(0.00474965416178299,-0.0185747665565142,0.0379807250413738));
#36407=CARTESIAN_POINT('',(0.00606380119694438,-0.0180310251530532,0.0382131547292891));
#36408=CARTESIAN_POINT('',(0.00606749675489961,-0.018029767989791,0.0380444706945485));
#36409=CARTESIAN_POINT('',(0.0061215042945471,-0.0181873072730242,0.0380160711436542));
#36410=CARTESIAN_POINT('',(0.00694748782462672,-0.0177094134570405,0.0382365440826416));
#36411=CARTESIAN_POINT('',(0.0069513148115175,-0.0177079163720193,0.038068014101374));
#36412=CARTESIAN_POINT('',(0.00701278761473244,-0.0178624923287709,0.0380394902056667));
#36413=CARTESIAN_POINT('',(0.00823823532605298,-0.0171275861325818,0.0382720683555505));
#36414=CARTESIAN_POINT('',(0.00824199786134128,-0.0171257761164743,0.0381035828034171));
#36415=CARTESIAN_POINT('',(0.00831467242736803,-0.0172751908127472,0.038075023547654));
#36416=CARTESIAN_POINT('',(0.0086626641886403,-0.0169170087108244,0.0382839795954378));
#36417=CARTESIAN_POINT('',(0.0086664417757708,-0.0169150732813902,0.0381154832438721));
#36418=CARTESIAN_POINT('',(0.00874277095704306,-0.0170626723128832,0.0380869325313221));
#36419=CARTESIAN_POINT('',(0.00949954853666518,-0.0164616375906773,0.0383080094950215));
#36420=CARTESIAN_POINT('',(0.00950323875888994,-0.0164595095632353,0.0381394377811394));
#36421=CARTESIAN_POINT('',(0.00958691185482858,-0.0166031712779041,0.0381109478454699));
#36422=CARTESIAN_POINT('',(0.00990843536764638,-0.0162186992949781,0.0383200270202185));
#36423=CARTESIAN_POINT('',(0.00991210717425925,-0.0162164537967256,0.0381513935373868));
#36424=CARTESIAN_POINT('',(0.00999935496721639,-0.0163580607416676,0.0381229531141535));
#36425=CARTESIAN_POINT('',(0.0110994261007969,-0.0154497874825496,0.0383559010620778));
#36426=CARTESIAN_POINT('',(0.0111031423256522,-0.0154471380416969,0.0381870634441405));
#36427=CARTESIAN_POINT('',(0.0112007117190244,-0.0155823067969157,0.0381587859658031));
#36428=CARTESIAN_POINT('',(0.0118494369587164,-0.0148821057065514,0.0383796746295091));
#36429=CARTESIAN_POINT('',(0.011852646263133,-0.0148795566452164,0.0382106555459431));
#36430=CARTESIAN_POINT('',(0.0119572588280899,-0.0150096152999654,0.0381825259246114));
#36431=CARTESIAN_POINT('',(0.0129092501586493,-0.0139489360514091,0.038415073154031));
#36432=CARTESIAN_POINT('',(0.0129122957065155,-0.0139461160896238,0.0382461342271903));
#36433=CARTESIAN_POINT('',(0.0130260382391751,-0.0140679459369744,0.0382179387953184));
#36434=CARTESIAN_POINT('',(0.0132516089108831,-0.0136242158973507,0.0384268476317155));
#36435=CARTESIAN_POINT('',(0.0132545427144061,-0.0136213651199016,0.0382579736292449));
#36436=CARTESIAN_POINT('',(0.0133712586534689,-0.0137402396292797,0.0382297260369069));
#36437=CARTESIAN_POINT('',(0.0139140780149237,-0.0129469235936279,0.0384504924275424));
#36438=CARTESIAN_POINT('',(0.0139168584048897,-0.01294393237065,0.0382817603825315));
#36439=CARTESIAN_POINT('',(0.0140392380233699,-0.0130567327058869,0.0382533985485152));
#36440=CARTESIAN_POINT('',(0.0142354224239416,-0.0125927827016563,0.0384624126901118));
#36441=CARTESIAN_POINT('',(0.0142381414406254,-0.012589711627674,0.0382937568838186));
#36442=CARTESIAN_POINT('',(0.014363241677094,-0.0126993490720532,0.0382653337823739));
#36443=CARTESIAN_POINT('',(0.0151522276287887,-0.0115026826837114,0.0384980076223509));
#36444=CARTESIAN_POINT('',(0.0151545874552716,-0.0114995531518966,0.0383295152258469));
#36445=CARTESIAN_POINT('',(0.0152876502554025,-0.0115993400969666,0.0383009622830993));
#36446=CARTESIAN_POINT('',(0.0157028445696647,-0.0107380131205138,0.0385215934366976));
#36447=CARTESIAN_POINT('',(0.0157053127628298,-0.0107343885637693,0.0383531321867574));
#36448=CARTESIAN_POINT('',(0.0158428716019425,-0.010827822373824,0.0383245525184931));
#36449=CARTESIAN_POINT('',(0.0166863994512137,-0.00913500556704324,0.0385690398252237));
#36450=CARTESIAN_POINT('',(0.0166885267815842,-0.00913114013625447,0.0384004187286762));
#36451=CARTESIAN_POINT('',(0.0168347853906698,-0.00921061383527548,0.0383719678507318));
#36452=CARTESIAN_POINT('',(0.0171193431567698,-0.00829667109200794,0.0385928971779095));
#36453=CARTESIAN_POINT('',(0.0171212465033512,-0.00829272483889006,0.0384240949560577));
#36454=CARTESIAN_POINT('',(0.0172714888685827,-0.00836491513506412,0.0383957899260171));
#36455=CARTESIAN_POINT('',(0.0176771319563529,-0.00698181001816414,0.0386288991507295));
#36456=CARTESIAN_POINT('',(0.0176786906208708,-0.00697786552822998,0.0384599999960005));
#36457=CARTESIAN_POINT('',(0.0178339126296295,-0.00703845721684935,0.0384317728072497));
#36458=CARTESIAN_POINT('',(0.0178464393626524,-0.00653667127314852,0.0386408395226));
#36459=CARTESIAN_POINT('',(0.0178478625413834,-0.00653278908310416,0.0384719535535284));
#36460=CARTESIAN_POINT('',(0.0180045668908952,-0.00658938096130684,0.0384437158153504));
#36461=CARTESIAN_POINT('',(0.0181494253443772,-0.00564108402055084,0.0386644913397127));
#36462=CARTESIAN_POINT('',(0.0181506465751278,-0.00563714975327069,0.038495697562868));
#36463=CARTESIAN_POINT('',(0.018309872103834,-0.00568584827677441,0.0384673853426935));
#36464=CARTESIAN_POINT('',(0.0182836395517567,-0.00518939017263809,0.0386762445560239));
#36465=CARTESIAN_POINT('',(0.0182847605137434,-0.00518544719602479,0.0385075191395397));
#36466=CARTESIAN_POINT('',(0.0184450696221258,-0.005230143102191,0.0384791520040357));
#36467=CARTESIAN_POINT('',(0.0186352161966197,-0.00382278691467086,0.0387114894144686));
#36468=CARTESIAN_POINT('',(0.0186359845944907,-0.00381897190788193,0.0385429418061745));
#36469=CARTESIAN_POINT('',(0.0187991701429938,-0.00385143102407525,0.0385144330338758));
#36470=CARTESIAN_POINT('',(0.0188017960362101,-0.0028964201027731,0.0387349811818274));
#36471=CARTESIAN_POINT('',(0.0188024454149778,-0.0028921752332426,0.0385665207905428));
#36472=CARTESIAN_POINT('',(0.018966882805175,-0.00291689698104377,0.0385379405990861));
#36473=CARTESIAN_POINT('',(0.0189479153503385,-0.00148347557315803,0.0387707536733621));
#36474=CARTESIAN_POINT('',(0.0189482467385373,-0.00147925369912812,0.0386022240958527));
#36475=CARTESIAN_POINT('',(0.0191139948493069,-0.0014915431171492,0.0385737003077644));
#36476=CARTESIAN_POINT('',(0.0189792661299307,-0.00100653752197626,0.038782814865168));
#36477=CARTESIAN_POINT('',(0.0189794916596513,-0.001002251562758,0.0386142366077066));
#36478=CARTESIAN_POINT('',(0.0191455543189113,-0.00101042246271182,0.0385857517789344));
#36479=CARTESIAN_POINT('',(0.0190058525312823,-5.68346111770116E-5,0.0388068420499248));
#36480=CARTESIAN_POINT('',(0.0190058674042672,-5.25318559422445E-5,0.0386381350600849));
#36481=CARTESIAN_POINT('',(0.0191722756290578,-5.23957056172181E-5,0.038609753788149));
#36482=CARTESIAN_POINT('',(0.0190012916831888,0.000415945346046065,0.0388188083349403));
#36483=CARTESIAN_POINT('',(0.0190011954646666,0.00042025103815367,0.0386500229389775));
#36484=CARTESIAN_POINT('',(0.019167642261252,0.000424526058990718,0.0386217047075898));
#36485=CARTESIAN_POINT('',(0.0189353110941103,0.00182821727683686,0.0388545731395467));
#36486=CARTESIAN_POINT('',(0.018934890195968,0.00183273174670508,0.0386855956068839));
#36487=CARTESIAN_POINT('',(0.019100944459924,0.00184915730125414,0.0386574305714316));
#36488=CARTESIAN_POINT('',(0.0188218749463008,0.00276167625899422,0.0388781470791831));
#36489=CARTESIAN_POINT('',(0.0188213246428188,0.00276552616071793,0.0387091476577289));
#36490=CARTESIAN_POINT('',(0.0189862822059325,0.00279074695963414,0.0386810023014141));
#36491=CARTESIAN_POINT('',(0.0185472934983701,0.00414974239546678,0.0389134831899818));
#36492=CARTESIAN_POINT('',(0.0185463978178042,0.00415373650031088,0.038744683372103));
#36493=CARTESIAN_POINT('',(0.0187087218937265,0.00419085004648558,0.0387163759892953));
#36494=CARTESIAN_POINT('',(0.0184382916390242,0.00461040202404379,0.0389252797588995));
#36495=CARTESIAN_POINT('',(0.0184373014075557,0.00461437039626621,0.0387565586044812));
#36496=CARTESIAN_POINT('',(0.018598559234186,0.00465549550858827,0.0387281879997201));
#36497=CARTESIAN_POINT('',(0.0181844048677269,0.00552755144667211,0.0389490404383303));
#36498=CARTESIAN_POINT('',(0.0181832126536465,0.00553146714312297,0.0387804504254259));
#36499=CARTESIAN_POINT('',(0.0183420680926315,0.00558057318884372,0.0387519746590418));
#36500=CARTESIAN_POINT('',(0.0180399541591308,0.00598194757027819,0.0389609521020994));
#36501=CARTESIAN_POINT('',(0.0180386500163758,0.00598588330045647,0.0387924150945185));
#36502=CARTESIAN_POINT('',(0.0181961788428216,0.00603889409903781,0.0387638967209641));
#36503=CARTESIAN_POINT('',(0.0175600527577911,0.00731704300465663,0.0389965132793485));
#36504=CARTESIAN_POINT('',(0.0175584774699178,0.00732081044190295,0.0388280482386248));
#36505=CARTESIAN_POINT('',(0.0177116499128679,0.00738553362907206,0.0387994730817159));
#36506=CARTESIAN_POINT('',(0.017176600931976,0.00817618649942297,0.0390201720001328));
#36507=CARTESIAN_POINT('',(0.0171746560250469,0.00818024084845669,0.0388516453823604));
#36508=CARTESIAN_POINT('',(0.0173246945182605,0.00825213319926071,0.0388231180125633));
#36509=CARTESIAN_POINT('',(0.0165075720298665,0.00941920787493285,0.0390558582625029));
#36510=CARTESIAN_POINT('',(0.0165054454097937,0.00942293852162265,0.0388871453891533));
#36511=CARTESIAN_POINT('',(0.0166496672349242,0.00950596673263848,0.0388587687948336));
#36512=CARTESIAN_POINT('',(0.0162688557302333,0.00982590126449492,0.0390677822215656));
#36513=CARTESIAN_POINT('',(0.0162666412000637,0.00982956491781396,0.0388989998022133));
#36514=CARTESIAN_POINT('',(0.0164088235359054,0.00991619979799271,0.0388706791571233));
#36515=CARTESIAN_POINT('',(0.0157594566755032,0.0106237247575267,0.0390916827747241));
#36516=CARTESIAN_POINT('',(0.0157570704482312,0.010627266788554,0.0389228038988642));
#36517=CARTESIAN_POINT('',(0.0158948546840466,0.0107209302791126,0.0388945605424311));
#36518=CARTESIAN_POINT('',(0.0154875468403251,0.0110164331272623,0.039103700532307));
#36519=CARTESIAN_POINT('',(0.0154851324209757,0.0110198284626436,0.038934798802496));
#36520=CARTESIAN_POINT('',(0.0156204878405909,0.0111170111446627,0.0389065739056364));
#36521=CARTESIAN_POINT('',(0.01463225995395,0.0121573267026454,0.0391394336004382));
#36522=CARTESIAN_POINT('',(0.0146296726940152,0.0121604286682179,0.0389706139625599));
#36523=CARTESIAN_POINT('',(0.0147573523537256,0.0122675988502235,0.0389423227946196));
#36524=CARTESIAN_POINT('',(0.0140116166276898,0.0128669651519896,0.0391628479121368));
#36525=CARTESIAN_POINT('',(0.014008934229898,0.0128699010213118,0.0389942080391084));
#36526=CARTESIAN_POINT('',(0.0141309339335042,0.0129831580760785,0.0389657727502402));
#36527=CARTESIAN_POINT('',(0.012672679814133,0.0141875783371347,0.0392099060817211));
#36528=CARTESIAN_POINT('',(0.0126696949858274,0.0141902322562065,0.0390414338041929));
#36529=CARTESIAN_POINT('',(0.0127797951853403,0.0143148573607752,0.0390128645733509));
#36530=CARTESIAN_POINT('',(0.0119543874113125,0.0147985541865073,0.0392335494260721));
#36531=CARTESIAN_POINT('',(0.0119509078822839,0.0148013492768455,0.0390650749354725));
#36532=CARTESIAN_POINT('',(0.012055068200747,0.014931008420279,0.0390365056751324));
#36533=CARTESIAN_POINT('',(0.0108011721063,0.0156384406904196,0.0392695930882427));
#36534=CARTESIAN_POINT('',(0.0107976455557038,0.0156408785488082,0.0391009499668969));
#36535=CARTESIAN_POINT('',(0.010891641938822,0.0157781079937479,0.0390725173883642));
#36536=CARTESIAN_POINT('',(0.0104050549928709,0.0159046738736348,0.0392816670826779));
#36537=CARTESIAN_POINT('',(0.0104014461052566,0.0159070323820953,0.0391129496189465));
#36538=CARTESIAN_POINT('',(0.0104920332148233,0.0160466424796337,0.0390845767324489));
#36539=CARTESIAN_POINT('',(0.00960060432550017,0.0164028112534571,0.0393056145314552));
#36540=CARTESIAN_POINT('',(0.00959688329125498,0.0164049915851909,0.0391367542902623));
#36541=CARTESIAN_POINT('',(0.00968049362552568,0.0165490736695186,0.0391084961636348));
#36542=CARTESIAN_POINT('',(0.00919077016220187,0.0166358376692505,0.0393175351290205));
#36543=CARTESIAN_POINT('',(0.00918704062898051,0.0166378968498416,0.0391486055828836));
#36544=CARTESIAN_POINT('',(0.00926704844523166,0.0167841022166925,0.0391204033728952));
#36545=CARTESIAN_POINT('',(0.00793881728687105,0.0172875846957858,0.0393531118455946));
#36546=CARTESIAN_POINT('',(0.00793487961528051,0.0172893992463166,0.0391840956119047));
#36547=CARTESIAN_POINT('',(0.00800402716637696,0.0174413142009149,0.039155961915177));
#36548=CARTESIAN_POINT('',(0.00707437008646464,0.017659234549578,0.0393765064409228));
#36549=CARTESIAN_POINT('',(0.00707080832974097,0.0176606790938871,0.039207641159205));
#36550=CARTESIAN_POINT('',(0.007131844103949,0.0178158234315231,0.0391793875957313));
#36551=CARTESIAN_POINT('',(0.005732249994112,0.0181208479176423,0.0394119261070158));
#36552=CARTESIAN_POINT('',(0.00572835454355227,0.0181220780387678,0.0392432790471558));
#36553=CARTESIAN_POINT('',(0.00577777163514192,0.0182809051014134,0.0392148490066115));
#36554=CARTESIAN_POINT('',(0.00527545652035367,0.0182591268759004,0.0394238350568987));
#36555=CARTESIAN_POINT('',(0.00527149473368085,0.0182602728773766,0.0392552533782693));
#36556=CARTESIAN_POINT('',(0.00531692029397464,0.0184202071183902,0.0392267708015014));
#36557=CARTESIAN_POINT('',(0.00435539353041513,0.018500181160291,0.0394476409160019));
#36558=CARTESIAN_POINT('',(0.00435136851956518,0.0185011277015551,0.0392791386244272));
#36559=CARTESIAN_POINT('',(0.00438871216218091,0.0186630486100609,0.0392505926666229));
#36560=CARTESIAN_POINT('',(0.00389346521987264,0.0186027756405381,0.039459504480206));
#36561=CARTESIAN_POINT('',(0.00388935165258131,0.0186036364179546,0.0392910186220323));
#36562=CARTESIAN_POINT('',(0.00392270794497542,0.0187664061473219,0.0392624593799105));
#36563=CARTESIAN_POINT('',(0.0025021362129001,0.0188581188397552,0.0394950907033245));
#36564=CARTESIAN_POINT('',(0.0024979024578147,0.0188586841465867,0.039326569989871));
#36565=CARTESIAN_POINT('',(0.00251913145143705,0.0190236684794769,0.0392980390079921));
#36566=CARTESIAN_POINT('',(0.00156722162533421,0.0189587090116307,0.0395188250839918));
#36567=CARTESIAN_POINT('',(0.00156273541928549,0.0189590661812377,0.0393501647798695));
#36568=CARTESIAN_POINT('',(0.0015760199744932,0.0191250631597236,0.0393217450128133));
#36569=CARTESIAN_POINT('',(0.000153819308255418,0.019005224212649,0.039554568327384));
#36570=CARTESIAN_POINT('',(0.000149530859344075,0.01900526053676,0.0393857282248346));
#36571=CARTESIAN_POINT('',(0.000150241301015367,0.0191718195442531,0.0393574537845495));
#36572=CARTESIAN_POINT('',(-0.000319160762607007,0.0190032637954438,0.0395665019919062));
#36573=CARTESIAN_POINT('',(-0.000323370020041294,0.019003192852083,0.0393976124045188));
#36574=CARTESIAN_POINT('',(-0.000326875348561001,0.0191697739060299,0.039369377919062));
#36575=CARTESIAN_POINT('',(-0.00126890586194998,0.018963538076665,0.0395903822535847));
#36576=CARTESIAN_POINT('',(-0.00127308020914811,0.0189632583539193,0.0394214973160597));
#36577=CARTESIAN_POINT('',(-0.00128490540974052,0.0191294501530534,0.0393932584593037));
#36578=CARTESIAN_POINT('',(-0.00174506512229052,0.0189256111751952,0.0396023189675094));
#36579=CARTESIAN_POINT('',(-0.00174915643471746,0.0189252355786291,0.0394334832095891));
#36580=CARTESIAN_POINT('',(-0.00176521655921334,0.0190910107260413,0.0394052049194109));
#36581=CARTESIAN_POINT('',(-0.00315527515090238,0.018760071462149,0.039637791882901));
#36582=CARTESIAN_POINT('',(-0.003159109299956,0.0187594121399547,0.0394691299482635));
#36583=CARTESIAN_POINT('',(-0.00318770175369042,0.0189234555223965,0.0394407127252026));
#36584=CARTESIAN_POINT('',(-0.00407912829785893,0.018580793512523,0.0396612080344229));
#36585=CARTESIAN_POINT('',(-0.00408316786564095,0.018579909525709,0.0394926925719882));
#36586=CARTESIAN_POINT('',(-0.00411956712144044,0.0187422127576033,0.039464156958556));
#36587=CARTESIAN_POINT('',(-0.00544090513770603,0.0182103774010545,0.0396966359311057));
#36588=CARTESIAN_POINT('',(-0.00544491365088278,0.0182091796481191,0.0395281488885336));
#36589=CARTESIAN_POINT('',(-0.00549317019086339,0.0183681706275683,0.0394995908528479));
#36590=CARTESIAN_POINT('',(-0.0058908137160072,0.0180699183671704,0.0397084917546821));
#36591=CARTESIAN_POINT('',(-0.00589485530925784,0.0180685997080032,0.0395399883854288));
#36592=CARTESIAN_POINT('',(-0.00594698956526464,0.0182263848992081,0.0395114433292663));
#36593=CARTESIAN_POINT('',(-0.00678246751915138,0.0177544859228465,0.0397323568648656));
#36594=CARTESIAN_POINT('',(-0.00678645328451132,0.0177529647917131,0.0395637699716895));
#36595=CARTESIAN_POINT('',(-0.00684640658568973,0.0179080488318765,0.0395352922314537));
#36596=CARTESIAN_POINT('',(-0.00722571835368339,0.017578833949069,0.0397444079220017));
#36597=CARTESIAN_POINT('',(-0.00722970204839152,0.0175771942536395,0.0395757558710103));
#36598=CARTESIAN_POINT('',(-0.00729352337765429,0.0177308137646229,0.0395473303724816));
#36599=CARTESIAN_POINT('',(-0.00853200419952799,0.0170032508445306,0.0397805349308342));
#36600=CARTESIAN_POINT('',(-0.0085360992930078,0.0170012150729036,0.039611674312779));
#36601=CARTESIAN_POINT('',(-0.00861120340273501,0.0171500754775071,0.0395834152712123));
#36602=CARTESIAN_POINT('',(-0.0093640660238232,0.0165589396761269,0.0398043541347681));
#36603=CARTESIAN_POINT('',(-0.00936760081192483,0.0165569485390271,0.0396353274950174));
#36604=CARTESIAN_POINT('',(-0.00945051414852193,0.016701814789159,0.0396072040025732));
#36605=CARTESIAN_POINT('',(-0.01095333582558,0.0155534128083901,0.0398514625261982));
#36606=CARTESIAN_POINT('',(-0.0109566123383997,0.0155510945355589,0.0396825712046406));
#36607=CARTESIAN_POINT('',(-0.0110533401052372,0.0156869529799877,0.0396543377658962));
#36608=CARTESIAN_POINT('',(-0.0117105392461648,0.0149921946210177,0.039874852741731));
#36609=CARTESIAN_POINT('',(-0.011713637850033,0.0149897904366676,0.0397061581247415));
#36610=CARTESIAN_POINT('',(-0.0118168992740911,0.0151204397263602,0.0396777669570562));
#36611=CARTESIAN_POINT('',(-0.0127884183122455,0.0140599436100801,0.0399104774481127));
#36612=CARTESIAN_POINT('',(-0.0127914607265617,0.0140571744085504,0.0397419455571428));
#36613=CARTESIAN_POINT('',(-0.0129038625355801,0.0141796081141066,0.0397134232557945));
#36614=CARTESIAN_POINT('',(-0.0131379114294796,0.0137338809283803,0.0399224413483593));
#36615=CARTESIAN_POINT('',(-0.0131409305574613,0.0137309932121728,0.0397539429397205));
#36616=CARTESIAN_POINT('',(-0.0132563078073279,0.013850572888493,0.0397253936890723));
#36617=CARTESIAN_POINT('',(-0.0138057031563641,0.0130624179401111,0.0399462274691676));
#36618=CARTESIAN_POINT('',(-0.0138085845594307,0.0130593726890895,0.0397777367289653));
#36619=CARTESIAN_POINT('',(-0.0139297708475482,0.0131730492921678,0.0397491816858674));
#36620=CARTESIAN_POINT('',(-0.0141255775468695,0.0127157202418076,0.0399581004650935));
#36621=CARTESIAN_POINT('',(-0.0141284240212117,0.0127125564928361,0.0397895871103025));
#36622=CARTESIAN_POINT('',(-0.0142523778617903,0.0128232511590351,0.0397610500977433));
#36623=CARTESIAN_POINT('',(-0.0150438981845955,0.0116433266987443,0.0399937332592782));
#36624=CARTESIAN_POINT('',(-0.0150466194918001,0.011639828119222,0.0398250918461492));
#36625=CARTESIAN_POINT('',(-0.0151785812924363,0.0117413244877355,0.0397966572050952));
#36626=CARTESIAN_POINT('',(-0.015601268190893,0.0108855078609694,0.0400175221674402));
#36627=CARTESIAN_POINT('',(-0.0156037502572203,0.0108819389745214,0.0398486971526389));
#36628=CARTESIAN_POINT('',(-0.0157408064102649,0.0109768426249763,0.0398204106081291));
#36629=CARTESIAN_POINT('',(-0.0163539519335297,0.00968357985430214,0.0400532444840827));
#36630=CARTESIAN_POINT('',(-0.0163561069607314,0.00967994124090683,0.0398843442193726));
#36631=CARTESIAN_POINT('',(-0.0164998281064669,0.00976425969374833,0.0398561178725525));
#36632=CARTESIAN_POINT('',(-0.0165915150789842,0.00927083072614016,0.0400651730542086));
#36633=CARTESIAN_POINT('',(-0.0165935289830433,0.0092672292824464,0.039896296072404));
#36634=CARTESIAN_POINT('',(-0.0167393345586793,0.00934782893475484,0.0398680510651776));
#36635=CARTESIAN_POINT('',(-0.0170350195453023,0.00842821357465935,0.0400889840246388));
#36636=CARTESIAN_POINT('',(-0.0170368417118387,0.0084245268980667,0.0399202084076463));
#36637=CARTESIAN_POINT('',(-0.0171863989694787,0.00849767210950886,0.039891881591703));
#36638=CARTESIAN_POINT('',(-0.0172396324978774,0.00800110402734881,0.0401007953333983));
#36639=CARTESIAN_POINT('',(-0.0172413601410088,0.00799738572201798,0.039932089458272));
#36640=CARTESIAN_POINT('',(-0.0173926212073374,0.0080667359571995,0.0399037066132332));
#36641=CARTESIAN_POINT('',(-0.0178034336420264,0.00670284475631644,0.0401361524066879));
#36642=CARTESIAN_POINT('',(-0.0178047945753691,0.00669919133529955,0.0399676203732049));
#36643=CARTESIAN_POINT('',(-0.0179608373997931,0.0067568816351323,0.0399390991282188));
#36644=CARTESIAN_POINT('',(-0.0181128517827389,0.00581485538526614,0.0401596376776761));
#36645=CARTESIAN_POINT('',(-0.0181141665497967,0.00581074175312345,0.0399911802605542));
#36646=CARTESIAN_POINT('',(-0.0182726660690083,0.00586101576834401,0.0399625976310416));
#36647=CARTESIAN_POINT('',(-0.0184777093830138,0.00444929676135907,0.040195251280918));
#36648=CARTESIAN_POINT('',(-0.0184787035275952,0.00444517229375046,0.0400267096747493));
#36649=CARTESIAN_POINT('',(-0.0186404590020018,0.00448342268040512,0.0399981955538656));
#36650=CARTESIAN_POINT('',(-0.0185827164300928,0.00398849194161903,0.0402071825625149));
#36651=CARTESIAN_POINT('',(-0.0185836162437446,0.00398429085242931,0.0400385885567563));
#36652=CARTESIAN_POINT('',(-0.0187463269246786,0.00401856738028491,0.040010116389651));
#36653=CARTESIAN_POINT('',(-0.0187587324938683,0.00305538428239273,0.0402312024082703));
#36654=CARTESIAN_POINT('',(-0.0187594268054271,0.0030511343055048,0.0400624751713173));
#36655=CARTESIAN_POINT('',(-0.0189237939209322,0.00307726697975156,0.0400341101664153));
#36656=CARTESIAN_POINT('',(-0.0188296379468907,0.00258246669485135,0.0402433059287324));
#36657=CARTESIAN_POINT('',(-0.0188302208997272,0.00257820196063475,0.0400744988885604));
#36658=CARTESIAN_POINT('',(-0.0189952883801537,0.00260020132984729,0.0400461980710632));
#36659=CARTESIAN_POINT('',(-0.018987584222582,0.00117014663797905,0.0402792453812985));
#36660=CARTESIAN_POINT('',(-0.0189878766130811,0.00116563546292821,0.0401102538110408));
#36661=CARTESIAN_POINT('',(-0.0191544678476417,0.00117549997084161,0.0400821000667122));
#36662=CARTESIAN_POINT('',(-0.019021886828312,0.000229388592566755,0.04030281238303));
#36663=CARTESIAN_POINT('',(-0.0190219485422196,0.000225513787905416,0.040133827629379));
#36664=CARTESIAN_POINT('',(-0.0191888011910571,0.000226509022047831,0.0401056704327208));
#36665=CARTESIAN_POINT('',(-0.0189515281684091,-0.00165056890722806,0.0403497808792148));
#36666=CARTESIAN_POINT('',(-0.0189511778767747,-0.0016544084517273,0.0401810645284669));
#36667=CARTESIAN_POINT('',(-0.0191170355267067,-0.00166987725288971,0.0401526910770812));
#36668=CARTESIAN_POINT('',(-0.0188464963096979,-0.0025917854637227,0.0403733212216877));
#36669=CARTESIAN_POINT('',(-0.0188459456773645,-0.00259582874536051,0.0402047736177609));
#36670=CARTESIAN_POINT('',(-0.0190106563679482,-0.00261928870902019,0.0401762639310132));
#36671=CARTESIAN_POINT('',(-0.0184926679060761,-0.00446419183693985,0.0404211076161054));
#36672=CARTESIAN_POINT('',(-0.0184917002032655,-0.00446818357577394,0.0402526399957149));
#36673=CARTESIAN_POINT('',(-0.0186531564962856,-0.0045079905629465,0.0402240668619258));
#36674=CARTESIAN_POINT('',(-0.0182479002120906,-0.00537572886801895,0.0404448565103214));
#36675=CARTESIAN_POINT('',(-0.0182466139791819,-0.00538004586951678,0.0402763139845434));
#36676=CARTESIAN_POINT('',(-0.018406104300253,-0.00542747010521316,0.0402477993929647));
#36677=CARTESIAN_POINT('',(-0.0176278853553927,-0.00715136217164255,0.0404924090082616));
#36678=CARTESIAN_POINT('',(-0.0176262006455918,-0.00715555313748112,0.040323620177768));
#36679=CARTESIAN_POINT('',(-0.0177804667049412,-0.00721858680345464,0.0402953035664709));
#36680=CARTESIAN_POINT('',(-0.0172526295359134,-0.00801545626095273,0.0405161760389477));
#36681=CARTESIAN_POINT('',(-0.0172509307221984,-0.00801912986087298,0.040347239024586));
#36682=CARTESIAN_POINT('',(-0.0174018482893674,-0.00809020306586266,0.040319043275123));
#36683=CARTESIAN_POINT('',(-0.0165891310234162,-0.00927501607177101,0.0405518309761127));
#36684=CARTESIAN_POINT('',(-0.0165871113566919,-0.00927862586719968,0.0403830003753058));
#36685=CARTESIAN_POINT('',(-0.016732118837969,-0.00936054912549886,0.0403547177731007));
#36686=CARTESIAN_POINT('',(-0.0163504407096611,-0.0096895664096134,0.0405637668909742));
#36687=CARTESIAN_POINT('',(-0.0163483530307484,-0.00969309279106215,0.0403950016662479));
#36688=CARTESIAN_POINT('',(-0.0164911668339191,-0.00977862891273121,0.040366666560219));
#36689=CARTESIAN_POINT('',(-0.0158470220953076,-0.0104926878976402,0.0405874381582746));
#36690=CARTESIAN_POINT('',(-0.0158447595959533,-0.010496101570109,0.04041879922213));
#36691=CARTESIAN_POINT('',(-0.0159830116902603,-0.01058857535944,0.0403903626650279));
#36692=CARTESIAN_POINT('',(-0.0155815030828519,-0.0108829408412664,0.0405992200571002));
#36693=CARTESIAN_POINT('',(-0.0155791404639051,-0.0108863256057379,0.0404306420263519));
#36694=CARTESIAN_POINT('',(-0.0157150102784006,-0.0109821387006477,0.0404021565358583));
#36695=CARTESIAN_POINT('',(-0.0147443380000451,-0.0120204432381726,0.0406345751477657));
#36696=CARTESIAN_POINT('',(-0.0147417946425176,-0.0120235500482091,0.040466107316148));
#36697=CARTESIAN_POINT('',(-0.014870115139696,-0.0121293123008178,0.0404375344932468));
#36698=CARTESIAN_POINT('',(-0.0141323054150094,-0.012734617153313,0.0406581742442809));
#36699=CARTESIAN_POINT('',(-0.0141292982380388,-0.0127379352802263,0.0404896901080622));
#36700=CARTESIAN_POINT('',(-0.0142525651721741,-0.0128496009415859,0.0404611285718946));
#36701=CARTESIAN_POINT('',(-0.0127993117038726,-0.0140737397407963,0.0407059276861236));
#36702=CARTESIAN_POINT('',(-0.012795989406329,-0.0140767800209882,0.0405372130140451));
#36703=CARTESIAN_POINT('',(-0.0129077330328863,-0.0142002990080325,0.0405088370003867));
#36704=CARTESIAN_POINT('',(-0.0120743866383509,-0.0147009483119556,0.0407301934339938));
#36705=CARTESIAN_POINT('',(-0.0120710300120229,-0.0147036972494881,0.0405612702667684));
#36706=CARTESIAN_POINT('',(-0.0121764415327295,-0.0148329955623863,0.0405330628488529));
#36707=CARTESIAN_POINT('',(-0.0105423258825493,-0.0158356578312777,0.0407782066571403));
#36708=CARTESIAN_POINT('',(-0.0105387562032422,-0.0158380387566235,0.0406091983341337));
#36709=CARTESIAN_POINT('',(-0.0106307531401576,-0.0159773049789665,0.040581058297319));
#36710=CARTESIAN_POINT('',(-0.00973264971430907,-0.016345206458774,0.0408019714360824));
#36711=CARTESIAN_POINT('',(-0.00972934845143041,-0.0163471907527672,0.0406331359711917));
#36712=CARTESIAN_POINT('',(-0.0098137431818835,-0.0164909303385969,0.0406048583516335));
#36713=CARTESIAN_POINT('',(-0.00806537401592001,-0.0172290448552643,0.040849071665102));
#36714=CARTESIAN_POINT('',(-0.00806187747714099,-0.0172306642979756,0.0406805112314068));
#36715=CARTESIAN_POINT('',(-0.00813148945943629,-0.0173818031815893,0.0406520128667242));
#36716=CARTESIAN_POINT('',(-0.00720410797528281,-0.0176065010020934,0.0408725336732333));
#36717=CARTESIAN_POINT('',(-0.00720015555035734,-0.0176081146295931,0.0407040676752542));
#36718=CARTESIAN_POINT('',(-0.00726254823193961,-0.017762253651073,0.0406754920583924));
#36719=CARTESIAN_POINT('',(-0.00587093155877073,-0.0180763429638379,0.0409081137712902));
#36720=CARTESIAN_POINT('',(-0.00586691205994924,-0.0180776491619511,0.0407395938948666));
#36721=CARTESIAN_POINT('',(-0.0059175910359496,-0.0182359248774687,0.0407110623000412));
#36722=CARTESIAN_POINT('',(-0.00541963181038933,-0.018216834715786,0.0409200341480749));
#36723=CARTESIAN_POINT('',(-0.00541552867837081,-0.0182180537864837,0.0407514716238395));
#36724=CARTESIAN_POINT('',(-0.00546231699354845,-0.0183775787376718,0.0407229741499068));
#36725=CARTESIAN_POINT('',(-0.00450289334993954,-0.0184648159346774,0.0409440335352421));
#36726=CARTESIAN_POINT('',(-0.00449872590875717,-0.0184658340544464,0.0407753565497765));
#36727=CARTESIAN_POINT('',(-0.00453751882102838,-0.0186276217911276,0.0407469511301288));
#36728=CARTESIAN_POINT('',(-0.00403695754679052,-0.0185722191308532,0.0409561242729045));
#36729=CARTESIAN_POINT('',(-0.00403276579261126,-0.0185731285420499,0.0407873765694338));
#36730=CARTESIAN_POINT('',(-0.00406749283074953,-0.0187359238531794,0.0407590279987012));
#36731=CARTESIAN_POINT('',(-0.00264132417527466,-0.0188393419555243,0.0409920272199963));
#36732=CARTESIAN_POINT('',(-0.00263689297781954,-0.0188399757678068,0.0408231190853848));
#36733=CARTESIAN_POINT('',(-0.00265961278377104,-0.0190052087860372,0.0407948982614302));
#36734=CARTESIAN_POINT('',(-0.00170611182026073,-0.0189466097837117,0.0410155716589265));
#36735=CARTESIAN_POINT('',(-0.00170222908050555,-0.0189469732330682,0.0408466877375895));
#36736=CARTESIAN_POINT('',(-0.00171619674648011,-0.0191131286454142,0.0408184492137106));
#36737=CARTESIAN_POINT('',(0.000173676291005686,-0.0190224781872767,0.0410625631663291));
#36738=CARTESIAN_POINT('',(0.000177561804452529,-0.0190224283900372,0.0408939239429425));
#36739=CARTESIAN_POINT('',(0.000180075422117499,-0.0191888972842088,0.0408654885305162));
#36740=CARTESIAN_POINT('',(0.00112054509379683,-0.0189908367634547,0.041086146524359));
#36741=CARTESIAN_POINT('',(0.00112470330846933,-0.0189905928322111,0.0409176462158715));
#36742=CARTESIAN_POINT('',(0.00113522074412725,-0.0191565845251325,0.0408890983625158));
#36743=CARTESIAN_POINT('',(0.00301448963456351,-0.0187835128377661,0.041134005321298));
#36744=CARTESIAN_POINT('',(0.00301863139178279,-0.0187828482042093,0.0409655173243587));
#36745=CARTESIAN_POINT('',(0.00304570274636773,-0.0189469427742119,0.0409369603164412));
#36746=CARTESIAN_POINT('',(0.00394221166531097,-0.0186103000822643,0.0411577955127677));
#36747=CARTESIAN_POINT('',(0.0039466673760474,-0.0186093396509136,0.0409891964228946));
#36748=CARTESIAN_POINT('',(0.00398152970205259,-0.0187721087890722,0.0409607271352016));
#36749=CARTESIAN_POINT('',(0.00576061524732153,-0.0181300748464635,0.0412053975508442));
#36750=CARTESIAN_POINT('',(0.00576497305527062,-0.0181287075485317,0.0410365127368558));
#36751=CARTESIAN_POINT('',(0.00581582182420553,-0.0182875225378765,0.041008273159893));
#36752=CARTESIAN_POINT('',(0.00665129567942447,-0.0178230540864072,0.0412291638059619));
#36753=CARTESIAN_POINT('',(0.00665505784648776,-0.0178216596144055,0.0410601325402539));
#36754=CARTESIAN_POINT('',(0.00671426399796193,-0.0179777285045373,0.0410320128311421));
#36755=CARTESIAN_POINT('',(0.00795874306948506,-0.0172593063750968,0.0412648016528986));
#36756=CARTESIAN_POINT('',(0.0079624897360314,-0.01725757706242,0.0410959001265478));
#36757=CARTESIAN_POINT('',(0.00803294542961736,-0.0174085796363617,0.0410676745710227));
#36758=CARTESIAN_POINT('',(0.00839055002517237,-0.0170535400231114,0.0412767285079113));
#36759=CARTESIAN_POINT('',(0.00839421742130898,-0.0170517379264982,0.0411079006699725));
#36760=CARTESIAN_POINT('',(0.00846844394164472,-0.0172008232970993,0.0410796158868639));
#36761=CARTESIAN_POINT('',(0.0092302457670169,-0.0166140639256399,0.0413003785807796));
#36762=CARTESIAN_POINT('',(0.00923381364818658,-0.0166120792976908,0.0411316946468232));
#36763=CARTESIAN_POINT('',(0.00931530390538305,-0.0167571365359391,0.0411032941901137));
#36764=CARTESIAN_POINT('',(0.00963990932261663,-0.0163796754406052,0.0413121493670696));
#36765=CARTESIAN_POINT('',(0.0096434555062509,-0.0163775901268873,0.0411435356216829));
#36766=CARTESIAN_POINT('',(0.00972845586542258,-0.01652052075835,0.0411150787592204));
#36767=CARTESIAN_POINT('',(0.0108389410363852,-0.0156334204306386,0.0413474703331632));
#36768=CARTESIAN_POINT('',(0.0108421950119882,-0.0156311517720273,0.041178994654508));
#36769=CARTESIAN_POINT('',(0.0109377134474799,-0.0157672818803707,0.0411504282304712));
#36770=CARTESIAN_POINT('',(0.0115985132592406,-0.0150786995332378,0.0413710456213849));
#36771=CARTESIAN_POINT('',(0.0116020174110474,-0.0150759907838975,0.0412025738370888));
#36772=CARTESIAN_POINT('',(0.0117037965647246,-0.0152075166331746,0.0411740025318393));
#36773=CARTESIAN_POINT('',(0.013037245328802,-0.0138536249290601,0.0414187558668103));
#36774=CARTESIAN_POINT('',(0.0130404966051281,-0.0138505813276262,0.0412500917664286));
#36775=CARTESIAN_POINT('',(0.0131549586138197,-0.0139715066661794,0.0412216752600993));
#36776=CARTESIAN_POINT('',(0.0137193186319365,-0.0131784541631398,0.0414430267121299));
#36777=CARTESIAN_POINT('',(0.0137222941911337,-0.0131753500627701,0.0412741734181582));
#36778=CARTESIAN_POINT('',(0.0138429835311531,-0.0132903920070307,0.0412459098280563));
#36779=CARTESIAN_POINT('',(0.0149581951487915,-0.0117534571826866,0.0414905424104802));
#36780=CARTESIAN_POINT('',(0.0149608243882024,-0.011750114412885,0.0413216314071093));
#36781=CARTESIAN_POINT('',(0.0150923642333444,-0.0118526683603501,0.0412934130886694));
#36782=CARTESIAN_POINT('',(0.015520688566203,-0.0109997943715279,0.0415139101617592));
#36783=CARTESIAN_POINT('',(0.0155229576784727,-0.0109966158267174,0.0413451631485277));
#36784=CARTESIAN_POINT('',(0.0156594313125402,-0.0110921438850482,0.0413168142304098));
#36785=CARTESIAN_POINT('',(0.0162795889764332,-0.00980799649289466,0.0415492121914758));
#36786=CARTESIAN_POINT('',(0.0162817062626187,-0.00980447906514115,0.0413806424581893));
#36787=CARTESIAN_POINT('',(0.0164245046421128,-0.00988960817174467,0.0413521504341661));
#36788=CARTESIAN_POINT('',(0.0165183582002229,-0.00940047153184422,0.0415610186696038));
#36789=CARTESIAN_POINT('',(0.0165204138835871,-0.00939686076164193,0.0413924953238669));
#36790=CARTESIAN_POINT('',(0.0166652153599872,-0.00947842675338205,0.0413639660176923));
#36791=CARTESIAN_POINT('',(0.0169668815467093,-0.00856445872380873,0.04158481274074));
#36792=CARTESIAN_POINT('',(0.016968759366247,-0.00856073776940504,0.041416327221764));
#36793=CARTESIAN_POINT('',(0.0171174145640933,-0.00863495449719448,0.0413877679181777));
#36794=CARTESIAN_POINT('',(0.017177065864082,-0.00813468948262829,0.0415968345520146));
#36795=CARTESIAN_POINT('',(0.0171788787931287,-0.00813085947155214,0.0414283427704703));
#36796=CARTESIAN_POINT('',(0.0173293372690474,-0.00820137076331004,0.0413997883749501));
#36797=CARTESIAN_POINT('',(0.0177535601601371,-0.00683448318101424,0.0416326921596994));
#36798=CARTESIAN_POINT('',(0.0177551425550477,-0.00683039655157697,0.0414641029034488));
#36799=CARTESIAN_POINT('',(0.0179106526810362,-0.00688967026267464,0.0414356266030977));
#36800=CARTESIAN_POINT('',(0.018069656200551,-0.00594744061890342,0.0416565058932169));
#36801=CARTESIAN_POINT('',(0.018071053086069,-0.00594315201602428,0.041487737925076));
#36802=CARTESIAN_POINT('',(0.0182294850460007,-0.00599484249099837,0.0414594047964829));
#36803=CARTESIAN_POINT('',(0.0185686762479634,-0.00413385867196868,0.0417040557893634));
#36804=CARTESIAN_POINT('',(0.018569665428116,-0.0041294751717134,0.0415350525030694));
#36805=CARTESIAN_POINT('',(0.018732662999263,-0.00416532793544681,0.0415069082292052));
#36806=CARTESIAN_POINT('',(0.0187516269698394,-0.0032072138444847,0.041727668157059));
#36807=CARTESIAN_POINT('',(0.0187522925110488,-0.00320341907381266,0.0415587004547988));
#36808=CARTESIAN_POINT('',(0.0189169160347779,-0.00323052407359695,0.0415305295422462));
#36809=CARTESIAN_POINT('',(0.0189785497013675,-0.00131315874630033,0.041775282469228));
#36810=CARTESIAN_POINT('',(0.0189787976176584,-0.00130933038624944,0.0416065960986041));
#36811=CARTESIAN_POINT('',(0.0191450183683159,-0.00131978865421991,0.0415781986729045));
#36812=CARTESIAN_POINT('',(0.0190196699561884,-0.000369682902736731,0.041798768663557));
#36813=CARTESIAN_POINT('',(0.0190197536794715,-0.000365571149283191,0.0416302401562733));
#36814=CARTESIAN_POINT('',(0.0191860834814799,-0.00036803283829089,0.0416017150620279));
#36815=CARTESIAN_POINT('',(0.0189632035263676,0.00151043791943559,0.0418459668701129));
#36816=CARTESIAN_POINT('',(0.0189628723964422,0.00151456480353777,0.0416774933135412));
#36817=CARTESIAN_POINT('',(0.0191285756981165,0.00152854275765588,0.0416489248534374));
#36818=CARTESIAN_POINT('',(0.0188656035494357,0.00244708229619764,0.041869676770902));
#36819=CARTESIAN_POINT('',(0.0188650082956082,0.00245155860199098,0.0417011164879532));
#36820=CARTESIAN_POINT('',(0.019029988696039,0.00247337433558962,0.0416726161446262));
#36821=CARTESIAN_POINT('',(0.0186125495933428,0.00384679085700881,0.0419056432466697));
#36822=CARTESIAN_POINT('',(0.0186116814547299,0.00385100058683171,0.0417368885715677));
#36823=CARTESIAN_POINT('',(0.0187745695464339,0.00388531336935315,0.0417085455414632));
#36824=CARTESIAN_POINT('',(0.0185098333503103,0.00431405271833229,0.0419177363955599));
#36825=CARTESIAN_POINT('',(0.0185088638003719,0.0043182070784044,0.0417489139784957));
#36826=CARTESIAN_POINT('',(0.0186709077889593,0.00435665613252931,0.0417206255091514));
#36827=CARTESIAN_POINT('',(0.0182715157482693,0.00523227424487254,0.041941661341413));
#36828=CARTESIAN_POINT('',(0.0182703464161454,0.00523636077672844,0.041772765548564));
#36829=CARTESIAN_POINT('',(0.0184303499014007,0.00528286586327708,0.0417445357014452));
#36830=CARTESIAN_POINT('',(0.0181357838983419,0.00568464048515436,0.0419535140553254));
#36831=CARTESIAN_POINT('',(0.0181345455695604,0.00568859447658796,0.0417846212593873));
#36832=CARTESIAN_POINT('',(0.0182933099783667,0.00573914511459434,0.0417563890549324));
#36833=CARTESIAN_POINT('',(0.0176799226482771,0.00702193102801493,0.0419888744003936));
#36834=CARTESIAN_POINT('',(0.0176784448562162,0.0070256238076518,0.0418201020793719));
#36835=CARTESIAN_POINT('',(0.0178329826032857,0.00708796730728556,0.0417917731207448));
#36836=CARTESIAN_POINT('',(0.0173113916908864,0.00788715324152287,0.0420122387595618));
#36837=CARTESIAN_POINT('',(0.0173097335223211,0.00789081251687946,0.0418436408609179));
#36838=CARTESIAN_POINT('',(0.017460819243278,0.00796059517179978,0.0418151717394463));
#36839=CARTESIAN_POINT('',(0.0164441541540594,0.00956458376972509,0.0420595310619518));
#36840=CARTESIAN_POINT('',(0.0164421174582832,0.0095680713322191,0.0418910660817133));
#36841=CARTESIAN_POINT('',(0.0165854185710355,0.00965242605887456,0.0418624909390898));
#36842=CARTESIAN_POINT('',(0.0159408649555386,0.0103817820325783,0.0420836316696311));
#36843=CARTESIAN_POINT('',(0.0159383978648997,0.010385544968291,0.041915133818142));
#36844=CARTESIAN_POINT('',(0.0160775560756277,0.0104766751733535,0.0418865832516409));
#36845=CARTESIAN_POINT('',(0.0148323250115084,0.0119119565334862,0.0421314054120078));
#36846=CARTESIAN_POINT('',(0.0148295044085068,0.0119154922548428,0.0419626612680497));
#36847=CARTESIAN_POINT('',(0.0149591363198844,0.0120201360514607,0.0419343088550291));
#36848=CARTESIAN_POINT('',(0.0142253115705693,0.0126304014464608,0.0421552128021273));
#36849=CARTESIAN_POINT('',(0.0142224595723812,0.012633607676376,0.0419862640682912));
#36850=CARTESIAN_POINT('',(0.0143467869578076,0.0127448697856584,0.0419580774261687));
#36851=CARTESIAN_POINT('',(0.0132364774583089,0.0136388158206757,0.0421907471038048));
#36852=CARTESIAN_POINT('',(0.0132334576479525,0.0136417465358339,0.0420217625471197));
#36853=CARTESIAN_POINT('',(0.0133490796759129,0.0137618674964216,0.041993603964865));
#36854=CARTESIAN_POINT('',(0.0128937599156229,0.01396336454063,0.0422025508615589));
#36855=CARTESIAN_POINT('',(0.0128907415118545,0.0139661539971817,0.0420336077348191));
#36856=CARTESIAN_POINT('',(0.013003246381497,0.0140891303563364,0.0420054159154212));
#36857=CARTESIAN_POINT('',(0.0121815880954904,0.0145888143976149,0.0422262280147507));
#36858=CARTESIAN_POINT('',(0.0121784421451099,0.0145914386973753,0.0420574090145197));
#36859=CARTESIAN_POINT('',(0.0122845861716777,0.0147197644261911,0.0420291170568967));
#36860=CARTESIAN_POINT('',(0.0118105913145593,0.0148907736728587,0.0422381485332703));
#36861=CARTESIAN_POINT('',(0.0118073893680565,0.0148933158527189,0.0420694090337606));
#36862=CARTESIAN_POINT('',(0.0119102049265592,0.0150242021930805,0.0420410531744612));
#36863=CARTESIAN_POINT('',(0.0106734218716814,0.0157473457018157,0.0422736889611043));
#36864=CARTESIAN_POINT('',(0.0106702181203719,0.0157494984225377,0.0421051454901133));
#36865=CARTESIAN_POINT('',(0.01076271558934,0.0158877999445305,0.0420766335422122));
#36866=CARTESIAN_POINT('',(0.00988050851272395,0.0162560718816535,0.0422972091975336));
#36867=CARTESIAN_POINT('',(0.00987683663777725,0.0162582984438685,0.0421287476323781));
#36868=CARTESIAN_POINT('',(0.00996268647807769,0.0164007066453042,0.0421001684059327));
#36869=CARTESIAN_POINT('',(0.00822699946699953,0.017152282683698,0.04234457338802));
#36870=CARTESIAN_POINT('',(0.00822310342235589,0.0171541579220479,0.0421760222602139));
#36871=CARTESIAN_POINT('',(0.00829450940136363,0.0173044330294566,0.0421475155211143));
#36872=CARTESIAN_POINT('',(0.00736640822147979,0.0175397753961563,0.0423684146679046));
#36873=CARTESIAN_POINT('',(0.00736227559279473,0.0175414972662327,0.0421997056878268));
#36874=CARTESIAN_POINT('',(0.00742635462325823,0.0176952661658757,0.0421713251998001));
#36875=CARTESIAN_POINT('',(0.00557485437135022,0.0181886967584633,0.0424165432900864));
#36876=CARTESIAN_POINT('',(0.00557059305018462,0.0181900151580173,0.0422476259115998));
#36877=CARTESIAN_POINT('',(0.00561903875309368,0.0183496257535651,0.0422194125176644));
#36878=CARTESIAN_POINT('',(0.00466249418556595,0.0184430462980749,0.0424402033696721));
#36879=CARTESIAN_POINT('',(0.00465872401835851,0.0184440139348268,0.0422713359950257));
#36880=CARTESIAN_POINT('',(0.00469862095603388,0.018605891838371,0.0422430841271073));
#36881=CARTESIAN_POINT('',(0.00281802077453407,0.0188133879909405,0.0424871885748908));
#36882=CARTESIAN_POINT('',(0.00281417986827133,0.0188139486691576,0.042318570161192));
#36883=CARTESIAN_POINT('',(0.00283785041442192,0.0189787211855483,0.0422901180916585));
#36884=CARTESIAN_POINT('',(0.0018839080918573,0.0189300934702549,0.0425106335656295));
#36885=CARTESIAN_POINT('',(0.00187973838254741,0.0189305086999314,0.0423421439355997));
#36886=CARTESIAN_POINT('',(0.00189551287781105,0.0190960706762482,0.0423135874532213));
#36887=CARTESIAN_POINT('',(0.000464554162843612,0.0190002256974114,0.042546347882846));
#36888=CARTESIAN_POINT('',(0.000460353791048119,0.0190003286426425,0.0423778524092138));
#36889=CARTESIAN_POINT('',(0.000463706370908465,0.0191664584001732,0.0423493011875901));
#36890=CARTESIAN_POINT('',(-1.3603547443907E-5,0.0190059266909682,0.0425583908750204));
#36891=CARTESIAN_POINT('',(-1.78713899531079E-5,0.0190059222927238,0.0423898667183118));
#36892=CARTESIAN_POINT('',(-1.86409425035557E-5,0.0191721206572552,0.0423613383876707));
#36893=CARTESIAN_POINT('',(-0.000962888698749424,0.0189815246962087,0.0425823743588719));
#36894=CARTESIAN_POINT('',(-0.000967165032777534,0.0189813094341095,0.0424137476132222));
#36895=CARTESIAN_POINT('',(-0.000976240535668051,0.0191473772967885,0.0423853018819463));
#36896=CARTESIAN_POINT('',(-0.00143457126590083,0.0189516225437873,0.0425943284623379));
#36897=CARTESIAN_POINT('',(-0.0014388688977218,0.0189512951800986,0.0424256301917518));
#36898=CARTESIAN_POINT('',(-0.00145205322852197,0.0191171736530932,0.0423972418708909));
#36899=CARTESIAN_POINT('',(-0.00284094099793105,0.0188100244891607,0.0426301040963971));
#36900=CARTESIAN_POINT('',(-0.00284545979462405,0.0188093587371052,0.0424611973850735));
#36901=CARTESIAN_POINT('',(-0.0028707299272499,0.0189742158760984,0.042432975391739));
#36902=CARTESIAN_POINT('',(-0.00376699808139046,0.0186467172316367,0.0426537986907363));
#36903=CARTESIAN_POINT('',(-0.00377090364480976,0.01864593864656,0.0424847683690623));
#36904=CARTESIAN_POINT('',(-0.00380486530349046,0.0188093633942862,0.0424566479060653));
#36905=CARTESIAN_POINT('',(-0.00513872791989791,0.0182979796666385,0.0426892045843495));
#36906=CARTESIAN_POINT('',(-0.00514269239735289,0.0182968646407614,0.0425203216200328));
#36907=CARTESIAN_POINT('',(-0.00518846589550756,0.0184570621158076,0.0424920811195789));
#36908=CARTESIAN_POINT('',(-0.00559306625344521,0.0181643680587182,0.0427010104062051));
#36909=CARTESIAN_POINT('',(-0.00559697087728178,0.0181631679712986,0.0425322025701378));
#36910=CARTESIAN_POINT('',(-0.00564672406313777,0.0183220802758641,0.0425039016870662));
#36911=CARTESIAN_POINT('',(-0.0064957694573478,0.0178614567223671,0.04272477133892));
#36912=CARTESIAN_POINT('',(-0.00649960558446819,0.0178600593602805,0.042556107270354));
#36913=CARTESIAN_POINT('',(-0.00655720284798014,0.0180161278563503,0.0425276908777702));
#36914=CARTESIAN_POINT('',(-0.00694126016116529,0.0176930038061895,0.0427366525222747));
#36915=CARTESIAN_POINT('',(-0.00694509541752452,0.0176915006586277,0.0425680564301373));
#36916=CARTESIAN_POINT('',(-0.00700652501390227,0.0178460130912245,0.0425395854091972));
#36917=CARTESIAN_POINT('',(-0.00824820177693959,0.0171423765181543,0.0427721357638053));
#36918=CARTESIAN_POINT('',(-0.008251790548277,0.0171406392387208,0.0426036659013395));
#36919=CARTESIAN_POINT('',(-0.00832471646847662,0.0172900888841845,0.0425750947903131));
#36920=CARTESIAN_POINT('',(-0.00908546781664353,0.0167134730961815,0.0427957318040787));
#36921=CARTESIAN_POINT('',(-0.00908936767614809,0.0167113403149665,0.0426272517131758));
#36922=CARTESIAN_POINT('',(-0.00916921216002814,0.0168572372731341,0.0425986870535596));
#36923=CARTESIAN_POINT('',(-0.0102909999685144,0.0159786356346231,0.0428313901050363));
#36924=CARTESIAN_POINT('',(-0.0102945991898559,0.0159763194692739,0.0426627520459007));
#36925=CARTESIAN_POINT('',(-0.0103852063330003,0.0161158016210226,0.0426343153725058));
#36926=CARTESIAN_POINT('',(-0.010684414992981,0.0157183797799352,0.0428433157318564));
#36927=CARTESIAN_POINT('',(-0.0106879657483226,0.0157159640201062,0.0426746099673093));
#36928=CARTESIAN_POINT('',(-0.0107820427352414,0.0158532295056831,0.0426462276658231));
#36929=CARTESIAN_POINT('',(-0.0114540765240435,0.0151666844639779,0.0428672547991974));
#36930=CARTESIAN_POINT('',(-0.0114575030590412,0.0151640988461154,0.0426984283455806));
#36931=CARTESIAN_POINT('',(-0.0115583793013117,0.0152966179800366,0.0426701429484309));
#36932=CARTESIAN_POINT('',(-0.0118318566377774,0.0148738979658878,0.0428793194454723));
#36933=CARTESIAN_POINT('',(-0.0118351611856566,0.0148712686395132,0.0427104387051855));
#36934=CARTESIAN_POINT('',(-0.0119394263670495,0.0150012189785698,0.0426821971437567));
#36935=CARTESIAN_POINT('',(-0.0129246431482226,0.0139590933902365,0.0429151506839148));
#36936=CARTESIAN_POINT('',(-0.0129277296762079,0.013956235532516,0.0427462529203825));
#36937=CARTESIAN_POINT('',(-0.0130415327640104,0.0140781574671,0.042718023992381));
#36938=CARTESIAN_POINT('',(-0.0135998275021078,0.0133014626056276,0.042938562210487));
#36939=CARTESIAN_POINT('',(-0.013602575516219,0.0132986712873312,0.0427698376504481));
#36940=CARTESIAN_POINT('',(-0.0137223200965974,0.0134144441308818,0.0427414706275737));
#36941=CARTESIAN_POINT('',(-0.0148467549202409,0.0118936152566955,0.0429855619714583));
#36942=CARTESIAN_POINT('',(-0.0148491996917421,0.011890543812061,0.0428170568736124));
#36943=CARTESIAN_POINT('',(-0.0149796173886599,0.0119937802269414,0.0427885140212086));
#36944=CARTESIAN_POINT('',(-0.0154185009886721,0.0111434013612562,0.043009149593558));
#36945=CARTESIAN_POINT('',(-0.0154210574184647,0.0111398501006241,0.0428406940622408));
#36946=CARTESIAN_POINT('',(-0.0155561398607172,0.0112368259946476,0.0428121097777485));
#36947=CARTESIAN_POINT('',(-0.0161957093387957,0.00994612440462015,0.04304515280486));
#36948=CARTESIAN_POINT('',(-0.0161979399841593,0.00994249463749885,0.0428765797355238));
#36949=CARTESIAN_POINT('',(-0.0163399589840616,0.0100289293449728,0.0428480908890324));
#36950=CARTESIAN_POINT('',(-0.0164400593245126,0.00953667116451164,0.0430572012611153));
#36951=CARTESIAN_POINT('',(-0.0164422174803105,0.00953294684637346,0.042888565959774));
#36952=CARTESIAN_POINT('',(-0.0165864061706359,0.00961586280349823,0.0428601269980955));
#36953=CARTESIAN_POINT('',(-0.016894147383795,0.00870697603465936,0.0430811362951355));
#36954=CARTESIAN_POINT('',(-0.0168961245689515,0.0087031443145647,0.0429123604322927));
#36955=CARTESIAN_POINT('',(-0.0170443990829768,0.00877885858332786,0.042884034500655));
#36956=CARTESIAN_POINT('',(-0.0171048065348784,0.00828534182490399,0.0430930647472596));
#36957=CARTESIAN_POINT('',(-0.0171066764884509,0.00828147746536018,0.0429242109612949));
#36958=CARTESIAN_POINT('',(-0.0172568737159689,0.00835351582487844,0.0428959477698145));
#36959=CARTESIAN_POINT('',(-0.017688402759418,0.00700039933326027,0.043128724510894));
#36960=CARTESIAN_POINT('',(-0.0176900583888289,0.0069962481391462,0.0429597124205211));
#36961=CARTESIAN_POINT('',(-0.0178454143940276,0.00705725387080521,0.042931575254563));
#36962=CARTESIAN_POINT('',(-0.0180132271233088,0.00611715943804409,0.0431522198964858));
#36963=CARTESIAN_POINT('',(-0.0180144803111107,0.00611351968480371,0.0429832705912268));
#36964=CARTESIAN_POINT('',(-0.0181727669051138,0.0061661772908184,0.0429550848131308));
#36965=CARTESIAN_POINT('',(-0.0184023284969058,0.00475166324970116,0.0431876550859494));
#36966=CARTESIAN_POINT('',(-0.0184033474459008,0.00474770852564244,0.043018925065945));
#36967=CARTESIAN_POINT('',(-0.018564689450059,0.00478855747754072,0.0429905616050906));
#36968=CARTESIAN_POINT('',(-0.018515972453872,0.0042877361244035,0.0431995615620718));
#36969=CARTESIAN_POINT('',(-0.0185168995642598,0.00428374021123731,0.0430309075356459));
#36970=CARTESIAN_POINT('',(-0.0186791254983124,0.00432051716027729,0.0430024830057629));
#36971=CARTESIAN_POINT('',(-0.0187072033441742,0.00335655478501059,0.0432233179844061));
#36972=CARTESIAN_POINT('',(-0.0187079274872983,0.00335251021259686,0.0430547756581805));
#36973=CARTESIAN_POINT('',(-0.0188716668817317,0.00338110383995676,0.0430262617061117));
#36974=CARTESIAN_POINT('',(-0.0187848419957819,0.00288997040124032,0.0432351521775762));
#36975=CARTESIAN_POINT('',(-0.0187854765891899,0.00288584828394335,0.0430666473531019));
#36976=CARTESIAN_POINT('',(-0.0189498247619837,0.00291040610459593,0.0430381032284253));
#36977=CARTESIAN_POINT('',(-0.0189651462740219,0.00148731224398622,0.0432706566150148));
#36978=CARTESIAN_POINT('',(-0.0189654708666694,0.00148315793899136,0.0431021765175295));
#36979=CARTESIAN_POINT('',(-0.019131318753891,0.00149540950004909,0.0430736132395977));
#36980=CARTESIAN_POINT('',(-0.0190154832834067,0.000548349506278168,0.0432943453252847));
#36981=CARTESIAN_POINT('',(-0.0190155990614365,0.000543835601436554,0.0431257663874186));
#36982=CARTESIAN_POINT('',(-0.0191819768803391,0.000548218567437135,0.0430972810643009));
#36983=CARTESIAN_POINT('',(-0.0189861153355352,-0.000865879544968052,0.0433301138001482));
#36984=CARTESIAN_POINT('',(-0.018985921377837,-0.000870172708024659,0.0431613409049158));
#36985=CARTESIAN_POINT('',(-0.0191522017187679,-0.000878390970992399,0.0431330125099441));
#36986=CARTESIAN_POINT('',(-0.018958776420447,-0.00133825739454921,0.0433420716187868));
#36987=CARTESIAN_POINT('',(-0.018958475476988,-0.00134250478669942,0.0431732337615662));
#36988=CARTESIAN_POINT('',(-0.0191245742056541,-0.00135490145970564,0.0431449577125661));
#36989=CARTESIAN_POINT('',(-0.0188680924290746,-0.00228499984736558,0.0433660434476357));
#36990=CARTESIAN_POINT('',(-0.018867583315166,-0.00228920930196638,0.0431971440969443));
#36991=CARTESIAN_POINT('',(-0.0190329223973134,-0.00230990336534812,0.0431689170616229));
#36992=CARTESIAN_POINT('',(-0.018804704452073,-0.00275806485483265,0.0433780088934093));
#36993=CARTESIAN_POINT('',(-0.0188041057185145,-0.00276215519583305,0.0432091237363117));
#36994=CARTESIAN_POINT('',(-0.0189688397708669,-0.00278708086793507,0.043180885340923));
#36995=CARTESIAN_POINT('',(-0.0185638443092955,-0.00415680280424106,0.0434135137709053));
#36996=CARTESIAN_POINT('',(-0.0185629695552276,-0.0041606564775658,0.0432447642656287));
#36997=CARTESIAN_POINT('',(-0.0187253545087216,-0.00419796417403942,0.0432164170789741));
#36998=CARTESIAN_POINT('',(-0.0183353368812342,-0.00506959719009099,0.0434368961714605));
#36999=CARTESIAN_POINT('',(-0.0183342669764093,-0.00507349342334267,0.0432683174256558));
#37000=CARTESIAN_POINT('',(-0.0184944243935023,-0.00511864724285449,0.0432398328593739));
#37001=CARTESIAN_POINT('',(-0.0178923697591036,-0.00640971551303542,0.0434722602728136));
#37002=CARTESIAN_POINT('',(-0.0178909687343637,-0.00641362442053553,0.043303769684843));
#37003=CARTESIAN_POINT('',(-0.018047139167788,-0.00647035981594991,0.0432752143871632));
#37004=CARTESIAN_POINT('',(-0.0177279437193191,-0.00685155606459969,0.043484092904052));
#37005=CARTESIAN_POINT('',(-0.0177264219885323,-0.00685549210929144,0.0433156079658385));
#37006=CARTESIAN_POINT('',(-0.0178811548515406,-0.00691602627884074,0.0432870480313056));
#37007=CARTESIAN_POINT('',(-0.0173649907948434,-0.00772534165695619,0.0435079218054287));
#37008=CARTESIAN_POINT('',(-0.0173632699341338,-0.00772921190972498,0.0433393911381997));
#37009=CARTESIAN_POINT('',(-0.0175148451097775,-0.00779739418046767,0.0433108682260294));
#37010=CARTESIAN_POINT('',(-0.017165602484246,-0.00815893710550448,0.0435199651766935));
#37011=CARTESIAN_POINT('',(-0.0171637581683695,-0.00816281321507147,0.043351385511468));
#37012=CARTESIAN_POINT('',(-0.0173136504702881,-0.00823476080683952,0.0433229018136475));
#37013=CARTESIAN_POINT('',(-0.0165210940987345,-0.009431760341298,0.043556046947235));
#37014=CARTESIAN_POINT('',(-0.0165188567241586,-0.00943571101744704,0.0433872789874135));
#37015=CARTESIAN_POINT('',(-0.0166633643727174,-0.00951867007146015,0.0433589456373712));
#37016=CARTESIAN_POINT('',(-0.0160329494926047,-0.0102385897110408,0.0435799136272656));
#37017=CARTESIAN_POINT('',(-0.0160306646401609,-0.0102421644523927,0.0434109413536699));
#37018=CARTESIAN_POINT('',(-0.0161709217927998,-0.0103325643479168,0.0433827738611434));
#37019=CARTESIAN_POINT('',(-0.0149436602822656,-0.0117716271632975,0.0436271814331457));
#37020=CARTESIAN_POINT('',(-0.0149410707316043,-0.0117749125269769,0.043458203402268));
#37021=CARTESIAN_POINT('',(-0.0150717262175193,-0.0118787143429182,0.0434300391083153));
#37022=CARTESIAN_POINT('',(-0.0143425139356339,-0.0124978339573583,0.0436505840409847));
#37023=CARTESIAN_POINT('',(-0.0143399871796448,-0.0125007572524888,0.0434817939080769));
#37024=CARTESIAN_POINT('',(-0.0144649508075557,-0.0126109912636555,0.0434534797499));
#37025=CARTESIAN_POINT('',(-0.013353254765621,-0.0135246618097943,0.043686185188991));
#37026=CARTESIAN_POINT('',(-0.0133503403783537,-0.0135275366571819,0.0435175966304388));
#37027=CARTESIAN_POINT('',(-0.0134666009456983,-0.013646403549451,0.0434891196980371));
#37028=CARTESIAN_POINT('',(-0.0130091106488293,-0.013855939438497,0.0436981192445647));
#37029=CARTESIAN_POINT('',(-0.0130060880561487,-0.0138587784869067,0.0435295834038134));
#37030=CARTESIAN_POINT('',(-0.0131193165195436,-0.0139804517481268,0.0435010640960348));
#37031=CARTESIAN_POINT('',(-0.0123030784965075,-0.014486486016476,0.0437218476773994));
#37032=CARTESIAN_POINT('',(-0.0122999076233398,-0.0144891782747915,0.0435533603286156));
#37033=CARTESIAN_POINT('',(-0.0124068999056232,-0.0146162992716977,0.0435248024699253));
#37034=CARTESIAN_POINT('',(-0.011939825755397,-0.0147872234611433,0.0437336919390996));
#37035=CARTESIAN_POINT('',(-0.0119365362629715,-0.0147898787470809,0.0435652034709374));
#37036=CARTESIAN_POINT('',(-0.0120403900735433,-0.0149195795744518,0.0435366464007867));
#37037=CARTESIAN_POINT('',(-0.0108198925979776,-0.0156465840107142,0.0437692594703814));
#37038=CARTESIAN_POINT('',(-0.0108163199250364,-0.0156490630775139,0.0436006916153784));
#37039=CARTESIAN_POINT('',(-0.0109104810471308,-0.0157862543759804,0.0435721982202406));
#37040=CARTESIAN_POINT('',(-0.0100332035243057,-0.0161625907830607,0.0437930330870528));
#37041=CARTESIAN_POINT('',(-0.0100294118999466,-0.0161649308481875,0.0436243007810868));
#37042=CARTESIAN_POINT('',(-0.0101168709807266,-0.0163067379621374,0.0435959391586223));
#37043=CARTESIAN_POINT('',(-0.00879216804478874,-0.0168499676414349,0.0438288524583594));
#37044=CARTESIAN_POINT('',(-0.00878838298714177,-0.0168519440507585,0.0436599726789626));
#37045=CARTESIAN_POINT('',(-0.00886488046311359,-0.016999950121302,0.0436317300461986));
#37046=CARTESIAN_POINT('',(-0.00836678386397909,-0.0170652673611714,0.0438408466943254));
#37047=CARTESIAN_POINT('',(-0.00836304432866484,-0.0170671014593458,0.0436719450370716));
#37048=CARTESIAN_POINT('',(-0.00843573579653323,-0.0172170398082215,0.0436437200774922));
#37049=CARTESIAN_POINT('',(-0.0075020610771226,-0.017462688851661,0.0438646944908298));
#37050=CARTESIAN_POINT('',(-0.00749825266116855,-0.0174643237639204,0.0436958505787912));
#37051=CARTESIAN_POINT('',(-0.00756332366407398,-0.0176176520556874,0.0436675786878873));
#37052=CARTESIAN_POINT('',(-0.00706477335026738,-0.0176440200780838,0.0438765091448451));
#37053=CARTESIAN_POINT('',(-0.00706096804890941,-0.0176455456634563,0.0437077276210945));
#37054=CARTESIAN_POINT('',(-0.00712213400549059,-0.0178003908836544,0.0436794056320971));
#37055=CARTESIAN_POINT('',(-0.00573852163197963,-0.0181372334578677,0.0439118465916292));
#37056=CARTESIAN_POINT('',(-0.00573481921426324,-0.0181383895346569,0.043743248215973));
#37057=CARTESIAN_POINT('',(-0.00578406965445588,-0.0182973783030603,0.0437147801112202));
#37058=CARTESIAN_POINT('',(-0.00483524655341389,-0.0183986073071731,0.0439352782854798));
#37059=CARTESIAN_POINT('',(-0.00483116852585073,-0.018399678078592,0.0437667982660677));
#37060=CARTESIAN_POINT('',(-0.00487278496604438,-0.0185606870996588,0.0437382340115492));
#37061=CARTESIAN_POINT('',(-0.00345175988030525,-0.018689768424132,0.0439708278229095));
#37062=CARTESIAN_POINT('',(-0.00344762002299385,-0.0186905334044925,0.0438023259722786));
#37063=CARTESIAN_POINT('',(-0.00347710746122709,-0.0188540666261451,0.0437737798863077));
#37064=CARTESIAN_POINT('',(-0.00298581589560767,-0.0187699373373264,0.0439827406953793));
#37065=CARTESIAN_POINT('',(-0.0029815945202669,-0.0187706073743282,0.0438142055341818));
#37066=CARTESIAN_POINT('',(-0.00300706790601135,-0.0189348569344595,0.0437856860537803));
#37067=CARTESIAN_POINT('',(-0.00204413509094533,-0.0188956914649766,0.0440067439405659));
#37068=CARTESIAN_POINT('',(-0.0020398726024733,-0.0188961543529943,0.0438380990315092));
#37069=CARTESIAN_POINT('',(-0.00205712019075991,-0.0190615944017183,0.043809667889534));
#37070=CARTESIAN_POINT('',(-0.00156830996680276,-0.0189410826500961,0.0440188361973977));
#37071=CARTESIAN_POINT('',(-0.00156401312848831,-0.0189414363423515,0.0438501166546982));
#37072=CARTESIAN_POINT('',(-0.00157712255868106,-0.0191073458819795,0.0438217454397834));
#37073=CARTESIAN_POINT('',(-0.000150154974504012,-0.0190229936109595,0.0440547882027781));
#37074=CARTESIAN_POINT('',(-0.000145588323455347,-0.0190230462400798,0.0438858608428633));
#37075=CARTESIAN_POINT('',(-0.000146539257022446,-0.0191898518619688,0.0438576554283318));
#37076=CARTESIAN_POINT('',(0.000790936627636269,-0.019006824755411,0.0440784751545746));
#37077=CARTESIAN_POINT('',(0.00079488815217747,-0.0190066717643781,0.0439094489159697));
#37078=CARTESIAN_POINT('',(0.000802778280913555,-0.0191733936965734,0.0438813251670424));
#37079=CARTESIAN_POINT('',(0.00219618132025848,-0.018878507081242,0.0441137553179732));
#37080=CARTESIAN_POINT('',(0.00220026426151477,-0.0188780303767659,0.0439448926290359));
#37081=CARTESIAN_POINT('',(0.00222026970006894,-0.0190434097462471,0.0439166358100154));
#37082=CARTESIAN_POINT('',(0.00266352565200299,-0.0188183179147578,0.044125500051272));
#37083=CARTESIAN_POINT('',(0.00266757183132161,-0.0188177472930563,0.0439567138470368));
#37084=CARTESIAN_POINT('',(0.00269168007756433,-0.0189824858408622,0.0439283955500007));
#37085=CARTESIAN_POINT('',(0.00359603759486174,-0.0186625821272436,0.0441490943401665));
#37086=CARTESIAN_POINT('',(0.00360004882176565,-0.0186618071442378,0.0439804491106465));
#37087=CARTESIAN_POINT('',(0.00363229267182523,-0.0188249870752841,0.0439520176016581));
#37088=CARTESIAN_POINT('',(0.00406249693166183,-0.018566712268401,0.0441609772952625));
#37089=CARTESIAN_POINT('',(0.00406652662148846,-0.0185658318754706,0.0439923969852757));
#37090=CARTESIAN_POINT('',(0.00410279819761283,-0.0187280858111682,0.0439639133116328));
#37091=CARTESIAN_POINT('',(0.0054497458441839,-0.0182265469396486,0.0441967294346886));
#37092=CARTESIAN_POINT('',(0.00545358262028542,-0.0182253907484344,0.0440282635270871));
#37093=CARTESIAN_POINT('',(0.00550208037506834,-0.0183844526912413,0.043999689222396));
#37094=CARTESIAN_POINT('',(0.0063465881321194,-0.0179333509087761,0.0442204124173489));
#37095=CARTESIAN_POINT('',(0.00635078959146271,-0.0179318513293681,0.044051922194549));
#37096=CARTESIAN_POINT('',(0.00640671032868024,-0.0180884976215383,0.0440233656430663));
#37097=CARTESIAN_POINT('',(0.00808635138350872,-0.0172190353109135,0.0442679269748748));
#37098=CARTESIAN_POINT('',(0.00809041392297931,-0.017217141719978,0.0440992201967355));
#37099=CARTESIAN_POINT('',(0.00816162287321362,-0.0173677050659826,0.0440708378489379));
#37100=CARTESIAN_POINT('',(0.00892927000815383,-0.0167979099162225,0.0442917541796707));
#37101=CARTESIAN_POINT('',(0.00893299016981508,-0.0167959318351288,0.0441228595101268));
#37102=CARTESIAN_POINT('',(0.00901191021205074,-0.0169428561738456,0.0440946294830747));
#37103=CARTESIAN_POINT('',(0.0101520063527029,-0.0160674259644378,0.0443275330439986));
#37104=CARTESIAN_POINT('',(0.0101555419580498,-0.0160651915313776,0.0441586481003933));
#37105=CARTESIAN_POINT('',(0.0102451320892497,-0.0162056661571703,0.0441304092466795));
#37106=CARTESIAN_POINT('',(0.0105530248471654,-0.0158068996913036,0.044339482773545));
#37107=CARTESIAN_POINT('',(0.0105564418813125,-0.0158046204070512,0.0441706477123562));
#37108=CARTESIAN_POINT('',(0.0106495601594412,-0.0159427075570703,0.0441423688593859));
#37109=CARTESIAN_POINT('',(0.0113276393296575,-0.0152613563778918,0.0443631513426043));
#37110=CARTESIAN_POINT('',(0.0113309294112503,-0.0152589120313818,0.0441944369148397));
#37111=CARTESIAN_POINT('',(0.0114307338273626,-0.0153920774500531,0.0441660609369003));
#37112=CARTESIAN_POINT('',(0.0117029764469784,-0.0149753766232204,0.0443749201640164));
#37113=CARTESIAN_POINT('',(0.0117062142264097,-0.014972848377937,0.044206274963219));
#37114=CARTESIAN_POINT('',(0.0118092359999567,-0.0151034343162899,0.0441778433696202));
#37115=CARTESIAN_POINT('',(0.0127937553720812,-0.0140785679095087,0.0444102184577515));
#37116=CARTESIAN_POINT('',(0.0127966613896774,-0.0140759112274443,0.0442417266093446));
#37117=CARTESIAN_POINT('',(0.0129092222992875,-0.0141983513220654,0.0442131731350139));
#37118=CARTESIAN_POINT('',(0.0134741569144895,-0.0134290820888552,0.0444337558421312));
#37119=CARTESIAN_POINT('',(0.0134772527320605,-0.0134259630804598,0.0442653011928489));
#37120=CARTESIAN_POINT('',(0.0135953916495663,-0.0135429841222457,0.0442367161687069));
#37121=CARTESIAN_POINT('',(0.0144237533789395,-0.0123765353003134,0.0444695263456117));
#37122=CARTESIAN_POINT('',(0.0144265326456636,-0.0123732984504774,0.0443009422857109));
#37123=CARTESIAN_POINT('',(0.0145531437809366,-0.0124810665665217,0.044272462273439));
#37124=CARTESIAN_POINT('',(0.014728973698961,-0.0120118394212612,0.0444815468308796));
#37125=CARTESIAN_POINT('',(0.0147316951565146,-0.0120084990933084,0.0443128975475059));
#37126=CARTESIAN_POINT('',(0.014861002078107,-0.0121131453026525,0.0442844698258981));
#37127=CARTESIAN_POINT('',(0.0153124435690708,-0.0112585978012749,0.0445056611452321));
#37128=CARTESIAN_POINT('',(0.0153150013476016,-0.0112551227366345,0.0443368677121805));
#37129=CARTESIAN_POINT('',(0.0154495190689251,-0.0113532550497856,0.0443085558935153));
#37130=CARTESIAN_POINT('',(0.0155882444401666,-0.0108733330355269,0.044517651274913));
#37131=CARTESIAN_POINT('',(0.015590696367927,-0.0108698150645401,0.0443487801060638));
#37132=CARTESIAN_POINT('',(0.0157277077512303,-0.0109645953864914,0.0443205309058317));
#37133=CARTESIAN_POINT('',(0.0163691710964169,-0.00969232591939088,0.0445534115306125));
#37134=CARTESIAN_POINT('',(0.0163714464651926,-0.0096885044715376,0.0443843937751832));
#37135=CARTESIAN_POINT('',(0.0165153057183266,-0.00977314734794248,0.0443562611772637));
#37136=CARTESIAN_POINT('',(0.0168280705761621,-0.0088715031155409,0.0445768634194298));
#37137=CARTESIAN_POINT('',(0.0168298773963543,-0.00886811101355751,0.0444079315425907));
#37138=CARTESIAN_POINT('',(0.0169779056880622,-0.00894497234046972,0.0443797317026779));
#37139=CARTESIAN_POINT('',(0.0174243664825587,-0.00759034481382917,0.0446121254669567));
#37140=CARTESIAN_POINT('',(0.0174259949050814,-0.00758660128298118,0.0444434164716655));
#37141=CARTESIAN_POINT('',(0.0175788687236481,-0.0076523374825775,0.0444150361200228));
#37142=CARTESIAN_POINT('',(0.0176077269712503,-0.00715493768044318,0.044623902971559));
#37143=CARTESIAN_POINT('',(0.0176092735419983,-0.00715113617066766,0.0444552686054724));
#37144=CARTESIAN_POINT('',(0.0177636450242175,-0.00721303680883226,0.0444268282888931));
#37145=CARTESIAN_POINT('',(0.0179429471430136,-0.00626704317267242,0.0446476246433377));
#37146=CARTESIAN_POINT('',(0.0179443015041592,-0.00626316109002529,0.0444790985861339));
#37147=CARTESIAN_POINT('',(0.0181014572970104,-0.00631723472224765,0.0444505715980682));
#37148=CARTESIAN_POINT('',(0.0180949724965274,-0.00581348313029633,0.0446595961907196));
#37149=CARTESIAN_POINT('',(0.0180962497503941,-0.00580950869140011,0.0444911054619768));
#37150=CARTESIAN_POINT('',(0.0182546606191797,-0.00585965097994928,0.0444625500480985));
#37151=CARTESIAN_POINT('',(0.0184959816576352,-0.00444939608775399,0.0446953019660419));
#37152=CARTESIAN_POINT('',(0.018496958849312,-0.00444533144179018,0.0445268281214257));
#37153=CARTESIAN_POINT('',(0.0186588124479543,-0.00448350568352277,0.0444982597993328));
#37154=CARTESIAN_POINT('',(0.0186931222678959,-0.00352871098495351,0.0447190290468711));
#37155=CARTESIAN_POINT('',(0.0186939437072589,-0.00352428564961369,0.0445504499253981));
#37156=CARTESIAN_POINT('',(0.0188575680062124,-0.00355473555155383,0.0445219648388717));
#37157=CARTESIAN_POINT('',(0.0189502365720984,-0.00166527931571346,0.0447665822341533));
#37158=CARTESIAN_POINT('',(0.018950644510258,-0.00166079385680507,0.0445977639216191));
#37159=CARTESIAN_POINT('',(0.019116722434608,-0.00167496209543366,0.0445694709399891));
#37160=CARTESIAN_POINT('',(0.0190102135009348,-0.000721603842810055,0.0447903421458515));
#37161=CARTESIAN_POINT('',(0.0190103745399458,-0.000717601730914487,0.0446214564980412));
#37162=CARTESIAN_POINT('',(0.0191770421900481,-0.000723030408788185,0.044593219240517));
#37163=CARTESIAN_POINT('',(0.018986960795852,0.0011850102083368,0.0448380670765952));
#37164=CARTESIAN_POINT('',(0.0189867025259235,0.00118898747267436,0.0446693435332347));
#37165=CARTESIAN_POINT('',(0.019152908993654,0.00120026015000668,0.0446409755342579));
#37166=CARTESIAN_POINT('',(0.0189041423152777,0.00212551926781839,0.0448615838243566));
#37167=CARTESIAN_POINT('',(0.0189036821317303,0.00212963503647161,0.0446929831128389));
#37168=CARTESIAN_POINT('',(0.0190689879037131,0.00214897360311979,0.0446645159522766));
#37169=CARTESIAN_POINT('',(0.0186018416989233,0.00398194854842917,0.0449088004107678));
#37170=CARTESIAN_POINT('',(0.0186009686985388,0.00398601997834442,0.0447402351269411));
#37171=CARTESIAN_POINT('',(0.0187635204626675,0.00402158525230051,0.0447117401013397));
#37172=CARTESIAN_POINT('',(0.018382348236366,0.00489786678679497,0.0449324980666317));
#37173=CARTESIAN_POINT('',(0.0183811758465752,0.00490221341614218,0.0447638576997983));
#37174=CARTESIAN_POINT('',(0.0185419608917838,0.00494549245887479,0.0447354216516968));
#37175=CARTESIAN_POINT('',(0.0179479062185708,0.00625280887325386,0.0449684687154362));
#37176=CARTESIAN_POINT('',(0.0179464943902665,0.0062568668598083,0.0447996428701011));
#37177=CARTESIAN_POINT('',(0.0181035577501198,0.00631225917213096,0.0447713570828861));
#37178=CARTESIAN_POINT('',(0.0177848319526543,0.00670258003035173,0.0449805623302665));
#37179=CARTESIAN_POINT('',(0.0177833220738104,0.0067065823745434,0.044811669837172));
#37180=CARTESIAN_POINT('',(0.0179390092271524,0.00676595516139307,0.0447834377416771));
#37181=CARTESIAN_POINT('',(0.0174283660129482,0.00758135111745522,0.0450045007790738));
#37182=CARTESIAN_POINT('',(0.0174266647478471,0.00758526492612676,0.044835520321406));
#37183=CARTESIAN_POINT('',(0.0175792882272123,0.00765236524299947,0.0448073587601778));
#37184=CARTESIAN_POINT('',(0.0172345799272952,0.00801192762887884,0.0450163802018326));
#37185=CARTESIAN_POINT('',(0.0172328260256429,0.00801570218315257,0.0448473807885217));
#37186=CARTESIAN_POINT('',(0.0173837160900334,0.00808665880559119,0.044819234475737));
#37187=CARTESIAN_POINT('',(0.0166075233603181,0.00927777377603944,0.0450517759664179));
#37188=CARTESIAN_POINT('',(0.0166055475967738,0.00928129451252952,0.0448828660892816));
#37189=CARTESIAN_POINT('',(0.0167507482423559,0.00936337902246387,0.0448546477246791));
#37190=CARTESIAN_POINT('',(0.0161288042341429,0.0100872971570167,0.045075201634086));
#37191=CARTESIAN_POINT('',(0.0161265818413747,0.0100908515680599,0.044906415077906));
#37192=CARTESIAN_POINT('',(0.0162675033284656,0.0101798132291225,0.0448780970874073));
#37193=CARTESIAN_POINT('',(0.0150489933465771,0.011636996571794,0.0451226650624829));
#37194=CARTESIAN_POINT('',(0.0150464140875462,0.0116403332888076,0.044953877202022));
#37195=CARTESIAN_POINT('',(0.0151778180517796,0.0117428355520045,0.0449255608731273));
#37196=CARTESIAN_POINT('',(0.0144429210201034,0.0123812019000766,0.0451468654392096));
#37197=CARTESIAN_POINT('',(0.0144400888394576,0.0123844959594197,0.0449779557783555));
#37198=CARTESIAN_POINT('',(0.0145663435705823,0.0124935061387918,0.0449497372028042));
#37199=CARTESIAN_POINT('',(0.0134685515906739,0.01340974086514,0.0451825562446273));
#37200=CARTESIAN_POINT('',(0.0134655641188587,0.0134127421838492,0.0450135709211634));
#37201=CARTESIAN_POINT('',(0.0135832408374368,0.0135308531692142,0.044985413154267));
#37202=CARTESIAN_POINT('',(0.0131321446070276,0.0137392811386444,0.0451945442673237));
#37203=CARTESIAN_POINT('',(0.0131256289439562,0.0137453916307771,0.0450257518235694));
#37204=CARTESIAN_POINT('',(0.0132431889465559,0.0138637230531154,0.0449973950606197));
#37205=CARTESIAN_POINT('',(0.0124364953824679,0.0143720092815323,0.0452251638180739));
#37206=CARTESIAN_POINT('',(0.0124288742620619,0.0143787537513585,0.0450495329495826));
#37207=CARTESIAN_POINT('',(0.0125454954734933,0.014508430361355,0.045026887812166));
#37208=CARTESIAN_POINT('',(0.0120772417837534,0.0146752127027321,0.0452428101759807));
#37209=CARTESIAN_POINT('',(0.0120638269525999,0.0146858875331522,0.0450611716033226));
#37210=CARTESIAN_POINT('',(0.0121871631803304,0.0148195625152073,0.0450435765026652));
#37211=CARTESIAN_POINT('',(0.0117064311150657,0.0149652754918919,0.0452574848572202));
#37212=CARTESIAN_POINT('',(0.0117017888431181,0.0149689068608435,0.0450664117380016));
#37213=CARTESIAN_POINT('',(0.0118192405672073,0.0151194868273913,0.045057783841377));
#37214=CARTESIAN_POINT('',(0.0135722303973856,0.013533541237196,0.0359858240518714));
#37215=CARTESIAN_POINT('',(0.013571622451412,0.0135341506939564,0.0359858446287144));
#37216=CARTESIAN_POINT('',(0.0135710144649558,0.0135347601152105,0.0359858652089559));
#37217=CARTESIAN_POINT('',(0.0135704064380024,0.0135353695009377,0.0359858857925812));
#37218=CARTESIAN_POINT('',(0.013570381808041,0.0135353510208532,0.0359857053491133));
#37219=CARTESIAN_POINT('',(0.0135722054159049,0.0135335224965762,0.0359856410406521));
#37220=CARTESIAN_POINT('',(0.0135704064380024,0.0135353695009377,0.0359858857925812));
#37221=CARTESIAN_POINT('',(0.0129036548070887,0.0142025964264844,0.0360085613545014));
#37222=CARTESIAN_POINT('',(0.0114611542483502,0.015448287166601,0.0360565775520735));
#37223=CARTESIAN_POINT('',(0.00909268102828358,0.0169514288058979,0.0361261820467452));
#37224=CARTESIAN_POINT('',(0.00647950090834531,0.0181120230886494,0.0361973328999772));
#37225=CARTESIAN_POINT('',(0.00287123768415439,0.0191126352245148,0.0362904101950139));
#37226=CARTESIAN_POINT('',(-0.000949677653458001,0.0193040117092425,0.036383990993209));
#37227=CARTESIAN_POINT('',(-0.00465102395568895,0.0186649672159626,0.0364775817539468));
#37228=CARTESIAN_POINT('',(-0.00735877861404485,0.0177724795978704,0.0365488480499061));
#37229=CARTESIAN_POINT('',(-0.00986237510046936,0.0165149149662214,0.0366178923756543));
#37230=CARTESIAN_POINT('',(-0.0122031927539453,0.0148689465492879,0.0366889731522299));
#37231=CARTESIAN_POINT('',(-0.0142334523316336,0.0129392989422766,0.036759211703248));
#37232=CARTESIAN_POINT('',(-0.0165756388821674,0.00994417572451643,0.0368531214084936));
#37233=CARTESIAN_POINT('',(-0.0181924746613863,0.00652957200048769,0.0369463139710774));
#37234=CARTESIAN_POINT('',(-0.0190261366639813,0.00283095697289045,0.037040783606513));
#37235=CARTESIAN_POINT('',(-0.0192356036156563,3.10245497638384E-5,0.0371099791765328));
#37236=CARTESIAN_POINT('',(-0.0190276609287275,-0.00281986751540245,0.0371812491961335));
#37237=CARTESIAN_POINT('',(-0.0184175486612505,-0.00555180159649675,0.0372512868433642));
#37238=CARTESIAN_POINT('',(-0.0173909007355282,-0.00821999643371724,0.0373217709207786));
#37239=CARTESIAN_POINT('',(-0.0155472357929439,-0.0114804485039055,0.0374146763836055));
#37240=CARTESIAN_POINT('',(-0.0129812711275626,-0.0143196448224917,0.0375095754402841));
#37241=CARTESIAN_POINT('',(-0.00991561226323179,-0.0164827729265894,0.0376021168106601));
#37242=CARTESIAN_POINT('',(-0.00736738918219378,-0.0177687876227372,0.0376735234568528));
#37243=CARTESIAN_POINT('',(-0.00470947524897598,-0.0186507963509578,0.0377433369936091));
#37244=CARTESIAN_POINT('',(-0.00189108857945936,-0.0191423871997642,0.0378138213830228));
#37245=CARTESIAN_POINT('',(0.000910715726981787,-0.0192135649995635,0.0378834946810402));
#37246=CARTESIAN_POINT('',(0.00468277998063177,-0.018754393673424,0.0379785967435593));
#37247=CARTESIAN_POINT('',(0.00823984871720905,-0.0174842256403166,0.038070608869898));
#37248=CARTESIAN_POINT('',(0.0114487135063291,-0.0154576187460385,0.0381657497589623));
#37249=CARTESIAN_POINT('',(0.0135750376321758,-0.0136288998762221,0.0382353373342439));
#37250=CARTESIAN_POINT('',(0.0154455607200755,-0.0114643757136311,0.0383058925721234));
#37251=CARTESIAN_POINT('',(0.0169460544911987,-0.00910137325776664,0.0383756965966336));
#37252=CARTESIAN_POINT('',(0.0181079837303313,-0.0064910253901214,0.0384470673278848));
#37253=CARTESIAN_POINT('',(0.0191108011877866,-0.00287969512756302,0.0385393341131735));
#37254=CARTESIAN_POINT('',(0.0193047752323962,0.000942482875310808,0.0386346426198504));
#37255=CARTESIAN_POINT('',(0.0186685396227,0.00463742868741877,0.0387273673272984));
#37256=CARTESIAN_POINT('',(0.0177752289363512,0.00735055566752598,0.0387979645948326));
#37257=CARTESIAN_POINT('',(0.0165206086502515,0.00985311295239786,0.0388679691965797));
#37258=CARTESIAN_POINT('',(0.0148766674473921,0.0121949490591136,0.0389391342272032));
#37259=CARTESIAN_POINT('',(0.01294505238683,0.0142268795201651,0.0390082266480041));
#37260=CARTESIAN_POINT('',(0.0099567045497623,0.0165679247808239,0.0391030670710161));
#37261=CARTESIAN_POINT('',(0.0065426543257601,0.0181884803449958,0.0391960410642187));
#37262=CARTESIAN_POINT('',(0.00283903174349127,0.0190242081903609,0.0392900399397408));
#37263=CARTESIAN_POINT('',(4.38490655596054E-5,0.0192361688814356,0.0393602697848384));
#37264=CARTESIAN_POINT('',(-0.00281004131304883,0.0190293691514629,0.0394310992984519));
#37265=CARTESIAN_POINT('',(-0.00554232062030348,0.018419201885183,0.0395002744159604));
#37266=CARTESIAN_POINT('',(-0.00820898556038362,0.0173965778160439,0.0395717411832897));
#37267=CARTESIAN_POINT('',(-0.0114742864751092,0.0155529990072777,0.0396650713268737));
#37268=CARTESIAN_POINT('',(-0.0143131630885914,0.0129864061291896,0.0397586567093767));
#37269=CARTESIAN_POINT('',(-0.0164770616490012,0.0099268333205899,0.0398525410597318));
#37270=CARTESIAN_POINT('',(-0.0177649442009733,0.00737585987507787,0.039923028622799));
#37271=CARTESIAN_POINT('',(-0.0186472732982126,0.00471948953200742,0.0399924153858999));
#37272=CARTESIAN_POINT('',(-0.0191420687654524,0.00190205791917451,0.0400641061633313));
#37273=CARTESIAN_POINT('',(-0.0192142413096121,-0.000901990499639644,0.0401336489952851));
#37274=CARTESIAN_POINT('',(-0.0187562485469653,-0.00466875352929895,0.0402272503848521));
#37275=CARTESIAN_POINT('',(-0.0174917918871846,-0.00822819321455465,0.0403213139141897));
#37276=CARTESIAN_POINT('',(-0.0154621346436875,-0.0114408475718349,0.0404149417726169));
#37277=CARTESIAN_POINT('',(-0.0130282697127285,-0.0142774028557637,0.0405080405422995));
#37278=CARTESIAN_POINT('',(-0.00991772725739437,-0.0165898472986663,0.0406038619665578));
#37279=CARTESIAN_POINT('',(-0.00650157038579237,-0.0181024042748644,0.0406960707748711));
#37280=CARTESIAN_POINT('',(-0.00283785189841008,-0.0191212759720652,0.0407913351761265));
#37281=CARTESIAN_POINT('',(0.000937913129849199,-0.0193054515594452,0.0408836654044101));
#37282=CARTESIAN_POINT('',(0.00467025910808451,-0.0186595712437484,0.040978151102671));
#37283=CARTESIAN_POINT('',(0.00733820999792568,-0.0177819060626436,0.0410483768661127));
#37284=CARTESIAN_POINT('',(0.00989155145181529,-0.0164970073708586,0.0411187932842743));
#37285=CARTESIAN_POINT('',(0.0121812338948817,-0.0148866942940362,0.0411882341378734));
#37286=CARTESIAN_POINT('',(0.014253871300758,-0.0129173177050997,0.041259874016993));
#37287=CARTESIAN_POINT('',(0.0165589423148337,-0.00996570506020658,0.0413523505246238));
#37288=CARTESIAN_POINT('',(0.0181987394001929,-0.00650877737202476,0.0414469474664291));
#37289=CARTESIAN_POINT('',(0.0190245583516211,-0.00284627763176505,0.0415404863055993));
#37290=CARTESIAN_POINT('',(0.0192349788993391,-1.59539726163646E-6,0.0416107539642663));
#37291=CARTESIAN_POINT('',(0.0190319275532812,0.00279222673795976,0.0416804834955781));
#37292=CARTESIAN_POINT('',(0.0184075959098026,0.00558491368172862,0.0417520799986338));
#37293=CARTESIAN_POINT('',(0.0174002159456161,0.00819885203171055,0.0418211207893093));
#37294=CARTESIAN_POINT('',(0.0155304117868589,0.0115077766069531,0.0419155436438027));
#37295=CARTESIAN_POINT('',(0.0129942997411232,0.0143099062533922,0.0420092587497652));
#37296=CARTESIAN_POINT('',(0.00989525219106396,0.0164943213741518,0.0421027240848228));
#37297=CARTESIAN_POINT('',(0.00739018379856946,0.0177598494195308,0.0421728334549609));
#37298=CARTESIAN_POINT('',(0.00467632015585543,0.0186587240946092,0.0422440867836995));
#37299=CARTESIAN_POINT('',(0.00191797928105586,0.019139444207654,0.0423130970541599));
#37300=CARTESIAN_POINT('',(-0.000939580996455013,0.0192127314628508,0.0423842646067995));
#37301=CARTESIAN_POINT('',(-0.00465786360752577,0.018757941368385,0.0424780497498932));
#37302=CARTESIAN_POINT('',(-0.00826216839263219,0.0174718493774394,0.0425712861204916));
#37303=CARTESIAN_POINT('',(-0.0114344912440321,0.0154686357718066,0.0426652059172387));
#37304=CARTESIAN_POINT('',(-0.0135973082957804,0.0136059152434581,0.0427360529788289));
#37305=CARTESIAN_POINT('',(-0.0154285214424727,0.0114874784926826,0.0428051467613729));
#37306=CARTESIAN_POINT('',(-0.0169623829047404,0.00907163903114544,0.0428766144053203));
#37307=CARTESIAN_POINT('',(-0.0181003765664633,0.00651102758883087,0.0429466099962544));
#37308=CARTESIAN_POINT('',(-0.0191177805482954,0.00284995029113454,0.043040145704006));
#37309=CARTESIAN_POINT('',(-0.0193076442662596,-0.000922083928633924,0.0431340336701195));
#37310=CARTESIAN_POINT('',(-0.0186616566678583,-0.00466251490238888,0.0432279439783494));
#37311=CARTESIAN_POINT('',(-0.0177855984884859,-0.00732641341906906,0.0432972980389548));
#37312=CARTESIAN_POINT('',(-0.0165026697800636,-0.00988354444963145,0.0433689452125143));
#37313=CARTESIAN_POINT('',(-0.0148934742398978,-0.0121738803150184,0.0434385501993439));
#37314=CARTESIAN_POINT('',(-0.0129255270265096,-0.0142454806427628,0.0435089315675407));
#37315=CARTESIAN_POINT('',(-0.00997363753172828,-0.0165550355305691,0.0436024404412654));
#37316=CARTESIAN_POINT('',(-0.00651591788045801,-0.0181956490664393,0.0436966553566115));
#37317=CARTESIAN_POINT('',(-0.00285917471887072,-0.0190218574159515,0.0437895534176288));
#37318=CARTESIAN_POINT('',(-1.05277131322721E-5,-0.0192359682957396,0.0438611833771685));
#37319=CARTESIAN_POINT('',(0.00278148828475611,-0.0190335330487122,0.0439304599081606));
#37320=CARTESIAN_POINT('',(0.00557400542520404,-0.018410296510478,0.0440011115084237));
#37321=CARTESIAN_POINT('',(0.00819095256643428,-0.0174042318789018,0.0440711755507273));
#37322=CARTESIAN_POINT('',(0.0114970905449255,-0.0155386360544783,0.044165649129919));
#37323=CARTESIAN_POINT('',(0.0142998874984641,-0.0130047891899287,0.044258106598296));
#37324=CARTESIAN_POINT('',(0.0164908396020408,-0.0099029506612536,0.0443533197536154));
#37325=CARTESIAN_POINT('',(0.0177548865816707,-0.00740121656659391,0.0444224149752557));
#37326=CARTESIAN_POINT('',(0.0186560074938801,-0.00468541369120382,0.044493277880731));
#37327=CARTESIAN_POINT('',(0.0191388070731541,-0.00192739063184559,0.0445633351153983));
#37328=CARTESIAN_POINT('',(0.0192136610128768,0.000927057006012885,0.0446341570303284));
#37329=CARTESIAN_POINT('',(0.018759240023971,0.00464974285234913,0.0447269745742573));
#37330=CARTESIAN_POINT('',(0.0174759318076413,0.00825514969859494,0.0448218815682069));
#37331=CARTESIAN_POINT('',(0.0154759249806765,0.0114239507166203,0.0449149351018996));
#37332=CARTESIAN_POINT('',(0.0142331749641786,0.0128696482775912,0.0449616671411353));
#37333=CARTESIAN_POINT('',(0.0135704061500135,0.0135353688366664,0.0449858818020359));
#37334=CARTESIAN_POINT('',(0.0135703818080404,0.0135353510208537,0.0449857053491134));
#37335=CARTESIAN_POINT('',(0.0135704061500135,0.0135353688366664,0.0449858818020359));
#37336=CARTESIAN_POINT('',(0.0135697787646435,0.0135359980612715,0.0449859048203564));
#37337=CARTESIAN_POINT('',(0.0135691513405032,0.0135366272436449,0.0449859278421744));
#37338=CARTESIAN_POINT('',(0.0135685238776161,0.0135372563838022,0.044985950867507));
#37339=CARTESIAN_POINT('',(0.0135684991741454,0.013537238300348,0.0449857717828516));
#37340=CARTESIAN_POINT('',(0.0133154147536411,0.0135536195643592,0.0451879940399793));
#37341=CARTESIAN_POINT('',(0.0133539318946654,0.0135157713941986,0.0451308262115416));
#37342=CARTESIAN_POINT('',(0.0134070278463947,0.0134882525375867,0.0450704755958725));
#37343=CARTESIAN_POINT('',(0.0135303802320928,0.0135096732135866,0.0449939978015681));
#37344=CARTESIAN_POINT('',(0.0135685175242368,0.0135372652440246,0.0449859511372893));
#37345=CARTESIAN_POINT('',(0.0133154066073941,0.0135536114581477,0.0451879939181472));
#37346=CARTESIAN_POINT('',(0.019,-3.9861646017376E-17,0.0448084035990546));
#37347=CARTESIAN_POINT('',(0.019,0.00251516724482142,0.0448716686934959));
#37348=CARTESIAN_POINT('',(0.0179878255210343,0.0075443863126556,0.0449981988823785));
#37349=CARTESIAN_POINT('',(0.0151095869241771,0.011790947767256,0.045124729071261));
#37350=CARTESIAN_POINT('',(0.013315398557798,0.0135536032569568,0.0451879941657023));
#37351=CARTESIAN_POINT('',(0.019,-4.91593209544621E-17,0.0448084035990546));
#37352=CARTESIAN_POINT('',(-0.019,7.9723292034752E-17,0.0433082162077251));
#37353=CARTESIAN_POINT('',(-0.019,-0.00248709418409184,0.0433707240156971));
#37354=CARTESIAN_POINT('',(-0.0180107055600589,-0.00746012312352672,0.0434957396316413));
#37355=CARTESIAN_POINT('',(-0.0137847972460807,-0.0137848390811386,0.0436832630555575));
#37356=CARTESIAN_POINT('',(-0.00746027851088496,-0.0180106936071851,0.0438707864794736));
#37357=CARTESIAN_POINT('',(-6.62381636648879E-17,-0.0194946531964074,0.0440583099033898));
#37358=CARTESIAN_POINT('',(0.00746027851088484,-0.0180106936071852,0.044245833327306));
#37359=CARTESIAN_POINT('',(0.0137847972460806,-0.0137848390811387,0.0444333567512222));
#37360=CARTESIAN_POINT('',(0.0180107055600588,-0.00746012312352681,0.0446208801751384));
#37361=CARTESIAN_POINT('',(0.019,-0.00248709418409196,0.0447458957910825));
#37362=CARTESIAN_POINT('',(0.019,-3.9861646017376E-17,0.0448084035990546));
#37363=CARTESIAN_POINT('',(-0.019,6.35745487137311E-18,0.0433082162077251));
#37364=CARTESIAN_POINT('',(0.019,-3.9861646017376E-17,0.0418080680515213));
#37365=CARTESIAN_POINT('',(0.019,0.00248709418409188,0.0418705742246965));
#37366=CARTESIAN_POINT('',(0.0180107055600589,0.00746012312352676,0.0419955865710468));
#37367=CARTESIAN_POINT('',(0.0137847972460807,0.0137848390811386,0.0421831050905722));
#37368=CARTESIAN_POINT('',(0.00746027851088491,0.0180106936071852,0.0423706236100977));
#37369=CARTESIAN_POINT('',(2.09173148415435E-17,0.0194946531964074,0.0425581421296232));
#37370=CARTESIAN_POINT('',(-0.00746027851088488,0.0180106936071852,0.0427456606491487));
#37371=CARTESIAN_POINT('',(-0.0137847972460807,0.0137848390811386,0.0429331791686741));
#37372=CARTESIAN_POINT('',(-0.0180107055600589,0.00746012312352679,0.0431206976881996));
#37373=CARTESIAN_POINT('',(-0.019,0.00248709418409192,0.0432457100345499));
#37374=CARTESIAN_POINT('',(-0.019,0.,0.0433082162077251));
#37375=CARTESIAN_POINT('',(0.019,8.95355988618673E-18,0.0418080680515213));
#37376=CARTESIAN_POINT('',(-0.019,7.9723292034752E-17,0.0403085360942082));
#37377=CARTESIAN_POINT('',(-0.019,-0.00248709418409184,0.0403710165924296));
#37378=CARTESIAN_POINT('',(-0.0180107055600589,-0.00746012312352672,0.0404959775888723));
#37379=CARTESIAN_POINT('',(-0.0137847972460807,-0.0137848390811386,0.0406834190835365));
#37380=CARTESIAN_POINT('',(-0.00746027851088496,-0.0180106936071851,0.0408708605782006));
#37381=CARTESIAN_POINT('',(-6.62381636648879E-17,-0.0194946531964074,0.0410583020728647));
#37382=CARTESIAN_POINT('',(0.00746027851088484,-0.0180106936071852,0.0412457435675289));
#37383=CARTESIAN_POINT('',(0.0137847972460806,-0.0137848390811387,0.041433185062193));
#37384=CARTESIAN_POINT('',(0.0180107055600588,-0.00746012312352681,0.0416206265568572));
#37385=CARTESIAN_POINT('',(0.019,-0.00248709418409196,0.0417455875532999));
#37386=CARTESIAN_POINT('',(0.019,-3.9861646017376E-17,0.0418080680515213));
#37387=CARTESIAN_POINT('',(-0.019,-5.14795421335563E-17,0.0403085360942082));
#37388=CARTESIAN_POINT('',(0.019,-1.60883575115789E-14,0.0388082819344598));
#37389=CARTESIAN_POINT('',(0.0190000000000021,0.0024870941840765,0.0388707925244493));
#37390=CARTESIAN_POINT('',(0.0180107055600646,0.00746012312351353,0.0389958137044283));
#37391=CARTESIAN_POINT('',(0.0137847972460896,0.0137848390811301,0.0391833454743969));
#37392=CARTESIAN_POINT('',(0.00746027851089453,0.0180106936071815,0.0393708772443654));
#37393=CARTESIAN_POINT('',(8.25327519264503E-15,0.0194946531964077,0.039558409014334));
#37394=CARTESIAN_POINT('',(-0.00746027851087928,0.0180106936071878,0.0397459407843026));
#37395=CARTESIAN_POINT('',(-0.0137847972460779,0.0137848390811417,0.0399334725542711));
#37396=CARTESIAN_POINT('',(-0.0180107055600583,0.00746012312352879,0.0401210043242397));
#37397=CARTESIAN_POINT('',(-0.019,0.00248709418409259,0.0402460255042187));
#37398=CARTESIAN_POINT('',(-0.019,0.,0.0403085360942082));
#37399=CARTESIAN_POINT('',(0.019,-1.61262072877242E-14,0.0388082819344598));
#37400=CARTESIAN_POINT('',(-0.019,7.9723292034752E-17,0.0373080333342866));
#37401=CARTESIAN_POINT('',(-0.019,-0.00248709418409117,0.0373705436926271));
#37402=CARTESIAN_POINT('',(-0.0180107055600594,-0.00746012312352471,0.0374955644093082));
#37403=CARTESIAN_POINT('',(-0.0137847972460834,-0.0137848390811355,0.0376830954843299));
#37404=CARTESIAN_POINT('',(-0.00746027851089055,-0.0180106936071825,0.0378706265593515));
#37405=CARTESIAN_POINT('',(-8.29022911553176E-15,-0.0194946531964072,0.0380581576343732));
#37406=CARTESIAN_POINT('',(0.00746027851087523,-0.0180106936071889,0.0382456887093948));
#37407=CARTESIAN_POINT('',(0.0137847972460717,-0.0137848390811472,0.0384332197844165));
#37408=CARTESIAN_POINT('',(0.0180107055600531,-0.00746012312354004,0.0386207508594381));
#37409=CARTESIAN_POINT('',(0.0189999999999979,-0.00248709418410734,0.0387457715761192));
#37410=CARTESIAN_POINT('',(0.019,-1.60883575115789E-14,0.0388082819344598));
#37411=CARTESIAN_POINT('',(-0.019,4.54954461515252E-17,0.0373080333342866));
#37412=CARTESIAN_POINT('',(0.0135947752080227,0.0132733600509943,0.0361780495049504));
#37413=CARTESIAN_POINT('',(0.0109753255973188,0.0159562397807274,0.0362722148240618));
#37414=CARTESIAN_POINT('',(0.00410759749193419,0.0197186661240115,0.0364605454622845));
#37415=CARTESIAN_POINT('',(-0.00759708232316353,0.0186558030226723,0.0367430414196185));
#37416=CARTESIAN_POINT('',(-0.0167144641966965,0.0112394322580518,0.0370255373769525));
#37417=CARTESIAN_POINT('',(-0.019,0.00374958129758905,0.0372138680151752));
#37418=CARTESIAN_POINT('',(-0.019,0.,0.0373080333342866));
#37419=CARTESIAN_POINT('',(0.0135947999945552,0.0132733842837834,0.0361780492531812));
#37420=CARTESIAN_POINT('',(0.0135722168793318,0.0135335509805304,0.0359858244640535));
#37421=CARTESIAN_POINT('',(0.0135448185599411,0.0134952138392626,0.0359934900823968));
#37422=CARTESIAN_POINT('',(0.0135257317133337,0.0133692298759541,0.0360662817720579));
#37423=CARTESIAN_POINT('',(0.01355510517062,0.0133140557191526,0.0361236111063028));
#37424=CARTESIAN_POINT('',(0.0135948247028973,0.013273408596571,0.0361780493788477));
#37425=CARTESIAN_POINT('',(0.0134214493584107,0.0137296865857405,0.0432866344382823));
#37426=CARTESIAN_POINT('',(0.0135335436975079,0.0135722252250888,0.0430141821297884));
#37427=CARTESIAN_POINT('',(0.013495210770777,0.0135448275134576,0.0430065171585731));
#37428=CARTESIAN_POINT('',(0.0133692322905148,0.0135257199693753,0.0429337223945325));
#37429=CARTESIAN_POINT('',(0.0133140317184763,0.0135551063111274,0.0428763716821991));
#37430=CARTESIAN_POINT('',(0.0132733898758911,0.0135948055585231,0.0428219506155445));
#37431=CARTESIAN_POINT('',(0.0135335224965767,0.0135722054159043,0.043014358959348));
#37432=CARTESIAN_POINT('',(0.0132733749216108,0.0135947904241369,0.0428219507431747));
#37433=CARTESIAN_POINT('',(0.013273389787819,0.013594805644538,0.0428219507440773));
#37434=CARTESIAN_POINT('',(0.0132873978720912,0.0135810767699496,0.0436106318019714));
#37435=CARTESIAN_POINT('',(0.0133014061630618,0.0135673481069843,0.044399312859878));
#37436=CARTESIAN_POINT('',(0.0133154146613603,0.0135536196550256,0.0451879939177751));
#37437=CARTESIAN_POINT('',(0.0135684900658114,0.0135372510065474,0.0449857721696874));
#37438=CARTESIAN_POINT('',(0.0135773102099061,0.0135436364574972,0.0449837092908326));
#37439=CARTESIAN_POINT('',(0.013585610235647,0.0135507472552975,0.0449816684977748));
#37440=CARTESIAN_POINT('',(0.0135932791745505,0.0135584892152446,0.04497965012538));
#37441=CARTESIAN_POINT('',(0.0135932855747001,0.0135584828160982,0.0449796496479541));
#37442=CARTESIAN_POINT('',(0.0135581119696951,0.0135929312435436,0.0430202462678972));
#37443=CARTESIAN_POINT('',(0.0135698386395681,0.0135814462998891,0.0436733806520518));
#37444=CARTESIAN_POINT('',(0.0135815653094411,0.0135699613562345,0.0443265150362065));
#37445=CARTESIAN_POINT('',(0.0135932919793141,0.01355847641258,0.0449796494203611));
#37446=CARTESIAN_POINT('',(0.0135581121542913,0.0135929310589486,0.0430202462613394));
#37447=CARTESIAN_POINT('',(0.0134129571505461,0.0137267074203667,0.0430647873816228));
#37448=CARTESIAN_POINT('',(0.0137072504062847,0.0134443055379105,0.0344382290633684));
#37449=CARTESIAN_POINT('',(0.0135929312391456,0.0135581119741857,0.0359797534819639));
#37450=CARTESIAN_POINT('',(0.0135814462969616,0.0135698386425573,0.0353266191814339));
#37451=CARTESIAN_POINT('',(0.0135699613547775,0.0135815653109288,0.0346734848809039));
#37452=CARTESIAN_POINT('',(0.0135584764125934,0.0135932919793003,0.0340203505803739));
#37453=CARTESIAN_POINT('',(0.0135929265320308,0.0135581166810912,0.0359797536492453));
#37454=CARTESIAN_POINT('',(0.0135584942938894,0.013593274088762,0.0340203499447281));
#37455=CARTESIAN_POINT('',(0.0135929218292959,0.0135581213835245,0.0359797540662325));
#37456=CARTESIAN_POINT('',(0.0135853714857596,0.0135505002845721,0.0359817380910061));
#37457=CARTESIAN_POINT('',(0.0135784328080303,0.0135422677164711,0.0359837004096582));
#37458=CARTESIAN_POINT('',(0.0135721957749986,0.0135335294431583,0.035985641334575));
#37459=CARTESIAN_POINT('',(0.0135948247912817,0.013273408506102,0.0361780492510671));
#37460=CARTESIAN_POINT('',(0.013582176399302,0.0132862934770642,0.0354520328340541));
#37461=CARTESIAN_POINT('',(0.0135695281552721,0.0132991785925841,0.034726016417029));
#37462=CARTESIAN_POINT('',(0.0135568800588317,0.0133120638530298,0.0340000000000049));
#37463=CARTESIAN_POINT('',(0.0135568795107147,0.0133120633124194,0.0340000000714098));
#37464=CARTESIAN_POINT('',(0.0135568800588317,0.0133120638530298,0.0340000000000049));
#37465=CARTESIAN_POINT('',(0.0134973437325541,0.0133726944056705,0.0340021345712315));
#37466=CARTESIAN_POINT('',(0.0134833406019767,0.0134731784383755,0.0340041824205536));
#37467=CARTESIAN_POINT('',(0.0135240277273972,0.0135478066093083,0.0340048056241338));
#37468=CARTESIAN_POINT('',(0.0135239956136941,0.0135478241103007,0.0340048065022042));
#37469=CARTESIAN_POINT('',(0.013524003738558,0.0135477557735323,0.0340049411805581));
#37470=CARTESIAN_POINT('',(0.0135307046512648,0.0135597739884161,0.034010635057669));
#37471=CARTESIAN_POINT('',(0.0135386771238806,0.013571204328877,0.0340148023321076));
#37472=CARTESIAN_POINT('',(0.0135477915582315,0.0135817709703549,0.0340174403420765));
#37473=CARTESIAN_POINT('',(0.0135477529825173,0.0135818241209862,0.0340173607059137));
#37474=CARTESIAN_POINT('',(0.0135478083242499,0.013581796823751,0.0340172784089037));
#37475=CARTESIAN_POINT('',(0.0135512239240925,0.013585753873175,0.034018307096211));
#37476=CARTESIAN_POINT('',(0.0135547955159251,0.0135895776046143,0.0340193306530654));
#37477=CARTESIAN_POINT('',(0.0135585121708165,0.0135932562026847,0.0340203490599872));
#37478=CARTESIAN_POINT('',(0.0116902830159151,0.0149778931431562,0.0428599463516431));
#37479=CARTESIAN_POINT('',(0.0116931710101275,0.0149756390564587,0.0430503063057597));
#37480=CARTESIAN_POINT('',(0.0118103172895557,0.0151254370962809,0.0430596673970548));
#37481=CARTESIAN_POINT('',(0.0120521347075991,0.0146954669938212,0.0428510193710697));
#37482=CARTESIAN_POINT('',(0.0120463403333191,0.0146998796691399,0.0430329133156896));
#37483=CARTESIAN_POINT('',(0.012169281878152,0.0148333572635523,0.043050300662135));
#37484=CARTESIAN_POINT('',(0.0124034181196442,0.0144002110811048,0.0428449791580437));
#37485=CARTESIAN_POINT('',(0.0124025987870145,0.014401052044687,0.0430207675215794));
#37486=CARTESIAN_POINT('',(0.0125195284727906,0.014530291707653,0.0430433330239107));
#37487=CARTESIAN_POINT('',(0.0130845840208317,0.0137842127534686,0.0428285872315281));
#37488=CARTESIAN_POINT('',(0.0130842898532399,0.0137843803990833,0.0429976801221143));
#37489=CARTESIAN_POINT('',(0.013202356541565,0.0139023415876872,0.0430257919690624));
#37490=CARTESIAN_POINT('',(0.0134144470800416,0.0134634970025393,0.0428172753093004));
#37491=CARTESIAN_POINT('',(0.0134174053542952,0.0134605501176648,0.0429862619436122));
#37492=CARTESIAN_POINT('',(0.0135355961119401,0.0135781436477725,0.0430144185077102));
#37493=CARTESIAN_POINT('',(0.0140525177593388,0.0127960887236721,0.0427941261457912));
#37494=CARTESIAN_POINT('',(0.014055317366581,0.0127930130042102,0.0429630677168436));
#37495=CARTESIAN_POINT('',(0.0141790411357716,0.0129046942850932,0.0429912609479785));
#37496=CARTESIAN_POINT('',(0.0143616949765598,0.0124481002284708,0.0427824935191819));
#37497=CARTESIAN_POINT('',(0.0143644074366707,0.0124449724353076,0.042951387722865));
#37498=CARTESIAN_POINT('',(0.0144907980623338,0.0125535396640404,0.0429796190399368));
#37499=CARTESIAN_POINT('',(0.0149497857727254,0.0117353051620916,0.0427593621514848));
#37500=CARTESIAN_POINT('',(0.0149523431506991,0.0117320456807852,0.0429281817614341));
#37501=CARTESIAN_POINT('',(0.0150837971203497,0.0118342876556258,0.0429564729838029));
#37502=CARTESIAN_POINT('',(0.0152294723517477,0.0113698647436651,0.0427478385465288));
#37503=CARTESIAN_POINT('',(0.0152319770460271,0.0113665102266746,0.0429166303007036));
#37504=CARTESIAN_POINT('',(0.0153658192417093,0.0114655502020432,0.0429449439662434));
#37505=CARTESIAN_POINT('',(0.0160263071195749,0.0102469551436804,0.0427132524624603));
#37506=CARTESIAN_POINT('',(0.0160285673500078,0.0102434197484808,0.0428820330083143));
#37507=CARTESIAN_POINT('',(0.0161693473214105,0.0103325727791095,0.0429103551701594));
#37508=CARTESIAN_POINT('',(0.0165014481567208,0.0094630354913846,0.042690150225392));
#37509=CARTESIAN_POINT('',(0.0165036238241023,0.00945922543135878,0.0428590308671038));
#37510=CARTESIAN_POINT('',(0.0166485580443778,0.00954171177013287,0.0428872730454636));
#37511=CARTESIAN_POINT('',(0.0173387201681154,0.00782404083015533,0.0426437283881698));
#37512=CARTESIAN_POINT('',(0.0173405252860055,0.00782005818368833,0.0428127489102698));
#37513=CARTESIAN_POINT('',(0.0174928823059129,0.00788821699864262,0.042840878879618));
#37514=CARTESIAN_POINT('',(0.0177017792545385,0.00696362252345879,0.0426204378972089));
#37515=CARTESIAN_POINT('',(0.0177032239234523,0.00695998520536297,0.0427893636130864));
#37516=CARTESIAN_POINT('',(0.0178587818090731,0.00702013455170138,0.0428175686439992));
#37517=CARTESIAN_POINT('',(0.01829135151316,0.0052222109539592,0.0425745084349314));
#37518=CARTESIAN_POINT('',(0.0182924116960155,0.00521845009209468,0.0427431979283701));
#37519=CARTESIAN_POINT('',(0.0184528145256494,0.00526322955959588,0.0427715929411472));
#37520=CARTESIAN_POINT('',(0.018521285815859,0.00433610970738375,0.0425516847293725));
#37521=CARTESIAN_POINT('',(0.0185222391423024,0.00433204131040263,0.0427202675416825));
#37522=CARTESIAN_POINT('',(0.0186844239914438,0.00436927932320634,0.042748749164781));
#37523=CARTESIAN_POINT('',(0.0187697946121533,0.00298408765527847,0.0425171503472629));
#37524=CARTESIAN_POINT('',(0.01877045363091,0.00297994313561533,0.042685728914949));
#37525=CARTESIAN_POINT('',(0.0189347575854476,0.00300534506766644,0.042714213540631));
#37526=CARTESIAN_POINT('',(0.0188365030539556,0.0025295870523152,0.0425055923622042));
#37527=CARTESIAN_POINT('',(0.018837067060276,0.00252538076843415,0.0426741900952649));
#37528=CARTESIAN_POINT('',(0.0190019562100111,0.00254684875031955,0.0427026594088152));
#37529=CARTESIAN_POINT('',(0.0189370424924125,0.00161278628388406,0.042482336595439));
#37530=CARTESIAN_POINT('',(0.0189374045043678,0.0016085482150996,0.0426510039425693));
#37531=CARTESIAN_POINT('',(0.0191032191867231,0.00162199833661797,0.0426794171728615));
#37532=CARTESIAN_POINT('',(0.0189708812277667,0.00114859680187076,0.0424705911901054));
#37533=CARTESIAN_POINT('',(0.0189711379065816,0.00114433652145144,0.0426393079072488));
#37534=CARTESIAN_POINT('',(0.0191372911038253,0.00115373805721631,0.0426676814839808));
#37535=CARTESIAN_POINT('',(0.0190209950275129,-0.000237033433351926,0.0424355926553317));
#37536=CARTESIAN_POINT('',(0.0190209497223709,-0.000241456245903946,0.0426044396407925));
#37537=CARTESIAN_POINT('',(0.0191876388490383,-0.000244031484226691,0.042632709358546));
#37538=CARTESIAN_POINT('',(0.0189870113680649,-0.00115373022849519,0.0424125803189054));
#37539=CARTESIAN_POINT('',(0.0189867827922777,-0.00115767434941267,0.0425814574287911));
#37540=CARTESIAN_POINT('',(0.0191531423808799,-0.00116873009402599,0.0426097014877259));
#37541=CARTESIAN_POINT('',(0.01878820108735,-0.00297341454097277,0.0423668250938457));
#37542=CARTESIAN_POINT('',(0.0187875748666947,-0.00297729522553448,0.0425354908799519));
#37543=CARTESIAN_POINT('',(0.0189518834296028,-0.00300425733578145,0.0425639051805033));
#37544=CARTESIAN_POINT('',(0.0186233771455114,-0.00387639995695613,0.0423439862261447));
#37545=CARTESIAN_POINT('',(0.0186225432584859,-0.00388042491741729,0.0425125064146396));
#37546=CARTESIAN_POINT('',(0.0187852255652517,-0.00391507702103005,0.0425410381574683));
#37547=CARTESIAN_POINT('',(0.018274665533442,-0.00522022632396231,0.042309152018482));
#37548=CARTESIAN_POINT('',(0.0182735185981123,-0.00522424059044953,0.0424776276212393));
#37549=CARTESIAN_POINT('',(0.018433065606184,-0.00527057225040032,0.0425061948623966));
#37550=CARTESIAN_POINT('',(0.0181415131957001,-0.00566548389294523,0.0422974690443417));
#37551=CARTESIAN_POINT('',(0.0181402488570975,-0.00566952979746723,0.0424659542399351));
#37552=CARTESIAN_POINT('',(0.0182986445061403,-0.00571969889912052,0.0424945138859628));
#37553=CARTESIAN_POINT('',(0.0178456356258476,-0.00653800412056035,0.0422742355721382));
#37554=CARTESIAN_POINT('',(0.01784417337783,-0.00654199865587599,0.0424427903170468));
#37555=CARTESIAN_POINT('',(0.0180000251383591,-0.00659981281907227,0.0424712938630216));
#37556=CARTESIAN_POINT('',(0.0176824727806309,-0.00696706185954262,0.0422626389575521));
#37557=CARTESIAN_POINT('',(0.0176808958611167,-0.00697105930894539,0.0424312511668981));
#37558=CARTESIAN_POINT('',(0.0178353846391573,-0.0070326110295655,0.042459708658246));
#37559=CARTESIAN_POINT('',(0.0171480895942689,-0.00823299469432104,0.0422278683197848));
#37560=CARTESIAN_POINT('',(0.0171461373322301,-0.00823709568725569,0.0423966772546488));
#37561=CARTESIAN_POINT('',(0.0172962060414754,-0.00830958663110433,0.0424249776750704));
#37562=CARTESIAN_POINT('',(0.0167322082218721,-0.00904873968945994,0.0422047043777687));
#37563=CARTESIAN_POINT('',(0.0167302252983698,-0.00905240950799154,0.0423737030474594));
#37564=CARTESIAN_POINT('',(0.0168766534262386,-0.00913246361302278,0.0424018492301041));
#37565=CARTESIAN_POINT('',(0.016017776215106,-0.0102294899975369,0.0421700643431915));
#37566=CARTESIAN_POINT('',(0.0160155304590875,-0.0102330052947774,0.0423390256013007));
#37567=CARTESIAN_POINT('',(0.016155636454386,-0.0103233270447803,0.0423672030318007));
#37568=CARTESIAN_POINT('',(0.0157639583700152,-0.0106166212588865,0.0421585036680659));
#37569=CARTESIAN_POINT('',(0.0157616695074945,-0.0106200230247405,0.0423274092588773));
#37570=CARTESIAN_POINT('',(0.0158994422981835,-0.0107137457762176,0.0423556313959451));
#37571=CARTESIAN_POINT('',(0.0152272801277975,-0.0113729930254,0.0421353516005726));
#37572=CARTESIAN_POINT('',(0.0152248306979017,-0.0113762692680501,0.0423041230377585));
#37573=CARTESIAN_POINT('',(0.0153577455710004,-0.0114765124210403,0.0423324532441816));
#37574=CARTESIAN_POINT('',(0.0149467207633388,-0.0117391073542602,0.0421238563386887));
#37575=CARTESIAN_POINT('',(0.0149441912424758,-0.011742330856736,0.042292551641195));
#37576=CARTESIAN_POINT('',(0.0150745657995214,-0.0118457083325256,0.0423209430424921));
#37577=CARTESIAN_POINT('',(0.014069384387219,-0.0128022199314398,0.0420894336026386));
#37578=CARTESIAN_POINT('',(0.0140667495585985,-0.0128050961186576,0.0422579508410219));
#37579=CARTESIAN_POINT('',(0.0141891092920901,-0.0129177740881277,0.0422864839229229));
#37580=CARTESIAN_POINT('',(0.0134371299761888,-0.0134641659672828,0.0420665540087471));
#37581=CARTESIAN_POINT('',(0.0134340693086654,-0.0134672128418654,0.0422350107166076));
#37582=CARTESIAN_POINT('',(0.0135511085133077,-0.0135853119533646,0.0422635938651249));
#37583=CARTESIAN_POINT('',(0.0124182379819621,-0.0143874049856545,0.0420319064132249));
#37584=CARTESIAN_POINT('',(0.0124150273123975,-0.0143901774409011,0.042200448692967));
#37585=CARTESIAN_POINT('',(0.0125231164314169,-0.0145164470673288,0.0422289622752316));
#37586=CARTESIAN_POINT('',(0.0120668099875688,-0.0146834930653284,0.0420203064047687));
#37587=CARTESIAN_POINT('',(0.0120634984437343,-0.0146862124321403,0.0421888988715361));
#37588=CARTESIAN_POINT('',(0.0121685715444792,-0.0148150826757778,0.0422173722479392));
#37589=CARTESIAN_POINT('',(0.0113398839142431,-0.0152518820047602,0.0419969773954634));
#37590=CARTESIAN_POINT('',(0.0113364404448756,-0.0152544443950376,0.0421656892462165));
#37591=CARTESIAN_POINT('',(0.0114352161544657,-0.0153883695391954,0.0421940666469763));
#37592=CARTESIAN_POINT('',(0.0109628963113278,-0.0155250853649475,0.0419852045877687));
#37593=CARTESIAN_POINT('',(0.0109593996535451,-0.015527552715629,0.0421539852232674));
#37594=CARTESIAN_POINT('',(0.0110549026147746,-0.0156639311220682,0.0421823072906783));
#37595=CARTESIAN_POINT('',(0.00981181685212698,-0.0162966786354659,0.0419502110722857));
#37596=CARTESIAN_POINT('',(0.00980802468690172,-0.01629897358581,0.0421191318727581));
#37597=CARTESIAN_POINT('',(0.00989364532800342,-0.0164421136866359,0.0421473424316667));
#37598=CARTESIAN_POINT('',(0.00901475697726111,-0.0167502804088702,0.0419273086335697));
#37599=CARTESIAN_POINT('',(0.00901132318991663,-0.0167521431827161,0.0420961716539068));
#37600=CARTESIAN_POINT('',(0.00908946333972755,-0.0168994032707856,0.042124427101066));
#37601=CARTESIAN_POINT('',(0.00736294102394891,-0.017539237059026,0.0418815910047469));
#37602=CARTESIAN_POINT('',(0.00735934332100566,-0.0175407328683054,0.0420502112706503));
#37603=CARTESIAN_POINT('',(0.00742286512687939,-0.0176945902813653,0.0420786619207783));
#37604=CARTESIAN_POINT('',(0.00650818842987571,-0.0178745959943225,0.0418587210379212));
#37605=CARTESIAN_POINT('',(0.00650426173646775,-0.0178760265082283,0.0420272155291122));
#37606=CARTESIAN_POINT('',(0.00656049360996185,-0.0180325388998404,0.0420557680753826));
#37607=CARTESIAN_POINT('',(0.00518125028045295,-0.0182857614055599,0.041823816448597));
#37608=CARTESIAN_POINT('',(0.00517721155912882,-0.0182869059511596,0.0419923098442186));
#37609=CARTESIAN_POINT('',(0.00522182413452343,-0.0184469637090321,0.0420208627463016));
#37610=CARTESIAN_POINT('',(0.00473302918526943,-0.0184068044888232,0.041812126906403));
#37611=CARTESIAN_POINT('',(0.00472890347372164,-0.0184078641754975,0.0419806453549743));
#37612=CARTESIAN_POINT('',(0.0047696534380224,-0.0185689808298537,0.0420091782601784));
#37613=CARTESIAN_POINT('',(0.0038358425246037,-0.0186144655814991,0.0417888747841534));
#37614=CARTESIAN_POINT('',(0.00383165727851394,-0.0186153295086939,0.0419574872132742));
#37615=CARTESIAN_POINT('',(0.0038645762329874,-0.0187783348169813,0.0419859444304395));
#37616=CARTESIAN_POINT('',(0.00338529441764298,-0.0187015910797529,0.0417772706777386));
#37617=CARTESIAN_POINT('',(0.00338105873145118,-0.0187023559206568,0.0419459499657417));
#37618=CARTESIAN_POINT('',(0.00341007283725043,-0.0188661831320287,0.0419743535313619));
#37619=CARTESIAN_POINT('',(0.00202788112853736,-0.0189136619130776,0.0417424975737002));
#37620=CARTESIAN_POINT('',(0.00202335886061544,-0.0189141621421916,0.0419113796263766));
#37621=CARTESIAN_POINT('',(0.00204075058140732,-0.0190799965482407,0.0419396213395313));
#37622=CARTESIAN_POINT('',(0.00111527657161592,-0.0189895589037079,0.0417193881771659));
#37623=CARTESIAN_POINT('',(0.00111124227504146,-0.0189898031317301,0.0418884155584991));
#37624=CARTESIAN_POINT('',(0.00112015474861678,-0.0191564722530023,0.0419165384790431));
#37625=CARTESIAN_POINT('',(-0.000265294000998375,-0.0190037211195645,0.0416848185347678));
#37626=CARTESIAN_POINT('',(-0.000269428442369693,-0.0190036621380701,0.0418537311390249));
#37627=CARTESIAN_POINT('',(-0.000272495772136029,-0.0191702742242257,0.0418819477804248));
#37628=CARTESIAN_POINT('',(-0.000728732033634883,-0.0189916745362715,0.0416732557504993));
#37629=CARTESIAN_POINT('',(-0.000732820037092626,-0.0189915195967747,0.0418420994331531));
#37630=CARTESIAN_POINT('',(-0.000739986546925877,-0.0191579229371231,0.0418703714712338));
#37631=CARTESIAN_POINT('',(-0.00165373562203119,-0.0189335657117441,0.0416501273390889));
#37632=CARTESIAN_POINT('',(-0.00165780624299728,-0.0189332081609065,0.0418188303614342));
#37633=CARTESIAN_POINT('',(-0.00167306542317714,-0.019098906581222,0.0418472155134374));
#37634=CARTESIAN_POINT('',(-0.00211248068853893,-0.0188877839132358,0.0416386316906292));
#37635=CARTESIAN_POINT('',(-0.00211656646631519,-0.0188873284324626,0.0418072640790303));
#37636=CARTESIAN_POINT('',(-0.00213580880466304,-0.0190525260587537,0.0418357059935484));
#37637=CARTESIAN_POINT('',(-0.00347773927072136,-0.0187015815591903,0.0416041849706497));
#37638=CARTESIAN_POINT('',(-0.00348162652046194,-0.0187008479423524,0.0417726705774203));
#37639=CARTESIAN_POINT('',(-0.00351295591739027,-0.0188641701699972,0.0418012290733437));
#37640=CARTESIAN_POINT('',(-0.00437333147735052,-0.0185125519319189,0.0415812587715974));
#37641=CARTESIAN_POINT('',(-0.00437759833950889,-0.0185115353469389,0.0417497243726128));
#37642=CARTESIAN_POINT('',(-0.00441633674311674,-0.0186732446887795,0.0417783005161147));
#37643=CARTESIAN_POINT('',(-0.00569496546372668,-0.0181322232552342,0.0415465561867922));
#37644=CARTESIAN_POINT('',(-0.00569903285637957,-0.0181309470948967,0.0417151481291254));
#37645=CARTESIAN_POINT('',(-0.00574948949371243,-0.0182893784412442,0.041743621825817));
#37646=CARTESIAN_POINT('',(-0.00613187049197437,-0.0179892539573154,0.0415349403823787));
#37647=CARTESIAN_POINT('',(-0.00613593199273233,-0.0179878677665463,0.041703592466749));
#37648=CARTESIAN_POINT('',(-0.00619020606605926,-0.0181451101082577,0.0417320179172437));
#37649=CARTESIAN_POINT('',(-0.00699824753201534,-0.0176702468899496,0.0415115949679377));
#37650=CARTESIAN_POINT('',(-0.00700224077842883,-0.0176686672242183,0.0416803700106387));
#37651=CARTESIAN_POINT('',(-0.00706413549155712,-0.0178232177429544,0.041708696666812));
#37652=CARTESIAN_POINT('',(-0.00742903192881274,-0.0174935023824463,0.0414998280884315));
#37653=CARTESIAN_POINT('',(-0.0074329489177034,-0.0174918378058293,0.0416686662427243));
#37654=CARTESIAN_POINT('',(-0.00749867232381402,-0.0176448802050545,0.041696942049135));
#37655=CARTESIAN_POINT('',(-0.00869032741724389,-0.0169213112197901,0.0414649178500639));
#37656=CARTESIAN_POINT('',(-0.00869418687519932,-0.0169193355548257,0.0416338437926145));
#37657=CARTESIAN_POINT('',(-0.00877088847995754,-0.0170674546052026,0.0416620501385558));
#37658=CARTESIAN_POINT('',(-0.00949541012943664,-0.0164825663036929,0.0414420968225364));
#37659=CARTESIAN_POINT('',(-0.00949879916290607,-0.0164806289998969,0.0416108965446497));
#37660=CARTESIAN_POINT('',(-0.00958282526174183,-0.0166245274441401,0.0416392030299223));
#37661=CARTESIAN_POINT('',(-0.011035843026309,-0.015493481667479,0.0413963760214746));
#37662=CARTESIAN_POINT('',(-0.0110390142666174,-0.0154912068770508,0.0415649356273811));
#37663=CARTESIAN_POINT('',(-0.0111363429551393,-0.0156261549868809,0.0415934348585898));
#37664=CARTESIAN_POINT('',(-0.0117711969806298,-0.0149431487864239,0.0413734589339542));
#37665=CARTESIAN_POINT('',(-0.0117745442615457,-0.0149405081863807,0.0415419254432952));
#37666=CARTESIAN_POINT('',(-0.0118779346569039,-0.0150707384352058,0.0415705006369759));
#37667=CARTESIAN_POINT('',(-0.0128199481592734,-0.0140308097662266,0.0413384716889231));
#37668=CARTESIAN_POINT('',(-0.012823067714203,-0.0140279603099078,0.0415069895682356));
#37669=CARTESIAN_POINT('',(-0.0129356768813544,-0.0141501790244631,0.0415355227587738));
#37670=CARTESIAN_POINT('',(-0.0131583924556861,-0.0137138083624527,0.0413267762023185));
#37671=CARTESIAN_POINT('',(-0.0131614799831733,-0.0137108438196155,0.0414953358982116));
#37672=CARTESIAN_POINT('',(-0.0132770380386662,-0.0138303492432787,0.0415238356278214));
#37673=CARTESIAN_POINT('',(-0.0138069700858022,-0.0130606052260107,0.0413035058920913));
#37674=CARTESIAN_POINT('',(-0.0138099208402457,-0.0130574883812653,0.0414721829022311));
#37675=CARTESIAN_POINT('',(-0.0139312251053164,-0.0131713498971273,0.0415005882390922));
#37676=CARTESIAN_POINT('',(-0.0141181439008517,-0.0127235089245412,0.0412918967450829));
#37677=CARTESIAN_POINT('',(-0.0141210247482436,-0.0127203095251467,0.0414606478017125));
#37678=CARTESIAN_POINT('',(-0.0142451005343464,-0.0128312773693915,0.0414889936415347));
#37679=CARTESIAN_POINT('',(-0.0150129218862625,-0.0116812175165574,0.0412571354604048));
#37680=CARTESIAN_POINT('',(-0.0150157186559916,-0.0116776467432949,0.0414260831456741));
#37681=CARTESIAN_POINT('',(-0.0151476205529159,-0.011779777158378,0.0414542721088526));
#37682=CARTESIAN_POINT('',(-0.01555798632197,-0.0109451809228585,0.0412341123150795));
#37683=CARTESIAN_POINT('',(-0.0155602657948406,-0.0109419608402871,0.0414031309680951));
#37684=CARTESIAN_POINT('',(-0.0156973111570896,-0.0110372036045412,0.041431260883828));
#37685=CARTESIAN_POINT('',(-0.0162971169504362,-0.0097783413757642,0.0411995908304197));
#37686=CARTESIAN_POINT('',(-0.0162992291652279,-0.00977481775363762,0.0413684386072347));
#37687=CARTESIAN_POINT('',(-0.0164424487701677,-0.00985986039481064,0.0413967074338958));
#37688=CARTESIAN_POINT('',(-0.0165311120487054,-0.00937746317451068,0.0411880216094757));
#37689=CARTESIAN_POINT('',(-0.0165331316590963,-0.00937390677878347,0.0413567935110557));
#37690=CARTESIAN_POINT('',(-0.0166783146320643,-0.0094553672421763,0.0413851233286793));
#37691=CARTESIAN_POINT('',(-0.0169683564716308,-0.00856092050002925,0.0411649046912745));
#37692=CARTESIAN_POINT('',(-0.0169701970106566,-0.00855726823880796,0.0413335398874641));
#37693=CARTESIAN_POINT('',(-0.0171190407602751,-0.00863148649995367,0.0413619794574576));
#37694=CARTESIAN_POINT('',(-0.0171708318982631,-0.00814698393664201,0.0411534035337962));
#37695=CARTESIAN_POINT('',(-0.0171726031991398,-0.00814325333577635,0.0413219778223036));
#37696=CARTESIAN_POINT('',(-0.0173231215110601,-0.00821384212091386,0.04135046633409));
#37697=CARTESIAN_POINT('',(-0.017731052841533,-0.00688861571725598,0.0411189213796909));
#37698=CARTESIAN_POINT('',(-0.0177325036627002,-0.00688486082694156,0.0412873887707809));
#37699=CARTESIAN_POINT('',(-0.0178878115569066,-0.00694425476119435,0.0413159619695044));
#37700=CARTESIAN_POINT('',(-0.0180418326806221,-0.00602770999892709,0.0410959463402988));
#37701=CARTESIAN_POINT('',(-0.0180432304820099,-0.00602349188773519,0.0412644359078562));
#37702=CARTESIAN_POINT('',(-0.0182011250457587,-0.00607574524266206,0.0412929929117318));
#37703=CARTESIAN_POINT('',(-0.0184143243537723,-0.00470349999157568,0.0410611960622287));
#37704=CARTESIAN_POINT('',(-0.018415385042611,-0.00469935355214511,0.0412298456009654));
#37705=CARTESIAN_POINT('',(-0.0185767091459214,-0.0047398876927624,0.0412582730424759));
#37706=CARTESIAN_POINT('',(-0.0185228150547828,-0.00425660020659874,0.0410495686245358));
#37707=CARTESIAN_POINT('',(-0.0185237743487955,-0.00425241841302469,0.041218284609882));
#37708=CARTESIAN_POINT('',(-0.0186861086030493,-0.00428906376273253,0.0412466586769884));
#37709=CARTESIAN_POINT('',(-0.0187077611289919,-0.00335156626267243,0.0410262187428564));
#37710=CARTESIAN_POINT('',(-0.0187085187711582,-0.00334734607949911,0.0411950507959571));
#37711=CARTESIAN_POINT('',(-0.0188725694807397,-0.00337608669774606,0.0412233316825547));
#37712=CARTESIAN_POINT('',(-0.0187842366968955,-0.00289229495447753,0.0410144682252158));
#37713=CARTESIAN_POINT('',(-0.0187848784700295,-0.00288812412115976,0.0411833510122318));
#37714=CARTESIAN_POINT('',(-0.0189496506391086,-0.00291278606496349,0.0412115909366078));
#37715=CARTESIAN_POINT('',(-0.0189616205224653,-0.00151941459674208,0.0409796698818028));
#37716=CARTESIAN_POINT('',(-0.0189619553202701,-0.00151523087861793,0.0411485646407798));
#37717=CARTESIAN_POINT('',(-0.0191282421326548,-0.00152787230521512,0.0411767959526733));
#37718=CARTESIAN_POINT('',(-0.0190124404528775,-0.000604158586940465,0.0409568928165333));
#37719=CARTESIAN_POINT('',(-0.019012577162559,-0.000600234906611998,0.0411256224683206));
#37720=CARTESIAN_POINT('',(-0.0191790764987429,-0.0006045732690382,0.0411539854380646));
#37721=CARTESIAN_POINT('',(-0.0189824657699048,0.00122633309780874,0.0409111447946851));
#37722=CARTESIAN_POINT('',(-0.0189822006506171,0.00123025769157615,0.0410796570137007));
#37723=CARTESIAN_POINT('',(-0.019148119656424,0.00124193696623813,0.0411081942232454));
#37724=CARTESIAN_POINT('',(-0.018901681485365,0.00214156878432867,0.0408881742600273));
#37725=CARTESIAN_POINT('',(-0.0189011856661895,0.00214588577272389,0.0410566312425167));
#37726=CARTESIAN_POINT('',(-0.0190663413782543,0.00216515858537636,0.0410852142632578));
#37727=CARTESIAN_POINT('',(-0.0186033079109007,0.00397200385251819,0.0408414167966276));
#37728=CARTESIAN_POINT('',(-0.0186024021643551,0.00397628464649719,0.04101000529016));
#37729=CARTESIAN_POINT('',(-0.0187650302612908,0.00401157895411037,0.0410384821772507));
#37730=CARTESIAN_POINT('',(-0.0183884060347462,0.00486877543600975,0.0408180973509746));
#37731=CARTESIAN_POINT('',(-0.0183872407774818,0.00487312486704268,0.0409868575445279));
#37732=CARTESIAN_POINT('',(-0.0185482076679463,0.0049161996783548,0.0410151969013339));
#37733=CARTESIAN_POINT('',(-0.0178349912586725,0.00661449450434864,0.0407717946732109));
#37734=CARTESIAN_POINT('',(-0.0178334421068741,0.00661870714934465,0.0409407905791265));
#37735=CARTESIAN_POINT('',(-0.0179897532959718,0.0066771387497462,0.0409689407226237));
#37736=CARTESIAN_POINT('',(-0.0174961250798382,0.00746554037439665,0.0407488694971596));
#37737=CARTESIAN_POINT('',(-0.0174946130470671,0.00746911998997856,0.0409178491190281));
#37738=CARTESIAN_POINT('',(-0.0176476722262288,0.0075355226464926,0.0409460105147068));
#37739=CARTESIAN_POINT('',(-0.0168928793059809,0.00870877719466603,0.0407143705486902));
#37740=CARTESIAN_POINT('',(-0.0168910022413453,0.00871241404999286,0.0408831464914586));
#37741=CARTESIAN_POINT('',(-0.0170386211619198,0.00878938945676106,0.0409114730783643));
#37742=CARTESIAN_POINT('',(-0.0166749785102286,0.009119172623828,0.0407027900269581));
#37743=CARTESIAN_POINT('',(-0.016673014372315,0.00912276786271566,0.0408714896140114));
#37744=CARTESIAN_POINT('',(-0.0168186292924956,0.00920328236964801,0.0408998775668188));
#37745=CARTESIAN_POINT('',(-0.0162111810736432,0.00992027347694162,0.040679672638002));
#37746=CARTESIAN_POINT('',(-0.0162090391497371,0.00992377055421589,0.0408482493232186));
#37747=CARTESIAN_POINT('',(-0.0163504414828778,0.0100112107376009,0.0408767357850865));
#37748=CARTESIAN_POINT('',(-0.0159659475062535,0.0103101504290009,0.0406681615251639));
#37749=CARTESIAN_POINT('',(-0.0159636955796252,0.0103136390279756,0.0408366905658618));
#37750=CARTESIAN_POINT('',(-0.0161029146929399,0.0104044111131456,0.0408652153212605));
#37751=CARTESIAN_POINT('',(-0.0151912304606125,0.0114485476658325,0.0406336358038875));
#37752=CARTESIAN_POINT('',(-0.0151887570996142,0.0114518230940977,0.0408021035855928));
#37753=CARTESIAN_POINT('',(-0.0153210581004132,0.0115525415338422,0.0408306766175204));
#37754=CARTESIAN_POINT('',(-0.014622929391933,0.0121659929574409,0.0406106136156221));
#37755=CARTESIAN_POINT('',(-0.0146200524401287,0.0121694312704499,0.0407791444424219));
#37756=CARTESIAN_POINT('',(-0.0147476614088916,0.0122761729483964,0.0408076683603165));
#37757=CARTESIAN_POINT('',(-0.0136929237305084,0.013180068356081,0.0405758288898158));
#37758=CARTESIAN_POINT('',(-0.0136899494192345,0.0131831608238865,0.0407445413794423));
#37759=CARTESIAN_POINT('',(-0.0138093974149318,0.0132990263264894,0.0407729182659139));
#37760=CARTESIAN_POINT('',(-0.0133699463592963,0.0135077049833778,0.0405641959706274));
#37761=CARTESIAN_POINT('',(-0.0133669040498033,0.0135107142257478,0.0407329759851868));
#37762=CARTESIAN_POINT('',(-0.0134835617534226,0.0136295024291177,0.0407612985551758));
#37763=CARTESIAN_POINT('',(-0.0126974466340598,0.0141417257979227,0.0405408572390954));
#37764=CARTESIAN_POINT('',(-0.0126942704203723,0.0141445792357152,0.0407097330667613));
#37765=CARTESIAN_POINT('',(-0.0128050897757068,0.0142689756279715,0.0407379788512432));
#37766=CARTESIAN_POINT('',(-0.0123473085932254,0.0144484142221285,0.0405291421134551));
#37767=CARTESIAN_POINT('',(-0.0123441362264028,0.0144511258181016,0.0406980432058043));
#37768=CARTESIAN_POINT('',(-0.0124518316916227,0.0145782718212011,0.0407262686057894));
#37769=CARTESIAN_POINT('',(-0.0112739729442342,0.0153214994754053,0.0404944578563007));
#37770=CARTESIAN_POINT('',(-0.0112706968323,0.0153239022315645,0.040663288702221));
#37771=CARTESIAN_POINT('',(-0.0113688367160017,0.0154586468259733,0.0406915709389472));
#37772=CARTESIAN_POINT('',(-0.0105227406984075,0.015846449056652,0.0404716901640879));
#37773=CARTESIAN_POINT('',(-0.0105194393318638,0.0158486533708075,0.0406403488733642));
#37774=CARTESIAN_POINT('',(-0.0106107746025583,0.015987838740842,0.0406687690173338));
#37775=CARTESIAN_POINT('',(-0.00895054844538835,0.0167846865337946,0.0404258943877726));
#37776=CARTESIAN_POINT('',(-0.00894702830538813,0.0167865531939525,0.0405943749416822));
#37777=CARTESIAN_POINT('',(-0.00902446640469956,0.0169337143448247,0.0406229375719325));
#37778=CARTESIAN_POINT('',(-0.00812959521963859,0.0171979852881533,0.0404028663029833));
#37779=CARTESIAN_POINT('',(-0.00812559482701923,0.0171998652676137,0.0405713328036029));
#37780=CARTESIAN_POINT('',(-0.00819621891715045,0.0173504161809429,0.0405999083468083));
#37781=CARTESIAN_POINT('',(-0.00641509672436712,0.017908309535624,0.0403560080925695));
#37782=CARTESIAN_POINT('',(-0.00641091300938563,0.0179098201634833,0.0405246641763426));
#37783=CARTESIAN_POINT('',(-0.00646659766446683,0.0180667225222605,0.0405530870384352));
#37784=CARTESIAN_POINT('',(-0.00554091433977066,0.0181971572148494,0.0403327083910855));
#37785=CARTESIAN_POINT('',(-0.00553667044157995,0.0181984389167098,0.0405015540723921));
#37786=CARTESIAN_POINT('',(-0.00558474581842807,0.0183580808702938,0.0405298243010591));
#37787=CARTESIAN_POINT('',(-0.00376554510048333,0.0186456142971705,0.0402864854352754));
#37788=CARTESIAN_POINT('',(-0.00376123008776989,0.0186464944816664,0.0404555036912967));
#37789=CARTESIAN_POINT('',(-0.003793777162837,0.0188101927161195,0.0404836357763015));
#37790=CARTESIAN_POINT('',(-0.00286343258050692,0.0188055903779473,0.0402636501187532));
#37791=CARTESIAN_POINT('',(-0.00285961923148408,0.0188061864461319,0.0404325693382625));
#37792=CARTESIAN_POINT('',(-0.0028837112541823,0.0189712087558258,0.0404607794640954));
#37793=CARTESIAN_POINT('',(-0.00148820256203909,0.0189472325693201,0.0402291505505034));
#37794=CARTESIAN_POINT('',(-0.00148412777908813,0.0189475506496586,0.0403978539570062));
#37795=CARTESIAN_POINT('',(-0.0014963771872161,0.0191134985983846,0.0404262388044884));
#37796=CARTESIAN_POINT('',(-0.00102418033302645,0.0189780140213413,0.0402175547526945));
#37797=CARTESIAN_POINT('',(-0.00102007596487487,0.0189782370293938,0.040386186882504));
#37798=CARTESIAN_POINT('',(-0.00102827742850561,0.0191443495699763,0.0404146290013965));
#37799=CARTESIAN_POINT('',(-9.94653092085578E-5,0.0190053694571048,0.0401944269820207));
#37800=CARTESIAN_POINT('',(-9.5347232664673E-5,0.0190053897152703,0.0403629579225951));
#37801=CARTESIAN_POINT('',(-9.54513631700061E-5,0.0191715910880823,0.0403914809997104));
#37802=CARTESIAN_POINT('',(0.000360908106152808,0.0190021130416573,0.040182902582199));
#37803=CARTESIAN_POINT('',(0.00036508457391054,0.0190020340033433,0.0403514016925515));
#37804=CARTESIAN_POINT('',(0.000368953206577203,0.0191681528175206,0.0403799503793336));
#37805=CARTESIAN_POINT('',(0.00173621476613258,0.0189427499883702,0.0401483286629736));
#37806=CARTESIAN_POINT('',(0.00174038507151665,0.018942367524321,0.0403168150310215));
#37807=CARTESIAN_POINT('',(0.00175629267941908,0.019107900727566,0.0403453733464093));
#37808=CARTESIAN_POINT('',(0.00264536369269936,0.0188373023911365,0.0401252635252426));
#37809=CARTESIAN_POINT('',(0.0026498181005769,0.0188366634599821,0.0402938505069245));
#37810=CARTESIAN_POINT('',(0.00267338975743924,0.019001418134499,0.0403223292851573));
#37811=CARTESIAN_POINT('',(0.00399750571961914,0.0185803774351344,0.0400904610146314));
#37812=CARTESIAN_POINT('',(0.00400170347017837,0.0185794760270892,0.0402592365037631));
#37813=CARTESIAN_POINT('',(0.00403734421194199,0.0187420999168206,0.0402875627973426));
#37814=CARTESIAN_POINT('',(0.00444628218356663,0.0184782136197958,0.0400788298521094));
#37815=CARTESIAN_POINT('',(0.00445042005209088,0.0184772168738629,0.0402476677986115));
#37816=CARTESIAN_POINT('',(0.0044900385877306,0.0186389941549713,0.0402759437723264));
#37817=CARTESIAN_POINT('',(0.00533986815207782,0.0182400551521407,0.0400555200353558));
#37818=CARTESIAN_POINT('',(0.00534393651522462,0.0182388647581097,0.0402244184479622));
#37819=CARTESIAN_POINT('',(0.00539139235855439,0.018398589225329,0.040252646219197));
#37820=CARTESIAN_POINT('',(0.00578471697858165,0.0181038543997353,0.0400438539969031));
#37821=CARTESIAN_POINT('',(0.00578866000748204,0.0181025955764972,0.0402127406699899));
#37822=CARTESIAN_POINT('',(0.0058400860869573,0.0182610687836968,0.0402409778479568));
#37823=CARTESIAN_POINT('',(0.00709142101432577,0.0176511111999784,0.0400092547774132));
#37824=CARTESIAN_POINT('',(0.00709510071739637,0.0176496216435868,0.0401780135018141));
#37825=CARTESIAN_POINT('',(0.00715805298410857,0.0178038862360618,0.0402063533533533));
#37826=CARTESIAN_POINT('',(0.00793306601481205,0.0172888585230262,0.0399864822613801));
#37827=CARTESIAN_POINT('',(0.00793673177941187,0.0172871845585934,0.0401550748827933));
#37828=CARTESIAN_POINT('',(0.0080069017507295,0.0174380718168385,0.0401835482854934));
#37829=CARTESIAN_POINT('',(0.00955857914425509,0.0164460247527357,0.0399406223908872));
#37830=CARTESIAN_POINT('',(0.00956207819624298,0.016443983806927,0.0401090888995002));
#37831=CARTESIAN_POINT('',(0.00964637023866028,0.0165873089892121,0.0401376628762792));
#37832=CARTESIAN_POINT('',(0.0103426468499878,0.0159653185213969,0.0399175291538284));
#37833=CARTESIAN_POINT('',(0.0103464020038493,0.0159628707005397,0.0400860241419123));
#37834=CARTESIAN_POINT('',(0.0104372015299546,0.0161022307137298,0.0401145769416713));
#37835=CARTESIAN_POINT('',(0.01184973396054,0.0148810464826116,0.0398705942900101));
#37836=CARTESIAN_POINT('',(0.0118532676421069,0.0148782502110272,0.0400393259823159));
#37837=CARTESIAN_POINT('',(0.0119573719452351,0.0150082890904317,0.0400676883273018));
#37838=CARTESIAN_POINT('',(0.0125544556346826,0.0142906873536392,0.0398473241536116));
#37839=CARTESIAN_POINT('',(0.0125577009027439,0.0142878293504653,0.0400162524377134));
#37840=CARTESIAN_POINT('',(0.0126682600067235,0.0144127392115931,0.040044455699943));
#37841=CARTESIAN_POINT('',(0.0138702467674847,0.0130174634983839,0.0398012190609471));
#37842=CARTESIAN_POINT('',(0.0138731763361025,0.0130143463746749,0.0399702245532373));
#37843=CARTESIAN_POINT('',(0.0139952835666706,0.0131281092670227,0.0399983668028166));
#37844=CARTESIAN_POINT('',(0.014481306834379,0.0123345873702583,0.0397784453084914));
#37845=CARTESIAN_POINT('',(0.0144838228841967,0.012331656650006,0.0399472909001995));
#37846=CARTESIAN_POINT('',(0.0146113743771591,0.0124389662669217,0.0399755604113871));
#37847=CARTESIAN_POINT('',(0.0153260921123727,0.0112393715958483,0.0397439245227315));
#37848=CARTESIAN_POINT('',(0.0153285096105525,0.0112360719338832,0.0399125601214955));
#37849=CARTESIAN_POINT('',(0.0154630920701157,0.0113337979723908,0.039940999371801));
#37850=CARTESIAN_POINT('',(0.0155966863258303,0.0108608051472629,0.0397323104378551));
#37851=CARTESIAN_POINT('',(0.0155990470192725,0.0108574170854443,0.039900884452663));
#37852=CARTESIAN_POINT('',(0.0157359025015417,0.0109518057717685,0.0399293731818519));
#37853=CARTESIAN_POINT('',(0.0161064285816707,0.0100894336380538,0.0397091645442032));
#37854=CARTESIAN_POINT('',(0.0161086256317495,0.0100859246916167,0.039877665024853));
#37855=CARTESIAN_POINT('',(0.0162498417096541,0.0101734992112851,0.0399062124401483));
#37856=CARTESIAN_POINT('',(0.0163459130563638,0.00969647156966717,0.0396976246968182));
#37857=CARTESIAN_POINT('',(0.0163480572635308,0.0096928566267872,0.0398661107170753));
#37858=CARTESIAN_POINT('',(0.0164913098660663,0.00977702593089619,0.0398946698174529));
#37859=CARTESIAN_POINT('',(0.0170192632791019,0.00849625891948276,0.039663001559238));
#37860=CARTESIAN_POINT('',(0.0170211738557721,0.00849243937980604,0.0398315233381999));
#37861=CARTESIAN_POINT('',(0.0171702868223079,0.00856614567002418,0.039860053468202));
#37862=CARTESIAN_POINT('',(0.017408256052215,0.00766779115074893,0.0396399001523585));
#37863=CARTESIAN_POINT('',(0.017410054063016,0.0076636774840293,0.0398085548241078));
#37864=CARTESIAN_POINT('',(0.01756261565577,0.00773038834989212,0.039836979076401));
#37865=CARTESIAN_POINT('',(0.017901776908571,0.00638255305449936,0.0396050998642632));
#37866=CARTESIAN_POINT('',(0.0179032179134461,0.00637851585957844,0.0397739321898089));
#37867=CARTESIAN_POINT('',(0.018060308309342,0.0064338436493023,0.0398022128536858));
#37868=CARTESIAN_POINT('',(0.0180512316794584,0.00594702367635226,0.039593478757892));
#37869=CARTESIAN_POINT('',(0.0180525517787113,0.00594301535819439,0.0397623614354607));
#37870=CARTESIAN_POINT('',(0.018211010758672,0.00599448261796389,0.039790601447071));
#37871=CARTESIAN_POINT('',(0.0183192930082589,0.00506137920236497,0.0395702177801257));
#37872=CARTESIAN_POINT('',(0.0183204096468456,0.00505733680610022,0.0397391088448937));
#37873=CARTESIAN_POINT('',(0.01848119299716,0.00510103722662414,0.0397673427472158));
#37874=CARTESIAN_POINT('',(0.0184375671426192,0.00461176875866541,0.039558593934693));
#37875=CARTESIAN_POINT('',(0.0184385674168231,0.00460777563908313,0.0397274423032781));
#37876=CARTESIAN_POINT('',(0.0186003367749354,0.00464745017759764,0.0397557104366488));
#37877=CARTESIAN_POINT('',(0.0187403696193654,0.00326308434116236,0.0395240534487004));
#37878=CARTESIAN_POINT('',(0.0187410285340265,0.00325922569557295,0.039692738761433));
#37879=CARTESIAN_POINT('',(0.0189052541067636,0.00328684376191785,0.0397211373335475));
#37880=CARTESIAN_POINT('',(0.0188754608754345,0.00235697139997309,0.039501263479842));
#37881=CARTESIAN_POINT('',(0.0188759732692699,0.00235290135231658,0.0396697996507904));
#37882=CARTESIAN_POINT('',(0.0190411319121178,0.00237273756414135,0.0396983185594243));
#37883=CARTESIAN_POINT('',(0.0190146343871304,0.000531052317676733,0.0394553276067802));
#37884=CARTESIAN_POINT('',(0.0190147467538104,0.000526926096965941,0.0396237985830803));
#37885=CARTESIAN_POINT('',(0.0191809803724045,0.000530781571160013,0.039652369114602));
#37886=CARTESIAN_POINT('',(0.0190186313319651,-0.000390183701124072,0.0394321458755341));
#37887=CARTESIAN_POINT('',(0.0190185238403849,-0.000394709366226374,0.0396006873315976));
#37888=CARTESIAN_POINT('',(0.0191848667598328,-0.000398521301419501,0.0396292028825932));
#37889=CARTESIAN_POINT('',(0.0188901598408957,-0.00224108059811265,0.039385203330183));
#37890=CARTESIAN_POINT('',(0.0188896397216407,-0.002245594987928,0.0395540134298593));
#37891=CARTESIAN_POINT('',(0.0190550980401844,-0.00226562263151752,0.0395823129296947));
#37892=CARTESIAN_POINT('',(0.0187592919286394,-0.00315070366996476,0.0393619574272701));
#37893=CARTESIAN_POINT('',(0.0187586023982082,-0.00315481802553601,0.0395309559011705));
#37894=CARTESIAN_POINT('',(0.0189230501531979,-0.00318320959294909,0.0395591022467701));
#37895=CARTESIAN_POINT('',(0.0183695100994604,-0.00493954107034915,0.0393160026007698));
#37896=CARTESIAN_POINT('',(0.0183684362350318,-0.00494351963126534,0.0394849528870032));
#37897=CARTESIAN_POINT('',(0.0185293451004069,-0.00498756854556453,0.03951313924705));
#37898=CARTESIAN_POINT('',(0.0181105844945499,-0.00581875143553138,0.0392932469575121));
#37899=CARTESIAN_POINT('',(0.0181094075575356,-0.00582245957346899,0.0394620130085385));
#37900=CARTESIAN_POINT('',(0.0182677162314112,-0.00587435703973338,0.0394903466503783));
#37901=CARTESIAN_POINT('',(0.0176238757386468,-0.00711419627923065,0.0392586871160342));
#37902=CARTESIAN_POINT('',(0.0176223390233472,-0.00711799882055952,0.0394272641248127));
#37903=CARTESIAN_POINT('',(0.0177762141027418,-0.00718095020999036,0.0394557503297173));
#37904=CARTESIAN_POINT('',(0.0174443626195664,-0.0075437181923097,0.0392470527849549));
#37905=CARTESIAN_POINT('',(0.0174427151918118,-0.00754752961849986,0.0394155815388059));
#37906=CARTESIAN_POINT('',(0.017594968480881,-0.0076141672192643,0.0394441065231024));
#37907=CARTESIAN_POINT('',(0.0170570743207949,-0.00838270165178186,0.0392238833103385));
#37908=CARTESIAN_POINT('',(0.017055236896513,-0.0083864394927787,0.0393923701383704));
#37909=CARTESIAN_POINT('',(0.0172040278677065,-0.00846038096201471,0.0394209284103667));
#37910=CARTESIAN_POINT('',(0.0168491312318907,-0.00879301415280329,0.0392123270661835));
#37911=CARTESIAN_POINT('',(0.0168471745089513,-0.00879676231529845,0.0393808173590088));
#37912=CARTESIAN_POINT('',(0.0169941627928814,-0.00887423627012989,0.0394093729459777));
#37913=CARTESIAN_POINT('',(0.0161833521667382,-0.00999701942034864,0.0391776573453862));
#37914=CARTESIAN_POINT('',(0.0161810727591944,-0.0100007222612511,0.0393462289924078));
#37915=CARTESIAN_POINT('',(0.0163223246381786,-0.0100886642409526,0.0393747193412268));
#37916=CARTESIAN_POINT('',(0.0156837813279877,-0.010763917526042,0.0391545287438872));
#37917=CARTESIAN_POINT('',(0.0156812560616843,-0.0107675778681655,0.0393232583031528));
#37918=CARTESIAN_POINT('',(0.0158183322906461,-0.0108622516976936,0.0393516221034215));
#37919=CARTESIAN_POINT('',(0.0148506052656618,-0.0118604490874667,0.0391197539368408));
#37920=CARTESIAN_POINT('',(0.0148479422599114,-0.0118637853368753,0.0392886298438068));
#37921=CARTESIAN_POINT('',(0.0149777130769401,-0.0119682589810861,0.0393168755614208));
#37922=CARTESIAN_POINT('',(0.0145588562855003,-0.0122169562012742,0.0391081591766584));
#37923=CARTESIAN_POINT('',(0.0145561740152432,-0.0122201533101118,0.0392770603641225));
#37924=CARTESIAN_POINT('',(0.0146833441921296,-0.0123278209611957,0.039305285685237));
#37925=CARTESIAN_POINT('',(0.0139465923348996,-0.0129115017488216,0.0390849487544811));
#37926=CARTESIAN_POINT('',(0.013943770796447,-0.0129145481191218,0.0392538016449171));
#37927=CARTESIAN_POINT('',(0.0140655078405243,-0.0130282424901708,0.0392820663107823));
#37928=CARTESIAN_POINT('',(0.0136268604230468,-0.0132484253304702,0.0390733528866772));
#37929=CARTESIAN_POINT('',(0.0136240004475653,-0.0132513693465652,0.0392421472865775));
#37930=CARTESIAN_POINT('',(0.0137428414645763,-0.0133679856135985,0.039270458921805));
#37931=CARTESIAN_POINT('',(0.0126400342360209,-0.0142154116865179,0.0390388473222273));
#37932=CARTESIAN_POINT('',(0.0126371160587943,-0.0142179882435716,0.0392074636684212));
#37933=CARTESIAN_POINT('',(0.01274698114767,-0.0143430328723232,0.0392359174436133));
#37934=CARTESIAN_POINT('',(0.0119408999779254,-0.0148072091698214,0.0390160292372545));
#37935=CARTESIAN_POINT('',(0.0119376451764601,-0.0148098347142087,0.0391845224127175));
#37936=CARTESIAN_POINT('',(0.0120414882136077,-0.014939730316981,0.0392130760164094));
#37937=CARTESIAN_POINT('',(0.0108314094346948,-0.0156169844585444,0.0389815148716734));
#37938=CARTESIAN_POINT('',(0.0108279596023054,-0.0156193773669341,0.0391500085767657));
#37939=CARTESIAN_POINT('',(0.0109220694615437,-0.0157563147823449,0.0391785612300089));
#37940=CARTESIAN_POINT('',(0.0104514076807421,-0.0158738715579762,0.0389699659783551));
#37941=CARTESIAN_POINT('',(0.0104478492511976,-0.0158762130743749,0.0391384844945757));
#37942=CARTESIAN_POINT('',(0.0105386895813438,-0.0160153790697043,0.0391670173443847));
#37943=CARTESIAN_POINT('',(0.00967075750576919,-0.0163611787476578,0.0389467298609994));
#37944=CARTESIAN_POINT('',(0.00966707931299868,-0.0163633545379347,0.03911534247122));
#37945=CARTESIAN_POINT('',(0.00975113060579868,-0.0165068460555297,0.0391437995424063));
#37946=CARTESIAN_POINT('',(0.00926909941956286,-0.0165921264293511,0.038935013836733));
#37947=CARTESIAN_POINT('',(0.00926533905731338,-0.0165942249251055,0.0391036939614964));
#37948=CARTESIAN_POINT('',(0.00934593266447067,-0.0167397810986317,0.0391320968632594));
#37949=CARTESIAN_POINT('',(0.00803891101736719,-0.0172405151791966,0.0388998173571397));
#37950=CARTESIAN_POINT('',(0.00803478692916257,-0.0172424556346622,0.0390687027422972));
#37951=CARTESIAN_POINT('',(0.00810491289056058,-0.0173937454431188,0.0390969418160552));
#37952=CARTESIAN_POINT('',(0.00719694598238467,-0.0176080046398765,0.0388766396692177));
#37953=CARTESIAN_POINT('',(0.00719321072406995,-0.0176095393284872,0.039045666972154));
#37954=CARTESIAN_POINT('',(0.00725554598247917,-0.0177643667872925,0.0390737899638824));
#37955=CARTESIAN_POINT('',(0.00547097376848593,-0.0182182958834193,0.0388308058862709));
#37956=CARTESIAN_POINT('',(0.00546714152685369,-0.0182194370884236,0.0389996812944908));
#37957=CARTESIAN_POINT('',(0.00551426182401809,-0.018379386571311,0.039027927476479));
#37958=CARTESIAN_POINT('',(0.00458696587175252,-0.0184610876513518,0.0388080477807771));
#37959=CARTESIAN_POINT('',(0.00458314615199965,-0.0184620486274569,0.0389767348121234));
#37960=CARTESIAN_POINT('',(0.00462238824093536,-0.0186238693783744,0.039005132143214));
#37961=CARTESIAN_POINT('',(0.0032286360895248,-0.0187293596339089,0.0387734340207107));
#37962=CARTESIAN_POINT('',(0.00322457741815377,-0.0187300579773913,0.0389419651805177));
#37963=CARTESIAN_POINT('',(0.00325205678091437,-0.0188939719824896,0.0389704880835262));
#37964=CARTESIAN_POINT('',(0.00276884731162698,-0.018802838132047,0.0387617786153882));
#37965=CARTESIAN_POINT('',(0.0027647144737126,-0.0188034470080187,0.0389302774843512));
#37966=CARTESIAN_POINT('',(0.00278821639135257,-0.0189679407842008,0.0389588263645261));
#37967=CARTESIAN_POINT('',(0.00185214901521399,-0.0189151468744101,0.0387385824745361));
#37968=CARTESIAN_POINT('',(0.00184797733394435,-0.0189155554236529,0.0389070729772705));
#37969=CARTESIAN_POINT('',(0.00186345704344516,-0.0190809879811251,0.0389356282183146));
#37970=CARTESIAN_POINT('',(0.00139400895517379,-0.0189543386481495,0.0387270101188289));
#37971=CARTESIAN_POINT('',(0.00138976923310706,-0.018954649465271,0.0388955215664241));
#37972=CARTESIAN_POINT('',(0.00140129624287683,-0.0191204303942124,0.038924060100892));
#37973=CARTESIAN_POINT('',(2.02044472024443E-5,-0.0190221042475243,0.0386923001021622));
#37974=CARTESIAN_POINT('',(1.57892815349546E-5,-0.0190221186024429,0.038860932720944));
#37975=CARTESIAN_POINT('',(1.54463184923638E-5,-0.0191885778823327,0.0388893743542784));
#37976=CARTESIAN_POINT('',(-0.000894847146022175,-0.0190011239467331,0.0386691556625014));
#37977=CARTESIAN_POINT('',(-0.000899209950171493,-0.019000911146055,0.0388379620111464));
#37978=CARTESIAN_POINT('',(-0.000907622778345695,-0.0191673736523758,0.0388662636778043));
#37979=CARTESIAN_POINT('',(-0.00226619172341018,-0.0188699560342946,0.0386344327853979));
#37980=CARTESIAN_POINT('',(-0.00227039970073797,-0.0188694512736974,0.0388033310914829));
#37981=CARTESIAN_POINT('',(-0.00229093120188463,-0.0190348059068781,0.0388315589464256));
#37982=CARTESIAN_POINT('',(-0.00272310077466777,-0.0188095535313365,0.0386228755156377));
#37983=CARTESIAN_POINT('',(-0.00272719692133164,-0.0188089615890709,0.0387917624583608));
#37984=CARTESIAN_POINT('',(-0.00275181268614869,-0.0189737424064369,0.0388199994159973));
#37985=CARTESIAN_POINT('',(-0.00363649386734613,-0.0186545033230575,0.0385996963066169));
#37986=CARTESIAN_POINT('',(-0.00364054066666757,-0.0186537130073739,0.038768495053176));
#37987=CARTESIAN_POINT('',(-0.00367313781043775,-0.0188170009701307,0.0387968032840231));
#37988=CARTESIAN_POINT('',(-0.00409075605437804,-0.0185601084600659,0.0385881226133647));
#37989=CARTESIAN_POINT('',(-0.0040947621471106,-0.0185592271993151,0.0387568547743207));
#37990=CARTESIAN_POINT('',(-0.00413133684550116,-0.018721587751719,0.0387852164985522));
#37991=CARTESIAN_POINT('',(-0.0054318056149998,-0.0182302806435945,0.0385536307897916));
#37992=CARTESIAN_POINT('',(-0.00543553993399363,-0.0182291542340229,0.0387221874031463));
#37993=CARTESIAN_POINT('',(-0.00548399425265249,-0.018388326153721,0.0387506890170043));
#37994=CARTESIAN_POINT('',(-0.00630289095283724,-0.0179474880114046,0.0385307760697278));
#37995=CARTESIAN_POINT('',(-0.00630691296692065,-0.0179460723628009,0.0386992425394241));
#37996=CARTESIAN_POINT('',(-0.00636260342768857,-0.0181027456265969,0.0387278177568434));
#37997=CARTESIAN_POINT('',(-0.00757562532439882,-0.0174304214239084,0.0384961973636378));
#37998=CARTESIAN_POINT('',(-0.00757950058939342,-0.0174287378520263,0.0386647159219878));
#37999=CARTESIAN_POINT('',(-0.00764637739074726,-0.017580874673372,0.038693248565823));
#38000=CARTESIAN_POINT('',(-0.00799419906197303,-0.0172425253962202,0.0384846255795232));
#38001=CARTESIAN_POINT('',(-0.00799808179991143,-0.0172407235900233,0.0386531854624822));
#38002=CARTESIAN_POINT('',(-0.00806858952341075,-0.0173912690974159,0.0386816850418112));
#38003=CARTESIAN_POINT('',(-0.00881982373767343,-0.0168351599314685,0.0384613513896509));
#38004=CARTESIAN_POINT('',(-0.0088236265238929,-0.0168331696460589,0.0386300286865617));
#38005=CARTESIAN_POINT('',(-0.00890140257395309,-0.016980241638005,0.0386584337931134));
#38006=CARTESIAN_POINT('',(-0.0092281569464443,-0.0166149242814184,0.0384496112284667));
#38007=CARTESIAN_POINT('',(-0.00923192123330994,-0.0166128313434524,0.0386183634345208));
#38008=CARTESIAN_POINT('',(-0.00931329725815699,-0.0167580465585342,0.0386467083577091));
#38009=CARTESIAN_POINT('',(-0.0104262512167785,-0.0159107398818068,0.0384144447107859));
#38010=CARTESIAN_POINT('',(-0.010430058486001,-0.0159082629531776,0.038583395354492));
#38011=CARTESIAN_POINT('',(-0.0105218200738479,-0.0160475866150257,0.0386115819744312));
#38012=CARTESIAN_POINT('',(-0.0111817027229834,-0.0153885444447047,0.0383913655628602));
#38013=CARTESIAN_POINT('',(-0.011184900762079,-0.0153862348573815,0.0385603823310762));
#38014=CARTESIAN_POINT('',(-0.0112837736795533,-0.0155206792071819,0.0385885137817382));
#38015=CARTESIAN_POINT('',(-0.0126091384792972,-0.014242450727376,0.0383456160376428));
#38016=CARTESIAN_POINT('',(-0.0126120620289027,-0.0142398454093418,0.0385144101986019));
#38017=CARTESIAN_POINT('',(-0.0127232467361194,-0.0143639888582395,0.0385427214008471));
#38018=CARTESIAN_POINT('',(-0.0132811162660052,-0.0136185486283295,0.0383228413906641));
#38019=CARTESIAN_POINT('',(-0.0132839880962257,-0.0136157600325511,0.0384914554416962));
#38020=CARTESIAN_POINT('',(-0.0134008120630799,-0.0137342997068811,0.0385199115843236));
#38021=CARTESIAN_POINT('',(-0.0145393021716353,-0.0122662793207722,0.0382766022493712));
#38022=CARTESIAN_POINT('',(-0.0145418913362455,-0.0122631986723181,0.0384450692067015));
#38023=CARTESIAN_POINT('',(-0.0146695491666348,-0.0123697456593811,0.0384736427431037));
#38024=CARTESIAN_POINT('',(-0.0151238750047054,-0.0115381541874378,0.0382531625212542));
#38025=CARTESIAN_POINT('',(-0.0151265669586711,-0.0115346068146102,0.038421653469323));
#38026=CARTESIAN_POINT('',(-0.0152590825261153,-0.0116351206443961,0.0384502094001571));
#38027=CARTESIAN_POINT('',(-0.015912946196592,-0.0103919821327371,0.0382180073303503));
#38028=CARTESIAN_POINT('',(-0.0159152891678387,-0.0103883973346115,0.0383866624251464));
#38029=CARTESIAN_POINT('',(-0.0160549201441163,-0.0104788084790954,0.038415085410731));
#38030=CARTESIAN_POINT('',(-0.0161622506892229,-0.00999971846528998,0.038206255530585));
#38031=CARTESIAN_POINT('',(-0.016164506233904,-0.00999606979149996,0.0383749782187102));
#38032=CARTESIAN_POINT('',(-0.0163063720435345,-0.0100830863974814,0.0384033468945532));
#38033=CARTESIAN_POINT('',(-0.0166284019221505,-0.00920374740210582,0.0381829405297265));
#38034=CARTESIAN_POINT('',(-0.0166304788976319,-0.0091999980748227,0.0383517776941159));
#38035=CARTESIAN_POINT('',(-0.0167765104297406,-0.00928009400932628,0.038380054478062));
#38036=CARTESIAN_POINT('',(-0.0168459427003453,-0.0087991026560107,0.0381713480300838));
#38037=CARTESIAN_POINT('',(-0.01684789442206,-0.00879536529539895,0.0383402335991688));
#38038=CARTESIAN_POINT('',(-0.0169958968586454,-0.00887187768206122,0.0383684712909901));
#38039=CARTESIAN_POINT('',(-0.0174528532182407,-0.00756557245685109,0.038136798429106));
#38040=CARTESIAN_POINT('',(-0.0174545163799049,-0.00756173319037529,0.0383056887441116));
#38041=CARTESIAN_POINT('',(-0.0176077926838441,-0.00762742152354258,0.0383339236141263));
#38042=CARTESIAN_POINT('',(-0.0177967463233965,-0.00671719229774001,0.0381140518336256));
#38043=CARTESIAN_POINT('',(-0.0177981441576787,-0.00671352296714926,0.0382827768219074));
#38044=CARTESIAN_POINT('',(-0.0179542998344343,-0.00677144528966483,0.0383111435427684));
#38045=CARTESIAN_POINT('',(-0.0183620354818313,-0.00496794776825526,0.0380681118033921));
#38046=CARTESIAN_POINT('',(-0.018363051915718,-0.00496414667738891,0.0382366207910613));
#38047=CARTESIAN_POINT('',(-0.0185238543331827,-0.0050066603498049,0.038265160581824));
#38048=CARTESIAN_POINT('',(-0.0185837873782487,-0.00406064450754518,0.0380447542023251));
#38049=CARTESIAN_POINT('',(-0.0185847093982919,-0.00405639286329004,0.0382132118941942));
#38050=CARTESIAN_POINT('',(-0.0187472682210555,-0.00409134689971549,0.0382417943471708));
#38051=CARTESIAN_POINT('',(-0.0188891167679676,-0.00224660963736494,0.0379983688731513));
#38052=CARTESIAN_POINT('',(-0.0188896422389133,-0.00224226097750333,0.0381669629359119));
#38053=CARTESIAN_POINT('',(-0.019054959181508,-0.00226136487600709,0.038195435365985));
#38054=CARTESIAN_POINT('',(-0.018975165678065,-0.0013350944840303,0.0379752144272462));
#38055=CARTESIAN_POINT('',(-0.0189754684707854,-0.00133060510680013,0.0381439802865186));
#38056=CARTESIAN_POINT('',(-0.0191417252033731,-0.0013418586227537,0.0381723150679244));
#38057=CARTESIAN_POINT('',(-0.0190054818029713,3.88443657746849E-5,0.0379404708993792));
#38058=CARTESIAN_POINT('',(-0.0190054745100075,4.31324813444525E-5,0.038109416100263));
#38059=CARTESIAN_POINT('',(-0.019172150328964,4.41105638862011E-5,0.038137605958912));
#38060=CARTESIAN_POINT('',(-0.0189990633653289,0.0004979394949072,0.0379288939423862));
#38061=CARTESIAN_POINT('',(-0.0189989535531816,0.000502132561226291,0.0380978803450399));
#38062=CARTESIAN_POINT('',(-0.0191656014577857,0.000507218265721521,0.0381260369267217));
#38063=CARTESIAN_POINT('',(-0.0189525853241847,0.00141840122316238,0.0379057637185006));
#38064=CARTESIAN_POINT('',(-0.0189522734866402,0.00142255874284645,0.0380747227358514));
#38065=CARTESIAN_POINT('',(-0.0191184478191296,0.00143571143768376,0.0381029019710031));
#38066=CARTESIAN_POINT('',(-0.0189122530979747,0.00188166508702157,0.037894151408753));
#38067=CARTESIAN_POINT('',(-0.0189118489177943,0.00188574527054257,0.038063053667648));
#38068=CARTESIAN_POINT('',(-0.0190775767604459,0.00190301444061339,0.0380912784925379));
#38069=CARTESIAN_POINT('',(-0.0187412890444881,0.00325883536209297,0.0378595082246926));
#38070=CARTESIAN_POINT('',(-0.0187406125358451,0.00326263690836655,0.0380282153208414));
#38071=CARTESIAN_POINT('',(-0.0189045331436087,0.0032921695621697,0.0380565962252799));
#38072=CARTESIAN_POINT('',(-0.0185618374760872,0.00415882992177338,0.0378366889422303));
#38073=CARTESIAN_POINT('',(-0.0185609491431853,0.00416281716727193,0.0380052367866357));
#38074=CARTESIAN_POINT('',(-0.0187231061596535,0.00419996532698986,0.0380337462943037));
#38075=CARTESIAN_POINT('',(-0.0180761523716431,0.00592371439588828,0.0377907874534993));
#38076=CARTESIAN_POINT('',(-0.0180748688338159,0.00592761944990612,0.0379592560582077));
#38077=CARTESIAN_POINT('',(-0.0182326246185282,0.00598016232025265,0.0379878284457428));
#38078=CARTESIAN_POINT('',(-0.0177699181807482,0.00678860415922227,0.0377677064269697));
#38079=CARTESIAN_POINT('',(-0.0177683037398952,0.0067927937783899,0.0379362404139646));
#38080=CARTESIAN_POINT('',(-0.0179235668226707,0.00685257390989074,0.0379647618166968));
#38081=CARTESIAN_POINT('',(-0.0172124925922568,0.00805877679345812,0.0377326384506189));
#38082=CARTESIAN_POINT('',(-0.0172106741003609,0.00806266492587303,0.0379013568168212));
#38083=CARTESIAN_POINT('',(-0.0173611188275609,0.00813380938310562,0.0379297289888462));
#38084=CARTESIAN_POINT('',(-0.0170100440513287,0.00847767119971143,0.0377208747988973));
#38085=CARTESIAN_POINT('',(-0.0170081349381613,0.00848149858679464,0.0378896612092541));
#38086=CARTESIAN_POINT('',(-0.0171568587931086,0.00855635316807159,0.0379179786338746));
#38087=CARTESIAN_POINT('',(-0.0165788942837513,0.00929261921778571,0.0376975970371511));
#38088=CARTESIAN_POINT('',(-0.0165768089937421,0.00929634189729705,0.0378664761540591));
#38089=CARTESIAN_POINT('',(-0.0167218201734232,0.00937836824818123,0.0378947193042335));
#38090=CARTESIAN_POINT('',(-0.0163494612799744,0.00969046055170924,0.0376860418887991));
#38091=CARTESIAN_POINT('',(-0.0163473352581449,0.00969404843687843,0.0378549427356594));
#38092=CARTESIAN_POINT('',(-0.0164902999149588,0.00977963570563989,0.0378831683516885));
#38093=CARTESIAN_POINT('',(-0.0156203482955152,0.0108556141477693,0.0376515924539111));
#38094=CARTESIAN_POINT('',(-0.0156180284090897,0.0108589406749027,0.0378204180917313));
#38095=CARTESIAN_POINT('',(-0.0157544376251322,0.0109547386773052,0.0378487044876896));
#38096=CARTESIAN_POINT('',(-0.0150800660109407,0.0115947011823282,0.0376288479886084));
#38097=CARTESIAN_POINT('',(-0.0150776530141183,0.0115978559373221,0.0377975020919996));
#38098=CARTESIAN_POINT('',(-0.0152090726333725,0.0117000441151153,0.0378259259415872));
#38099=CARTESIAN_POINT('',(-0.0138899671273516,0.0129967034129007,0.0375828447234847));
#38100=CARTESIAN_POINT('',(-0.0138872362715129,0.012999608535133,0.0377513232998163));
#38101=CARTESIAN_POINT('',(-0.0140080363523487,0.0131138898465719,0.0377798875104862));
#38102=CARTESIAN_POINT('',(-0.0132352395046215,0.0136628607595305,0.0375594358076555));
#38103=CARTESIAN_POINT('',(-0.0132320559776592,0.0136659307572992,0.0377279052139145));
#38104=CARTESIAN_POINT('',(-0.0133474072445037,0.01378571121355,0.0377564784160232));
#38105=CARTESIAN_POINT('',(-0.0118541866040858,0.0148769482366017,0.0375130004253377));
#38106=CARTESIAN_POINT('',(-0.0118507133088228,0.0148797301405445,0.037681662651709));
#38107=CARTESIAN_POINT('',(-0.0119540859306551,0.0150102460804287,0.0377100805846133));
#38108=CARTESIAN_POINT('',(-0.0111245971527733,0.0154299398798176,0.0374898310539834));
#38109=CARTESIAN_POINT('',(-0.0111210000172843,0.0154325211989581,0.0376586824095242));
#38110=CARTESIAN_POINT('',(-0.0112180880535137,0.0155680677046641,0.0376869480447593));
#38111=CARTESIAN_POINT('',(-0.00997220227959034,0.0161791566010563,0.0374551387958382));
#38112=CARTESIAN_POINT('',(-0.00996857621133361,0.0161813926709487,0.0376241191859782));
#38113=CARTESIAN_POINT('',(-0.0100554962773422,0.0163236603376851,0.0376522808569229));
#38114=CARTESIAN_POINT('',(-0.00957836420746147,0.0164154651534365,0.0374436011601459));
#38115=CARTESIAN_POINT('',(-0.00957477908506208,0.0164175580583187,0.0376125866569281));
#38116=CARTESIAN_POINT('',(-0.00965815868034406,0.016561933580948,0.0376407441702482));
#38117=CARTESIAN_POINT('',(-0.0087709104510153,0.0168607143073696,0.0374205183467233));
#38118=CARTESIAN_POINT('',(-0.00876724454505143,0.0168626198141756,0.0375894250550103));
#38119=CARTESIAN_POINT('',(-0.00884348370640528,0.0170107899134816,0.0376176464448556));
#38120=CARTESIAN_POINT('',(-0.00835552574480931,0.0170704106985969,0.0374089138537229));
#38121=CARTESIAN_POINT('',(-0.00835185234045116,0.0170722108662611,0.0375777503312692));
#38122=CARTESIAN_POINT('',(-0.00842437110571596,0.0172221429219192,0.0376060281742487));
#38123=CARTESIAN_POINT('',(-0.00709535000394028,0.0176496724016442,0.0373743041538517));
#38124=CARTESIAN_POINT('',(-0.00709177332643238,0.017651093352714,0.0375429359937664));
#38125=CARTESIAN_POINT('',(-0.00715290993974597,0.0178059340849104,0.0375713771896712));
#38126=CARTESIAN_POINT('',(-0.00623594483585662,0.0179708283088807,0.0373514569820704));
#38127=CARTESIAN_POINT('',(-0.00623201002423933,0.0179721951179589,0.0375199580659789));
#38128=CARTESIAN_POINT('',(-0.0062858482836886,0.018129549085295,0.0375485052860181));
#38129=CARTESIAN_POINT('',(-0.00447973693691539,0.0184870126055874,0.0373054773677039));
#38130=CARTESIAN_POINT('',(-0.00447566124786949,0.0184880002476111,0.0374739656879611));
#38131=CARTESIAN_POINT('',(-0.00451411766434778,0.0186497894895065,0.0375025224533009));
#38132=CARTESIAN_POINT('',(-0.00358293467330361,0.0186820427185273,0.0372823466294694));
#38133=CARTESIAN_POINT('',(-0.00357850782552124,0.0186828778714969,0.0374509379058908));
#38134=CARTESIAN_POINT('',(-0.00360943877298218,0.0188464195850049,0.037479413249492));
#38135=CARTESIAN_POINT('',(-0.00220875574312944,0.0188768491364344,0.0372472514308504));
#38136=CARTESIAN_POINT('',(-0.00220449059337534,0.0188773499285656,0.0374160326403601));
#38137=CARTESIAN_POINT('',(-0.0022232067701182,0.0190427855844601,0.0374443543460284));
#38138=CARTESIAN_POINT('',(-0.00174634370278357,0.0189251840013327,0.0372355034658549));
#38139=CARTESIAN_POINT('',(-0.00174210867013681,0.0189255738019317,0.0374043467624972));
#38140=CARTESIAN_POINT('',(-0.00175674155373469,0.0190914932990551,0.0374326184330959));
#38141=CARTESIAN_POINT('',(-0.000826925959229854,0.0189875880319355,0.0372122807955014));
#38142=CARTESIAN_POINT('',(-0.000822695137451099,0.018987772823908,0.0373811798831107));
#38143=CARTESIAN_POINT('',(-0.000829275233720999,0.0191542684591979,0.037409407128447));
#38144=CARTESIAN_POINT('',(-0.000368042929881957,0.0190019572021535,0.0372007721319376));
#38145=CARTESIAN_POINT('',(-0.000363906221962559,0.0190020383817323,0.0373696562651259));
#38146=CARTESIAN_POINT('',(-0.000366380226777539,0.0191686249449107,0.0373978955030339));
#38147=CARTESIAN_POINT('',(0.00100616796991394,0.0189954457294153,0.0371663944497608));
#38148=CARTESIAN_POINT('',(0.00101012857597821,0.0189952254684106,0.0373351479087102));
#38149=CARTESIAN_POINT('',(0.00101984822205786,0.0191615481916715,0.0373634919782864));
#38150=CARTESIAN_POINT('',(0.00191906942536007,0.0189252033176999,0.0371436379295908));
#38151=CARTESIAN_POINT('',(0.00192308311659654,0.0189248035834472,0.0373122263406783));
#38152=CARTESIAN_POINT('',(0.00194071232178894,0.0190902698078212,0.0373407031328573));
#38153=CARTESIAN_POINT('',(0.00373829288974369,0.0186513086496933,0.0370975552521172));
#38154=CARTESIAN_POINT('',(0.0037422675429787,0.0186505057536746,0.0372660211976757));
#38155=CARTESIAN_POINT('',(0.00377577997758983,0.0188133693612429,0.0372945956264843));
#38156=CARTESIAN_POINT('',(0.00464927567758443,0.0184452957233617,0.0370740963463626));
#38157=CARTESIAN_POINT('',(0.00465361877516417,0.0184441880652167,0.0372425962806732));
#38158=CARTESIAN_POINT('',(0.00469469620446711,0.0186053679006123,0.0372711450893036));
#38159=CARTESIAN_POINT('',(0.00640788824246925,0.0179104345821219,0.0370276234011098));
#38160=CARTESIAN_POINT('',(0.00641213455974086,0.0179089297463029,0.0371963613560363));
#38161=CARTESIAN_POINT('',(0.00646865877424517,0.0180656268478557,0.037224718661612));
#38162=CARTESIAN_POINT('',(0.00726207630727607,0.0175813053681433,0.0370044523100431));
#38163=CARTESIAN_POINT('',(0.00726606320926511,0.0175796532564351,0.037173385881105));
#38164=CARTESIAN_POINT('',(0.00733032923813791,0.0177335936136366,0.0372015848501821));
#38165=CARTESIAN_POINT('',(0.00850599272108748,0.0169958259732782,0.0369698402137862));
#38166=CARTESIAN_POINT('',(0.00850976493640867,0.0169939382644222,0.0371388274221191));
#38167=CARTESIAN_POINT('',(0.00858499122493516,0.0171427289552142,0.0371669838066493));
#38168=CARTESIAN_POINT('',(0.00891438003054646,0.0167853089728822,0.0369583414018185));
#38169=CARTESIAN_POINT('',(0.00891801964524323,0.0167833776381234,0.0371272959471482));
#38170=CARTESIAN_POINT('',(0.00899687630653875,0.0169302306085211,0.0371554785530948));
#38171=CARTESIAN_POINT('',(0.00971840175291147,0.016332955519842,0.0369352875453021));
#38172=CARTESIAN_POINT('',(0.00972192944744112,0.0163308544625574,0.0371041284248019));
#38173=CARTESIAN_POINT('',(0.00980775423010033,0.0164735976811781,0.0371324027994236));
#38174=CARTESIAN_POINT('',(0.010115519109279,0.0160900516915207,0.0369236852535701));
#38175=CARTESIAN_POINT('',(0.0101189831416029,0.0160878761573662,0.0370924497054347));
#38176=CARTESIAN_POINT('',(0.0102082411546516,0.0162283894770379,0.0371207855168135));
#38177=CARTESIAN_POINT('',(0.011270743586706,0.0153239779478668,0.0368890886031778));
#38178=CARTESIAN_POINT('',(0.0112738475288275,0.0153216765286443,0.0370576557087243));
#38179=CARTESIAN_POINT('',(0.0113732583737178,0.0154551150530701,0.0370861487868824));
#38180=CARTESIAN_POINT('',(0.0119960433226631,0.0147625421329569,0.0368662057002651));
#38181=CARTESIAN_POINT('',(0.0119993377869907,0.0147598621502207,0.0370346769756178));
#38182=CARTESIAN_POINT('',(0.0121047025895979,0.0148884994495844,0.0370632482888409));
#38183=CARTESIAN_POINT('',(0.0133594794395941,0.0135411230970551,0.0368201469046876));
#38184=CARTESIAN_POINT('',(0.0133625258969465,0.0135381225996254,0.0369886716378074));
#38185=CARTESIAN_POINT('',(0.0134798097341667,0.0136560742344555,0.0370171994129493));
#38186=CARTESIAN_POINT('',(0.0139976186714959,0.01288114301712,0.0367969732272835));
#38187=CARTESIAN_POINT('',(0.0140006506527497,0.0128778290839074,0.0369656331369593));
#38188=CARTESIAN_POINT('',(0.0141234832663436,0.0129902601921686,0.0369940531835233));
#38189=CARTESIAN_POINT('',(0.0148871651265421,0.0118146776498597,0.0367618712903768));
#38190=CARTESIAN_POINT('',(0.0148898311117952,0.0118113208332762,0.0369307085403116));
#38191=CARTESIAN_POINT('',(0.0150206911999236,0.0119143565375086,0.0369589852579205));
#38192=CARTESIAN_POINT('',(0.0151714138970381,0.0114472840332302,0.0367501501470596));
#38193=CARTESIAN_POINT('',(0.0151739527294179,0.0114439186647624,0.0369190362901996));
#38194=CARTESIAN_POINT('',(0.0153073745596128,0.0115437077107914,0.0369472735194286));
#38195=CARTESIAN_POINT('',(0.0157082289777055,0.0106987687962991,0.0367270025048148));
#38196=CARTESIAN_POINT('',(0.0157105865147794,0.0106953068463507,0.0368958908144695));
#38197=CARTESIAN_POINT('',(0.0158486853398397,0.0107885189926399,0.0369241269577371));
#38198=CARTESIAN_POINT('',(0.0159619428674269,0.0103163047026149,0.0367155289826961));
#38199=CARTESIAN_POINT('',(0.0159641782183735,0.0103128486834407,0.036884373293912));
#38200=CARTESIAN_POINT('',(0.0161044773088418,0.0104026139781047,0.0369126447041816));
#38201=CARTESIAN_POINT('',(0.0166797308494157,0.00914470502924076,0.0366811972170258));
#38202=CARTESIAN_POINT('',(0.0166816017193964,0.00914126628356073,0.0368498775850132));
#38203=CARTESIAN_POINT('',(0.0168280801599711,0.00922047590564887,0.0368782801257313));
#38204=CARTESIAN_POINT('',(0.0171006766352299,0.00833148822032756,0.0366584160864228));
#38205=CARTESIAN_POINT('',(0.0171024790722256,0.00832779764663219,0.0368269487267926));
#38206=CARTESIAN_POINT('',(0.017252357518434,0.00839995519488384,0.0368554704816954));
#38207=CARTESIAN_POINT('',(0.0176445139573953,0.00706277824544435,0.0366237857316965));
#38208=CARTESIAN_POINT('',(0.0176460648564801,0.00705890305230766,0.0367922715457667));
#38209=CARTESIAN_POINT('',(0.0178005846173115,0.00711997051471082,0.0368208306062401));
#38210=CARTESIAN_POINT('',(0.0178114967886425,0.00663064607588128,0.0366121409164746));
#38211=CARTESIAN_POINT('',(0.0178129748056691,0.00662667350514105,0.0367806354324629));
#38212=CARTESIAN_POINT('',(0.0179689296391234,0.00668401444243181,0.0368091876132652));
#38213=CARTESIAN_POINT('',(0.0181136579656142,0.00575415331218789,0.0365887630218576));
#38214=CARTESIAN_POINT('',(0.0181149468808211,0.00575009966218317,0.0367573264175973));
#38215=CARTESIAN_POINT('',(0.0182735869117889,0.0057997897582315,0.0367858230275019));
#38216=CARTESIAN_POINT('',(0.0182478310032561,0.00531297353456236,0.0365771140207169));
#38217=CARTESIAN_POINT('',(0.018249030517764,0.00530884742971662,0.0367457347909464));
#38218=CARTESIAN_POINT('',(0.0184088854457252,0.00535472955377455,0.0367741854134964));
#38219=CARTESIAN_POINT('',(0.018600988193285,0.00398087109094014,0.0365422440402653));
#38220=CARTESIAN_POINT('',(0.0186019530843162,0.00397643426041515,0.0367110601598061));
#38221=CARTESIAN_POINT('',(0.0187650148720769,0.00401092391464825,0.0367393548042703));
#38222=CARTESIAN_POINT('',(0.0187708608753656,0.00308142894533311,0.0365190923932619));
#38223=CARTESIAN_POINT('',(0.0187715368712848,0.00307732305295663,0.0366880943303872));
#38224=CARTESIAN_POINT('',(0.0189363401960049,0.00310359636864942,0.0367162378719251));
#38225=CARTESIAN_POINT('',(0.0189279634989396,0.00171531436468066,0.0364845827643801));
#38226=CARTESIAN_POINT('',(0.0189283390501015,0.00171116260852284,0.0366535411453261));
#38227=CARTESIAN_POINT('',(0.0190944145090531,0.00172549529433406,0.0366817208931037));
#38228=CARTESIAN_POINT('',(0.018963983478816,0.00125710692474757,0.0364731051806145));
#38229=CARTESIAN_POINT('',(0.0189642564545632,0.00125301548742518,0.0366420074484449));
#38230=CARTESIAN_POINT('',(0.0191305660401824,0.00126326236653834,0.0366702322676994));
#38231=CARTESIAN_POINT('',(0.0190026530986991,0.00033490657735888,0.0364500633580356));
#38232=CARTESIAN_POINT('',(0.0190027232547102,0.000330815741490651,0.0366188320274701));
#38233=CARTESIAN_POINT('',(0.0191691840164528,0.00033297175633165,0.0366471644579997));
#38234=CARTESIAN_POINT('',(0.019005161708661,-0.000130707036364811,0.0364384584739173));
#38235=CARTESIAN_POINT('',(0.0190051352620632,-0.000134805107419141,0.0366071509145178));
#38236=CARTESIAN_POINT('',(0.0191715078304247,-0.000136721059686821,0.0366355446099033));
#38237=CARTESIAN_POINT('',(0.018961975556038,-0.00151542291755907,0.0364038573031784));
#38238=CARTESIAN_POINT('',(0.0189616516139013,-0.0015193124786197,0.036572373712744));
#38239=CARTESIAN_POINT('',(0.0191273800290963,-0.00153354890875932,0.0366009074512625));
#38240=CARTESIAN_POINT('',(0.0188665153486165,-0.0024274179881491,0.0363809331684296));
#38241=CARTESIAN_POINT('',(0.0188659579023432,-0.00243170631394234,0.0365493931119482));
#38242=CARTESIAN_POINT('',(0.0190307969644883,-0.00245349709780482,0.0365779736750566));
#38243=CARTESIAN_POINT('',(0.018545820612552,-0.00422969234056243,0.0363347989938727));
#38244=CARTESIAN_POINT('',(0.0185448595612686,-0.00423393749797188,0.0365033744097998));
#38245=CARTESIAN_POINT('',(0.0187069583442499,-0.00427150106843692,0.0365318617477388));
#38246=CARTESIAN_POINT('',(0.0183205926808351,-0.00511997279119293,0.0363115915560491));
#38247=CARTESIAN_POINT('',(0.0183193857280646,-0.00512425118141887,0.03648032703392));
#38248=CARTESIAN_POINT('',(0.0184797066320657,-0.00516956856814049,0.0365086860629788));
#38249=CARTESIAN_POINT('',(0.0178818398582988,-0.00643850624540062,0.0362765066738982));
#38250=CARTESIAN_POINT('',(0.0178803952622417,-0.00644252177524659,0.0364453859504565));
#38251=CARTESIAN_POINT('',(0.0180369260922356,-0.0064995733336445,0.0364736289751795));
#38252=CARTESIAN_POINT('',(0.0177192671303535,-0.00687309947165825,0.0362648324652074));
#38253=CARTESIAN_POINT('',(0.0177177597326137,-0.00687698699387712,0.0364337333983774));
#38254=CARTESIAN_POINT('',(0.0178728419492951,-0.00693792755685441,0.0364619589459061));
#38255=CARTESIAN_POINT('',(0.0173656132613296,-0.00772317292581675,0.0362417572165986));
#38256=CARTESIAN_POINT('',(0.0173639262756046,-0.00772696373847354,0.0364106054406504));
#38257=CARTESIAN_POINT('',(0.0175158214621759,-0.00779531716318344,0.0364388738637441));
#38258=CARTESIAN_POINT('',(0.0171740610956206,-0.0081401059249469,0.0362303035090353));
#38259=CARTESIAN_POINT('',(0.0171723044984121,-0.00814381578093226,0.0363990930090974));
#38260=CARTESIAN_POINT('',(0.0173224233726417,-0.0082158214229691,0.0364274085936535));
#38261=CARTESIAN_POINT('',(0.0165559248141777,-0.00936697120146884,0.0361959942743846));
#38262=CARTESIAN_POINT('',(0.0165539948838148,-0.00937035510245631,0.0363646063064641));
#38263=CARTESIAN_POINT('',(0.0166983735051786,-0.00945317342502582,0.0363930635492081));
#38264=CARTESIAN_POINT('',(0.0160860880286729,-0.010153094424609,0.0361731779386068));
#38265=CARTESIAN_POINT('',(0.016083853004231,-0.0101566361433608,0.0363416684933638));
#38266=CARTESIAN_POINT('',(0.0162241091707267,-0.0102459909534076,0.0363702242164136));
#38267=CARTESIAN_POINT('',(0.0152933608774182,-0.0112838380743594,0.0361384739484449));
#38268=CARTESIAN_POINT('',(0.0152908671216402,-0.0112872183148005,0.0363069689458261));
#38269=CARTESIAN_POINT('',(0.0154241499532452,-0.0113864396905706,0.0363355205556882));
#38270=CARTESIAN_POINT('',(0.0150134609046653,-0.0116537805840718,0.0361267920987623));
#38271=CARTESIAN_POINT('',(0.0150108462100671,-0.0116571471098475,0.0362953136654874));
#38272=CARTESIAN_POINT('',(0.0151417283120323,-0.0117595700123999,0.0363238440647179));
#38273=CARTESIAN_POINT('',(0.0144276705469642,-0.0123716180358861,0.0361033948396687));
#38274=CARTESIAN_POINT('',(0.0144248879956393,-0.0123748653478363,0.0362720137224976));
#38275=CARTESIAN_POINT('',(0.0145507063085901,-0.0124836165091143,0.0363004657579308));
#38276=CARTESIAN_POINT('',(0.0141233515699902,-0.0127177757869468,0.0360917386081692));
#38277=CARTESIAN_POINT('',(0.0141204692867383,-0.0127209738099472,0.036260425760229));
#38278=CARTESIAN_POINT('',(0.0142436908282717,-0.0128327805268058,0.0362888230033628));
#38279=CARTESIAN_POINT('',(0.0131770131949719,-0.0137189593412155,0.0360568696793308));
#38280=CARTESIAN_POINT('',(0.0131737412271933,-0.0137221233895215,0.0362257603444948));
#38281=CARTESIAN_POINT('',(0.0132889779293669,-0.0138426541031448,0.0362539951485338));
#38282=CARTESIAN_POINT('',(0.0125017814668455,-0.0143368853017285,0.0360337816477872));
#38283=CARTESIAN_POINT('',(0.0124987491438331,-0.0143395397828666,0.0362028095268066));
#38284=CARTESIAN_POINT('',(0.0126077753735881,-0.0144659152885397,0.0362309320457858));
#38285=CARTESIAN_POINT('',(0.0114227446193982,-0.0151898357581618,0.0359993506669855));
#38286=CARTESIAN_POINT('',(0.0114194417068658,-0.0151923179076328,0.0361682566460626));
#38287=CARTESIAN_POINT('',(0.0115189958909884,-0.0153259415942862,0.0361964786244854));
#38288=CARTESIAN_POINT('',(0.0110519919396605,-0.0154617814951672,0.0359878837661081));
#38289=CARTESIAN_POINT('',(0.0110486648770015,-0.0154641620043371,0.0361567203751101));
#38290=CARTESIAN_POINT('',(0.0111448792418167,-0.0156001083291818,0.0361849981130821));
#38291=CARTESIAN_POINT('',(0.0102878646876576,-0.0159803958964433,0.0359648386603841));
#38292=CARTESIAN_POINT('',(0.0102844273139459,-0.0159826064635074,0.0361335349989411));
#38293=CARTESIAN_POINT('',(0.0103738367441834,-0.0161229349409537,0.036161925518539));
#38294=CARTESIAN_POINT('',(0.0098932911377497,-0.0162276251860447,0.0359532272935491));
#38295=CARTESIAN_POINT('',(0.00988978065682202,-0.0162297670937197,0.0361218530719544));
#38296=CARTESIAN_POINT('',(0.0099757011286439,-0.0163721603468361,0.0361503002884256));
#38297=CARTESIAN_POINT('',(0.00869387420900978,-0.0169194759404076,0.035918607098746));
#38298=CARTESIAN_POINT('',(0.00869034660227495,-0.0169212768624291,0.0360870893761529));
#38299=CARTESIAN_POINT('',(0.00876551477290953,-0.0170696169282755,0.0361156505378651));
#38300=CARTESIAN_POINT('',(0.00786843804549885,-0.0173183579629828,0.0358956386852973));
#38301=CARTESIAN_POINT('',(0.00786443472044417,-0.0173201673320902,0.0360641062936784));
#38302=CARTESIAN_POINT('',(0.0079327484477341,-0.0174717737992693,0.0360926808363628));
#38303=CARTESIAN_POINT('',(0.00616721922613437,-0.0179945338040935,0.0358494377904948));
#38304=CARTESIAN_POINT('',(0.00616304254324382,-0.0179959756148133,0.0360180747453525));
#38305=CARTESIAN_POINT('',(0.00621652364098048,-0.0181536144369596,0.0360465129090835));
#38306=CARTESIAN_POINT('',(0.00529144001220449,-0.0182718361121899,0.0358262080660678));
#38307=CARTESIAN_POINT('',(0.0052872486792983,-0.0182730424973861,0.0359950206772658));
#38308=CARTESIAN_POINT('',(0.00533305796727003,-0.0184333095392014,0.036023317273135));
#38309=CARTESIAN_POINT('',(0.00393855418278351,-0.0185930800037985,0.0357911672875431));
#38310=CARTESIAN_POINT('',(0.00393441101622293,-0.0185939582056733,0.0359600665272096));
#38311=CARTESIAN_POINT('',(0.00396828548438073,-0.0187571049648598,0.0359882936532595));
#38312=CARTESIAN_POINT('',(0.00348406197957908,-0.0186834968768611,0.0357795515499011));
#38313=CARTESIAN_POINT('',(0.00347999570770636,-0.0186842562470553,0.0359484353312303));
#38314=CARTESIAN_POINT('',(0.00350979662203613,-0.0188481742293118,0.0359766748522456));
#38315=CARTESIAN_POINT('',(0.00257552661300216,-0.0188302524170799,0.0357565296715141));
#38316=CARTESIAN_POINT('',(0.00257144268580103,-0.0188308095699434,0.035925322804152));
#38317=CARTESIAN_POINT('',(0.00259325999889579,-0.0189958767125214,0.0359536355516433));
#38318=CARTESIAN_POINT('',(0.00212033184012026,-0.018886869367471,0.0357450875726116));
#38319=CARTESIAN_POINT('',(0.00211625489474283,-0.0188873287106048,0.0359138145667818));
#38320=CARTESIAN_POINT('',(0.00213405629354057,-0.0190527966293634,0.0359421804492124));
#38321=CARTESIAN_POINT('',(0.000752012093046373,-0.0190071840175358,0.035710780080294));
#38322=CARTESIAN_POINT('',(0.000748109685983577,-0.0190073255153809,0.0358793332535717));
#38323=CARTESIAN_POINT('',(0.000753706604604977,-0.0191736087781649,0.0359078376370782));
#38324=CARTESIAN_POINT('',(-0.000163833649728999,-0.0190216050376802,0.0356879200859886));
#38325=CARTESIAN_POINT('',(-0.000168104459227904,-0.0190215649227648,0.035856385020059));
#38326=CARTESIAN_POINT('',(-0.000170161240575154,-0.0191878298444561,0.035884961489837));
#38327=CARTESIAN_POINT('',(-0.00154313375493487,-0.0189428301246924,0.0356531407796446));
#38328=CARTESIAN_POINT('',(-0.00154734732021483,-0.018942487564402,0.0358216619959281));
#38329=CARTESIAN_POINT('',(-0.00156152930468212,-0.0191080719713565,0.0358501925027523));
#38330=CARTESIAN_POINT('',(-0.00200553802655285,-0.0188995280394954,0.035641425773187));
#38331=CARTESIAN_POINT('',(-0.00200979696251775,-0.0188990745436516,0.0358099902070311));
#38332=CARTESIAN_POINT('',(-0.00202797804982009,-0.0190643219579432,0.0358384861311067));
#38333=CARTESIAN_POINT('',(-0.00292365854862329,-0.0187794186167379,0.0356180154682183));
#38334=CARTESIAN_POINT('',(-0.0029279022118001,-0.0187787597635309,0.0357866999464391));
#38335=CARTESIAN_POINT('',(-0.00295412988974707,-0.0189430592887084,0.0358150992871516));
#38336=CARTESIAN_POINT('',(-0.00337795740793425,-0.0187029448940798,0.0356063569578135));
#38337=CARTESIAN_POINT('',(-0.00338219373654105,-0.0187021778709024,0.0357751163672398));
#38338=CARTESIAN_POINT('',(-0.00341240350341812,-0.0188658828347146,0.0358034554891367));
#38339=CARTESIAN_POINT('',(-0.00472692781808232,-0.0184255021436554,0.0355715087063121));
#38340=CARTESIAN_POINT('',(-0.00473132273337695,-0.0184243896130631,0.035740463350948));
#38341=CARTESIAN_POINT('',(-0.00477316172383682,-0.0185858864378482,0.0357686467238541));
#38342=CARTESIAN_POINT('',(-0.00560774563104161,-0.0181767552827158,0.0355485132903271));
#38343=CARTESIAN_POINT('',(-0.00561151282205915,-0.0181756053784645,0.035717528399292));
#38344=CARTESIAN_POINT('',(-0.00566162890118377,-0.0183347876745961,0.035745661182169));
#38345=CARTESIAN_POINT('',(-0.00690130839944473,-0.0177082538182991,0.0355141335005034));
#38346=CARTESIAN_POINT('',(-0.00690513394921139,-0.0177067610821227,0.0356829736687975));
#38347=CARTESIAN_POINT('',(-0.00696632560854634,-0.0178616695579185,0.0357112486182751));
#38348=CARTESIAN_POINT('',(-0.00732786701516761,-0.0175361287238716,0.0355026692113962));
#38349=CARTESIAN_POINT('',(-0.00733164200843698,-0.017534553312147,0.0356714338948254));
#38350=CARTESIAN_POINT('',(-0.0073965431904294,-0.0176878468471484,0.0356997695200506));
#38351=CARTESIAN_POINT('',(-0.00817151566703478,-0.0171592475742844,0.0354796072250903));
#38352=CARTESIAN_POINT('',(-0.00817520837825819,-0.0171574869932219,0.0356482364567335));
#38353=CARTESIAN_POINT('',(-0.00824742094186209,-0.0173073061966473,0.0356766808108588));
#38354=CARTESIAN_POINT('',(-0.00858934050716055,-0.0169539387269213,0.0354679864751644));
#38355=CARTESIAN_POINT('',(-0.00859302665771972,-0.0169520724615698,0.0356365553227494));
#38356=CARTESIAN_POINT('',(-0.00866882261477138,-0.01710003058645,0.0356650481939536));
#38357=CARTESIAN_POINT('',(-0.00980833503611941,-0.0162987054282184,0.035433336011985));
#38358=CARTESIAN_POINT('',(-0.00981178625827609,-0.016296620164032,0.0356018022451308));
#38359=CARTESIAN_POINT('',(-0.00989827033312281,-0.0164386371414768,0.0356303763771952));
#38360=CARTESIAN_POINT('',(-0.0105818582595534,-0.0158070307930283,0.035410322798043));
#38361=CARTESIAN_POINT('',(-0.0105855487126754,-0.0158045469626697,0.0355788165800883));
#38362=CARTESIAN_POINT('',(-0.010678461477246,-0.0159424955200915,0.0356073702040998));
#38363=CARTESIAN_POINT('',(-0.0120524426450354,-0.0147165407961638,0.0353640686396772));
#38364=CARTESIAN_POINT('',(-0.0120559075893778,-0.0147137185160198,0.0355327736044921));
#38365=CARTESIAN_POINT('',(-0.0121617899069155,-0.0148422678510516,0.0355611573495344));
#38366=CARTESIAN_POINT('',(-0.0127495106129697,-0.0141177348621299,0.0353408302732254));
#38367=CARTESIAN_POINT('',(-0.0127526531198844,-0.0141148948912311,0.0355097152778329));
#38368=CARTESIAN_POINT('',(-0.0128649418112909,-0.0142381832734485,0.0355379531024191));
#38369=CARTESIAN_POINT('',(-0.0140640980308915,-0.0128086535235012,0.035294208453188));
#38370=CARTESIAN_POINT('',(-0.0140669123797478,-0.0128055615864941,0.0354630977749176));
#38371=CARTESIAN_POINT('',(-0.0141906727480833,-0.0129173343768273,0.0354913334496882));
#38372=CARTESIAN_POINT('',(-0.0146674069019048,-0.0121122061437758,0.0352713151253847));
#38373=CARTESIAN_POINT('',(-0.0146699184948938,-0.0121091832973698,0.035440036275915));
#38374=CARTESIAN_POINT('',(-0.0147989395557303,-0.0122144984851512,0.0354684060970901));
#38375=CARTESIAN_POINT('',(-0.0157641239006939,-0.0106456921117857,0.0352255501119424));
#38376=CARTESIAN_POINT('',(-0.0157663186936035,-0.0106424218237481,0.0353940576562385));
#38377=CARTESIAN_POINT('',(-0.0159046881144227,-0.0107347128770398,0.0354225986144043));
#38378=CARTESIAN_POINT('',(-0.0162586300252783,-0.00987451380899395,0.0352026403041944));
#38379=CARTESIAN_POINT('',(-0.0162608829420131,-0.00987079107989347,0.0353710978626173));
#38380=CARTESIAN_POINT('',(-0.0164032860051871,-0.00995663241126164,0.0353996804267765));
#38381=CARTESIAN_POINT('',(-0.0169180517691241,-0.00865978017347781,0.0351677876717183));
#38382=CARTESIAN_POINT('',(-0.016919990653101,-0.00865599475686332,0.0353363508374712));
#38383=CARTESIAN_POINT('',(-0.0170682756651896,-0.00873114150250666,0.0353648476304432));
#38384=CARTESIAN_POINT('',(-0.0171248289518239,-0.0082434408190218,0.0351560446564631));
#38385=CARTESIAN_POINT('',(-0.0171266915858875,-0.00823956726551623,0.0353246654407593));
#38386=CARTESIAN_POINT('',(-0.0172768170667127,-0.008311131019232,0.0353531160574958));
#38387=CARTESIAN_POINT('',(-0.0175057833600715,-0.00740011027729877,0.035132630000989));
#38388=CARTESIAN_POINT('',(-0.0175074618837968,-0.00739614457712032,0.0353013859018486));
#38389=CARTESIAN_POINT('',(-0.017661032054276,-0.00746037704417608,0.0353297278574223));
#38390=CARTESIAN_POINT('',(-0.0176798425091695,-0.00697379259955303,0.0351209752849925));
#38391=CARTESIAN_POINT('',(-0.0176814170602976,-0.00696979623835056,0.0352898076032935));
#38392=CARTESIAN_POINT('',(-0.0178365863050473,-0.00703031247343333,0.0353180880602619));
#38393=CARTESIAN_POINT('',(-0.0181539581319484,-0.0056812200825124,0.0350861705288966));
#38394=CARTESIAN_POINT('',(-0.0181553082467342,-0.00567694642197531,0.0352551707870785));
#38395=CARTESIAN_POINT('',(-0.0183147029008516,-0.00572637091688139,0.0352833174288937));
#38396=CARTESIAN_POINT('',(-0.0184061981139469,-0.00480141276233039,0.035063277094861));
#38397=CARTESIAN_POINT('',(-0.0184071921267651,-0.00479765830709078,0.03523225027595));
#38398=CARTESIAN_POINT('',(-0.0185688744888827,-0.00483879487407327,0.0352604168793913));
#38399=CARTESIAN_POINT('',(-0.0186889294040412,-0.00345461157176816,0.0350289233414967));
#38400=CARTESIAN_POINT('',(-0.018689671368071,-0.00345058715816061,0.0351976913984222));
#38401=CARTESIAN_POINT('',(-0.0188535109674506,-0.00348008264673463,0.0352260243248854));
#38402=CARTESIAN_POINT('',(-0.0187671737170645,-0.00300114582666555,0.0350174544050953));
#38403=CARTESIAN_POINT('',(-0.0187678225433682,-0.00299709954103612,0.035186147134013));
#38404=CARTESIAN_POINT('',(-0.0189322391930674,-0.00302261047148245,0.0352145405972404));
#38405=CARTESIAN_POINT('',(-0.0188909159202362,-0.00208494155648397,0.0349943638038464));
#38406=CARTESIAN_POINT('',(-0.0188913643710508,-0.00208086367720278,0.0351629355397262));
#38407=CARTESIAN_POINT('',(-0.0190566924975937,-0.00209833028062096,0.0351914259662282));
#38408=CARTESIAN_POINT('',(-0.0189362711550871,-0.00162179856622392,0.0349827318494094));
#38409=CARTESIAN_POINT('',(-0.0189366263747109,-0.00161765906985487,0.0351512568869062));
#38410=CARTESIAN_POINT('',(-0.019102274027967,-0.00163111402455153,0.0351797848456837));
#38411=CARTESIAN_POINT('',(-0.0190208368298371,-0.00024114246053665,0.0349480433217033));
#38412=CARTESIAN_POINT('',(-0.0190208853968919,-0.000237030054909648,0.0351165120695049));
#38413=CARTESIAN_POINT('',(-0.0191871591507164,-0.000238336653427598,0.0351450843400414));
#38414=CARTESIAN_POINT('',(-0.0190100560265515,0.000675166803218607,0.0349249873572056));
#38415=CARTESIAN_POINT('',(-0.0190098842172453,0.000679648750286042,0.0350935242556918));
#38416=CARTESIAN_POINT('',(-0.0191761360813997,0.000685993308868359,0.0351220432919113));
#38417=CARTESIAN_POINT('',(-0.0188570830529375,0.00249969979785826,0.0348786981384304));
#38418=CARTESIAN_POINT('',(-0.0188565049119517,0.00250416120399566,0.0350474721130656));
#38419=CARTESIAN_POINT('',(-0.0190216222788578,0.00252648896835062,0.0350758005679836));
#38420=CARTESIAN_POINT('',(-0.0187149048326804,0.00340792494756124,0.0348554874810762));
#38421=CARTESIAN_POINT('',(-0.0187141768543059,0.00341195073388233,0.0350244173224227));
#38422=CARTESIAN_POINT('',(-0.0188781294109306,0.00344264883378809,0.0350526189203356));
#38423=CARTESIAN_POINT('',(-0.0182935911308715,0.0052159504293076,0.0348089597471648));
#38424=CARTESIAN_POINT('',(-0.0182924738681908,0.00521984354838879,0.0349777832279153));
#38425=CARTESIAN_POINT('',(-0.018452547375611,0.00526634224321446,0.0350060713410159));
#38426=CARTESIAN_POINT('',(-0.0180194587189408,0.00609403747428862,0.0347861076178894));
#38427=CARTESIAN_POINT('',(-0.0180181939337391,0.0060978076924339,0.0349547581780811));
#38428=CARTESIAN_POINT('',(-0.0181755974548477,0.00615199150236652,0.0349831848912084));
#38429=CARTESIAN_POINT('',(-0.0173500477454275,0.00779833498209935,0.0347403003356644));
#38430=CARTESIAN_POINT('',(-0.0173484029273116,0.00780197274722938,0.0349087789228932));
#38431=CARTESIAN_POINT('',(-0.0174997017420979,0.00787097230989661,0.0349373431390131));
#38432=CARTESIAN_POINT('',(-0.0169546694139038,0.00862490930693604,0.0347173366651471));
#38433=CARTESIAN_POINT('',(-0.0169526543496618,0.00862884823398127,0.0348858068825127));
#38434=CARTESIAN_POINT('',(-0.0171006519871961,0.00870468149543935,0.0349143794419575));
#38435=CARTESIAN_POINT('',(-0.0162686860858967,0.00982559524458752,0.0346824162041079));
#38436=CARTESIAN_POINT('',(-0.0162664768054821,0.00982925613773177,0.0348510359353158));
#38437=CARTESIAN_POINT('',(-0.0164084926672397,0.00991579353543065,0.0348794872876429));
#38438=CARTESIAN_POINT('',(-0.0160233612223135,0.0102208476249506,0.0346706515686278));
#38439=CARTESIAN_POINT('',(-0.0160210437661859,0.0102244771619029,0.0348393400591364));
#38440=CARTESIAN_POINT('',(-0.016160983761665,0.0103144874313735,0.034867736231845));
#38441=CARTESIAN_POINT('',(-0.0155071783420045,0.0109882323829841,0.0346472437132341));
#38442=CARTESIAN_POINT('',(-0.0155046880682326,0.0109917502076387,0.0348160726583768));
#38443=CARTESIAN_POINT('',(-0.0156402140687233,0.0110885504931114,0.0348443559162426));
#38444=CARTESIAN_POINT('',(-0.0152364648233893,0.0113604855289649,0.0346356001016534));
#38445=CARTESIAN_POINT('',(-0.0152339091320912,0.0113639109933041,0.0348045006911381));
#38446=CARTESIAN_POINT('',(-0.0153670984922735,0.011464041519689,0.0348327262025861));
#38447=CARTESIAN_POINT('',(-0.0143873413094915,0.0124437284250746,0.0346008656037464));
#38448=CARTESIAN_POINT('',(-0.0143844751282124,0.0124470545266044,0.0347698845094911));
#38449=CARTESIAN_POINT('',(-0.0145103762353732,0.0125566260963977,0.0347980160624915));
#38450=CARTESIAN_POINT('',(-0.0137721352635693,0.0131213741649385,0.0345780643470608));
#38451=CARTESIAN_POINT('',(-0.0137694818893377,0.0131241809415071,0.0347469744606031));
#38452=CARTESIAN_POINT('',(-0.0138895112515776,0.0132399470206423,0.0347751919476471));
#38453=CARTESIAN_POINT('',(-0.0127756253635579,0.0140710319093379,0.0345437131909995));
#38454=CARTESIAN_POINT('',(-0.0127725972833309,0.0140737786150071,0.0347124090405052));
#38455=CARTESIAN_POINT('',(-0.012883865704725,0.014197492280553,0.0347407999552201));
#38456=CARTESIAN_POINT('',(-0.0124311249251211,0.0143764065730164,0.0345322328101261));
#38457=CARTESIAN_POINT('',(-0.0124280148068597,0.014379097791852,0.0347008592833387));
#38458=CARTESIAN_POINT('',(-0.0125362170837346,0.0145053941696239,0.0347293059401341));
#38459=CARTESIAN_POINT('',(-0.0117168670088797,0.0149642560908607,0.0345091027245447));
#38460=CARTESIAN_POINT('',(-0.0117136215730514,0.0149667956603315,0.0346776315441962));
#38461=CARTESIAN_POINT('',(-0.0118154798778907,0.0150981234397663,0.0347061563112278));
#38462=CARTESIAN_POINT('',(-0.0113471776301141,0.0152464405664509,0.0344974581748037));
#38463=CARTESIAN_POINT('',(-0.0113438235877949,0.015248937087422,0.0346659571752721));
#38464=CARTESIAN_POINT('',(-0.0114424601046325,0.0153826585151736,0.034694505939985));
#38465=CARTESIAN_POINT('',(-0.0102183752170634,0.0160447614000967,0.0344627249289449));
#38466=CARTESIAN_POINT('',(-0.0102148320542317,0.0160470183317958,0.0346312187415583));
#38467=CARTESIAN_POINT('',(-0.0103035592236308,0.0161876779090066,0.0346597711170653));
#38468=CARTESIAN_POINT('',(-0.00943380695794407,0.0165179153350184,0.0344396288436497));
#38469=CARTESIAN_POINT('',(-0.00942988974465749,0.0165201371650897,0.0346082295981398));
#38470=CARTESIAN_POINT('',(-0.00951206580947337,0.0166648848158917,0.0346366973123326));
#38471=CARTESIAN_POINT('',(-0.00780188490406774,0.0173484533223647,0.0343933234065022));
#38472=CARTESIAN_POINT('',(-0.00779777914175426,0.0173503145054647,0.034562171101279));
#38473=CARTESIAN_POINT('',(-0.00786576731965972,0.0175025251763002,0.0345904404061971));
#38474=CARTESIAN_POINT('',(-0.00695372238075959,0.0177061261627772,0.0343701512269808));
#38475=CARTESIAN_POINT('',(-0.00695002520057826,0.0177075890954631,0.034539100426332));
#38476=CARTESIAN_POINT('',(-0.0070101380881009,0.0178631977841725,0.0345672863120182));
#38477=CARTESIAN_POINT('',(-0.00519515796776929,0.018299494318991,0.0343237363307037));
#38478=CARTESIAN_POINT('',(-0.00519136109862996,0.0183005601040781,0.0344924904081236));
#38479=CARTESIAN_POINT('',(-0.00523596905492631,0.0184610903605914,0.034520833944751));
#38480=CARTESIAN_POINT('',(-0.00430497969731492,0.0185284965405738,0.0343009075934802));
#38481=CARTESIAN_POINT('',(-0.00430107815167976,0.0185294115816766,0.0344694813381066));
#38482=CARTESIAN_POINT('',(-0.00433788529026169,0.0186916714610529,0.0344979698502093));
#38483=CARTESIAN_POINT('',(-0.00250372476356489,0.0188565478430348,0.0342550702880657));
#38484=CARTESIAN_POINT('',(-0.00249972990529646,0.0188570709966858,0.034423500382658));
#38485=CARTESIAN_POINT('',(-0.00252074042207348,0.0190219709299539,0.0344521034780259));
#38486=CARTESIAN_POINT('',(-0.00159264608432865,0.0189555845333338,0.0342320626380529));
#38487=CARTESIAN_POINT('',(-0.0015881755748559,0.0189559473119425,0.0344005162798639));
#38488=CARTESIAN_POINT('',(-0.00160166636770651,0.0191216793941357,0.0344291022586503));
#38489=CARTESIAN_POINT('',(-0.000210002491991403,0.0190044356819909,0.034197081799291));
#38490=CARTESIAN_POINT('',(-0.000205708220503096,0.0190044849460703,0.0343657219829218));
#38491=CARTESIAN_POINT('',(-0.000206904170197636,0.0191708090168374,0.0343941568771733));
#38492=CARTESIAN_POINT('',(0.000255435682216471,0.0190039032550806,0.0341852994832117));
#38493=CARTESIAN_POINT('',(0.000259749403271307,0.0190038432168092,0.0343540184504881));
#38494=CARTESIAN_POINT('',(0.00026261141636447,0.0191702421981893,0.0343823900786291));
#38495=CARTESIAN_POINT('',(0.00117908482266063,0.0189690101296083,0.0341618973737084));
#38496=CARTESIAN_POINT('',(0.00118339102487519,0.0189687444916224,0.0343307637358417));
#38497=CARTESIAN_POINT('',(0.00119434650285929,0.019134972944291,0.0343590169212069));
#38498=CARTESIAN_POINT('',(0.0016379001804294,0.0189348266131091,0.034150262492255));
#38499=CARTESIAN_POINT('',(0.00164214190181302,0.0189344586555448,0.0343191982485964));
#38500=CARTESIAN_POINT('',(0.00165717600464392,0.0191004487829492,0.0343473954438282));
#38501=CARTESIAN_POINT('',(0.00300552223200003,0.01878319300841,0.0341155853588129));
#38502=CARTESIAN_POINT('',(0.00300979096658495,0.018782514997603,0.0342846031666856));
#38503=CARTESIAN_POINT('',(0.00303672412957713,0.0189472313784724,0.0343127355979453));
#38504=CARTESIAN_POINT('',(0.00390554832426864,0.0186169105380753,0.0340927041117735));
#38505=CARTESIAN_POINT('',(0.0039096582421905,0.0186160486743014,0.0342616778831394));
#38506=CARTESIAN_POINT('',(0.00394460615251096,0.0187792043180145,0.0342898449453726));
#38507=CARTESIAN_POINT('',(0.00568208757458414,0.0181536923652092,0.0340465762972639));
#38508=CARTESIAN_POINT('',(0.00568610013138219,0.0181524363616078,0.0342155462581155));
#38509=CARTESIAN_POINT('',(0.00573661376778426,0.0183114590571226,0.0342437162610204));
#38510=CARTESIAN_POINT('',(0.00656322007882397,0.0178543406867263,0.0340232170608366));
#38511=CARTESIAN_POINT('',(0.00656718587587333,0.017852881965957,0.0341922163861871));
#38512=CARTESIAN_POINT('',(0.00662541375372108,0.0180092844977502,0.0342203627200268));
#38513=CARTESIAN_POINT('',(0.00741375790559362,0.0174938901824966,0.0340000000000022));
#38514=CARTESIAN_POINT('',(0.00741762796059613,0.0174922500869792,0.0341689995579578));
#38515=CARTESIAN_POINT('',(0.00748331487893838,0.0176454543212183,0.0341971457690361));
#38516=CARTESIAN_POINT('',(0.00749179746249453,0.0176780363949439,0.0340000000000022));
#38517=CARTESIAN_POINT('',(0.00748331487893831,0.0176454543212184,0.0341971457690361));
#38518=CARTESIAN_POINT('',(0.00741375790559352,0.0174938901824966,0.034));
#38519=CARTESIAN_POINT('',(-0.019,0.,0.0349419586621878));
#38520=CARTESIAN_POINT('',(-0.019,0.00312176764345404,0.0348634621070055));
#38521=CARTESIAN_POINT('',(-0.0174298121913408,0.00936163759178525,0.0347064689966408));
#38522=CARTESIAN_POINT('',(-0.0109250154031967,0.0164955140888929,0.0344709793310939));
#38523=CARTESIAN_POINT('',(-0.00181847642276099,0.0197010597411713,0.034235489665547));
#38524=CARTESIAN_POINT('',(0.00453944946718008,0.0187119970007115,0.0340784965551823));
#38525=CARTESIAN_POINT('',(0.00741375790559356,0.0174938901824965,0.034));
#38526=CARTESIAN_POINT('',(-0.019,-3.2076351825911E-17,0.0349419586621878));
#38527=CARTESIAN_POINT('',(0.019,-3.9861646017376E-17,0.0364417130293248));
#38528=CARTESIAN_POINT('',(0.019,-0.00248709418409196,0.0363792232640274));
#38529=CARTESIAN_POINT('',(0.0180107055600589,-0.00746012312352682,0.0362542437334327));
#38530=CARTESIAN_POINT('',(0.0137847972460806,-0.0137848390811387,0.0360667744375406));
#38531=CARTESIAN_POINT('',(0.00746027851088484,-0.0180106936071852,0.0358793051416484));
#38532=CARTESIAN_POINT('',(-6.51922979228107E-17,-0.0194946531964074,0.0356918358457563));
#38533=CARTESIAN_POINT('',(-0.00746027851088496,-0.0180106936071851,0.0355043665498642));
#38534=CARTESIAN_POINT('',(-0.0137847972460807,-0.0137848390811386,0.035316897253972));
#38535=CARTESIAN_POINT('',(-0.0180107055600589,-0.00746012312352672,0.0351294279580799));
#38536=CARTESIAN_POINT('',(-0.019,-0.00248709418409184,0.0350044484274852));
#38537=CARTESIAN_POINT('',(-0.019,7.9723292034752E-17,0.0349419586621878));
#38538=CARTESIAN_POINT('',(0.019,-3.3932914654129E-18,0.0364417130293248));
#38539=CARTESIAN_POINT('',(-0.019,0.,0.0379414621394879));
#38540=CARTESIAN_POINT('',(-0.019,0.00248709418409192,0.0378789725932311));
#38541=CARTESIAN_POINT('',(-0.0180107055600589,0.00746012312352679,0.0377539935007175));
#38542=CARTESIAN_POINT('',(-0.0137847972460807,0.0137848390811386,0.0375665248619471));
#38543=CARTESIAN_POINT('',(-0.00746027851088488,0.0180106936071852,0.0373790562231767));
#38544=CARTESIAN_POINT('',(2.09173148415435E-17,0.0194946531964074,0.0371915875844063));
#38545=CARTESIAN_POINT('',(0.00746027851088491,0.0180106936071852,0.037004118945636));
#38546=CARTESIAN_POINT('',(0.0137847972460807,0.0137848390811386,0.0368166503068656));
#38547=CARTESIAN_POINT('',(0.0180107055600589,0.00746012312352675,0.0366291816680952));
#38548=CARTESIAN_POINT('',(0.019,0.00248709418409188,0.0365042025755816));
#38549=CARTESIAN_POINT('',(0.019,-3.9861646017376E-17,0.0364417130293248));
#38550=CARTESIAN_POINT('',(-0.019,2.6601721082709E-17,0.0379414621394879));
#38551=CARTESIAN_POINT('',(0.019,6.13906938284383E-17,0.0394419409570244));
#38552=CARTESIAN_POINT('',(0.019,-0.00248709418409186,0.0393794210062937));
#38553=CARTESIAN_POINT('',(0.0180107055600589,-0.00746012312352674,0.0392543811048323));
#38554=CARTESIAN_POINT('',(0.0137847972460807,-0.0137848390811386,0.0390668212526403));
#38555=CARTESIAN_POINT('',(0.00746027851088491,-0.0180106936071852,0.0388792614004482));
#38556=CARTESIAN_POINT('',(-2.12659367555693E-17,-0.0194946531964074,0.0386917015482561));
#38557=CARTESIAN_POINT('',(-0.00746027851088491,-0.0180106936071852,0.0385041416960641));
#38558=CARTESIAN_POINT('',(-0.0137847972460807,-0.0137848390811386,0.038316581843872));
#38559=CARTESIAN_POINT('',(-0.0180107055600589,-0.00746012312352674,0.03812902199168));
#38560=CARTESIAN_POINT('',(-0.019,-0.00248709418409185,0.0380039820902186));
#38561=CARTESIAN_POINT('',(-0.019,7.9723292034752E-17,0.0379414621394879));
#38562=CARTESIAN_POINT('',(0.019,5.51687858964173E-17,0.0394419409570244));
#38563=CARTESIAN_POINT('',(-0.019,0.,0.0409417911129512));
#38564=CARTESIAN_POINT('',(-0.019,0.00248709418409192,0.0408792973564542));
#38565=CARTESIAN_POINT('',(-0.0180107055600589,0.00746012312352678,0.0407543098434603));
#38566=CARTESIAN_POINT('',(-0.0137847972460807,0.0137848390811386,0.0405668285739695));
#38567=CARTESIAN_POINT('',(-0.00746027851088491,0.0180106936071852,0.0403793473044786));
#38568=CARTESIAN_POINT('',(-3.20732160903668E-17,0.0194946531964074,0.0401918660349878));
#38569=CARTESIAN_POINT('',(0.00746027851088485,0.0180106936071852,0.0400043847654969));
#38570=CARTESIAN_POINT('',(0.0137847972460806,0.0137848390811386,0.0398169034960061));
#38571=CARTESIAN_POINT('',(0.0180107055600588,0.00746012312352683,0.0396294222265152));
#38572=CARTESIAN_POINT('',(0.019,0.00248709418409198,0.0395044347135213));
#38573=CARTESIAN_POINT('',(0.019,6.13906938284383E-17,0.0394419409570244));
#38574=CARTESIAN_POINT('',(-0.019,4.74885777153119E-15,0.0409417911129512));
#38575=CARTESIAN_POINT('',(0.019,1.90546421099058E-14,0.0424415956712427));
#38576=CARTESIAN_POINT('',(0.0190000000000025,-0.00248709418407366,0.0423791038146472));
#38577=CARTESIAN_POINT('',(0.0180107055600657,-0.00746012312351111,0.0422541201014563));
#38578=CARTESIAN_POINT('',(0.0137847972460913,-0.0137848390811285,0.0420666445316698));
#38579=CARTESIAN_POINT('',(0.00746027851089627,-0.0180106936071808,0.0418791689618834));
#38580=CARTESIAN_POINT('',(9.73352383959826E-15,-0.0194946531964077,0.0416916933920969));
#38581=CARTESIAN_POINT('',(-0.00746027851087828,-0.0180106936071883,0.0415042178223105));
#38582=CARTESIAN_POINT('',(-0.0137847972460775,-0.0137848390811422,0.0413167422525241));
#38583=CARTESIAN_POINT('',(-0.0180107055600582,-0.00746012312352912,0.0411292666827376));
#38584=CARTESIAN_POINT('',(-0.019,-0.00248709418409264,0.0410042829695467));
#38585=CARTESIAN_POINT('',(-0.019,7.9723292034752E-17,0.0409417911129512));
#38586=CARTESIAN_POINT('',(0.019,1.90573078608331E-14,0.0424415956712427));
#38587=CARTESIAN_POINT('',(0.0132733600509949,0.0135947752080221,0.0428219504950535));
#38588=CARTESIAN_POINT('',(0.0150800156837313,0.0118308335220045,0.0427585580244184));
#38589=CARTESIAN_POINT('',(0.0179798105748163,0.00757378477671875,0.0426317730831481));
#38590=CARTESIAN_POINT('',(0.0189999999999975,0.00252497422701,0.0425049881418778));
#38591=CARTESIAN_POINT('',(0.019,1.90546421099058E-14,0.0424415956712427));
#38592=CARTESIAN_POINT('',(0.0135335405895343,0.0135722295367336,0.0430141822613637));
#38593=CARTESIAN_POINT('',(0.0135341500471712,0.0135716215917096,0.0430141616768234));
#38594=CARTESIAN_POINT('',(0.0135347594691913,0.0135710136063163,0.0430141410888615));
#38595=CARTESIAN_POINT('',(0.0135353688555734,0.0135704055805392,0.0430141204974931));
#38596=CARTESIAN_POINT('',(0.0135353510208537,0.0135703818080405,0.0430142946508867));
#38597=CARTESIAN_POINT('',(0.0135353688555734,0.0135704055805392,0.0430141204974931));
#38598=CARTESIAN_POINT('',(0.0161498178403471,0.0109578623504477,0.0429252407150377));
#38599=CARTESIAN_POINT('',(0.018896002464485,0.00590598767738096,0.0427847623969909));
#38600=CARTESIAN_POINT('',(0.0193098145538766,-0.000625315742798855,0.0426233441156423));
#38601=CARTESIAN_POINT('',(0.018756637468961,-0.00425420435492626,0.0425326941106314));
#38602=CARTESIAN_POINT('',(0.017939462958948,-0.00693277608908051,0.0424630453307758));
#38603=CARTESIAN_POINT('',(0.0167719383093269,-0.00941371737899657,0.0423943015591571));
#38604=CARTESIAN_POINT('',(0.0152275971629559,-0.011749218418051,0.0423251314671479));
#38605=CARTESIAN_POINT('',(0.0133927598958916,-0.0138018238182261,0.0422570767083249));
#38606=CARTESIAN_POINT('',(0.0112669003617152,-0.015588270498333,0.0421876505427081));
#38607=CARTESIAN_POINT('',(0.00890096294820859,-0.0170486177791914,0.0421184486185939));
#38608=CARTESIAN_POINT('',(0.0063781955005646,-0.0181446735945083,0.042050625438433));
#38609=CARTESIAN_POINT('',(0.00367453763971176,-0.018878268632462,0.041980836710611));
#38610=CARTESIAN_POINT('',(0.00095276270518741,-0.0192096809442985,0.0419121587103747));
#38611=CARTESIAN_POINT('',(-0.00184583529240445,-0.0191442027451065,0.04184309187272));
#38612=CARTESIAN_POINT('',(-0.00546575961568702,-0.0185311108673583,0.0417521611352773));
#38613=CARTESIAN_POINT('',(-0.00894299434047007,-0.0171264964984881,0.0416589517043263));
#38614=CARTESIAN_POINT('',(-0.011969492833948,-0.0150542322956112,0.0415685362868275));
#38615=CARTESIAN_POINT('',(-0.0140294246337335,-0.0131558205092909,0.0414986313581724));
#38616=CARTESIAN_POINT('',(-0.0157584853266227,-0.0110265159034489,0.0414300096906797));
#38617=CARTESIAN_POINT('',(-0.0176676247681137,-0.00782515303996317,0.041338199097655));
#38618=CARTESIAN_POINT('',(-0.0188342416993615,-0.00431655998882969,0.0412464695364074));
#38619=CARTESIAN_POINT('',(-0.0192225789677563,-0.000621704652356598,0.0411542685630935));
#38620=CARTESIAN_POINT('',(-0.0191151445766951,0.00212441003994294,0.0410864281170052));
#38621=CARTESIAN_POINT('',(-0.0186037925464179,0.00487875125399747,0.0410164256524546));
#38622=CARTESIAN_POINT('',(-0.0177208152379379,0.00747598493059139,0.0409479265235543));
#38623=CARTESIAN_POINT('',(-0.016448360009597,0.00996756637677533,0.0408790004502757));
#38624=CARTESIAN_POINT('',(-0.014324722750542,0.012965147511815,0.0407877055934287));
#38625=CARTESIAN_POINT('',(-0.011550414631196,0.015487795214077,0.0406948338092932));
#38626=CARTESIAN_POINT('',(-0.00837128058162158,0.0173152952700514,0.0406043068008098));
#38627=CARTESIAN_POINT('',(-0.0057673062400589,0.0183480298387254,0.040534205167538));
#38628=CARTESIAN_POINT('',(-0.00309772308846666,0.0189819792717225,0.0404658161268834));
#38629=CARTESIAN_POINT('',(0.000613590956548792,0.0193129287051469,0.0403740753133858));
#38630=CARTESIAN_POINT('',(0.00427983448328106,0.0188431233165396,0.0402820726208667));
#38631=CARTESIAN_POINT('',(0.00778010889064711,0.0175885872608356,0.0401901465007869));
#38632=CARTESIAN_POINT('',(0.0102063567334771,0.0163012867396412,0.0401221673372315));
#38633=CARTESIAN_POINT('',(0.0124675930149152,0.0146450218783127,0.0400519767699712));
#38634=CARTESIAN_POINT('',(0.0144237842802552,0.0127225832477427,0.0399837570344856));
#38635=CARTESIAN_POINT('',(0.0161159401675219,0.0104963981981657,0.0399148699216431));
#38636=CARTESIAN_POINT('',(0.0178968799936531,0.00728075889012127,0.0398232181034071));
#38637=CARTESIAN_POINT('',(0.0189651862938166,0.00368753414307424,0.0397307671157354));
#38638=CARTESIAN_POINT('',(0.0192327028976888,3.00353480110928E-5,0.0396399980054814));
#38639=CARTESIAN_POINT('',(0.0190337323354013,-0.00276394975683582,0.0395697780757167));
#38640=CARTESIAN_POINT('',(0.018446230547656,-0.00544438105205532,0.0395016869387841));
#38641=CARTESIAN_POINT('',(0.0171349139652453,-0.00893052771404328,0.0394098557370111));
#38642=CARTESIAN_POINT('',(0.0151220674546025,-0.0120297481353181,0.0393177805662593));
#38643=CARTESIAN_POINT('',(0.0124711767467395,-0.0146408504437676,0.0392260048260426));
#38644=CARTESIAN_POINT('',(0.0102598867147642,-0.0162675495412288,0.0391578555996006));
#38645=CARTESIAN_POINT('',(0.00778642693052377,-0.0175869696511293,0.0390875873063964));
#38646=CARTESIAN_POINT('',(0.00520447288027298,-0.0185150591603213,0.039019639281149));
#38647=CARTESIAN_POINT('',(0.00246754413694701,-0.0190742684960932,0.0389506880769338));
#38648=CARTESIAN_POINT('',(-0.000290406066513938,-0.0192298276349607,0.0388817156801483));
#38649=CARTESIAN_POINT('',(-0.00304518049289391,-0.0189913664368629,0.0388127338115798));
#38650=CARTESIAN_POINT('',(-0.00576121780142906,-0.0183489981346029,0.0387439292815532));
#38651=CARTESIAN_POINT('',(-0.00831583448795037,-0.0173420717943234,0.0386756497980644));
#38652=CARTESIAN_POINT('',(-0.0115547279583845,-0.0154885311234985,0.0385821304483689));
#38653=CARTESIAN_POINT('',(-0.0142851239316347,-0.0130133529355991,0.0384923772384108));
#38654=CARTESIAN_POINT('',(-0.0164584685016815,-0.00995259962459248,0.0383985070890661));
#38655=CARTESIAN_POINT('',(-0.0181280991357095,-0.00668324788376798,0.0383072159644954));
#38656=CARTESIAN_POINT('',(-0.0190770573354136,-0.00305385807602741,0.0382152822618342));
#38657=CARTESIAN_POINT('',(-0.0192239215401177,0.00060811378866868,0.0381233883639684));
#38658=CARTESIAN_POINT('',(-0.0189310231518623,0.00339509759960875,0.0380542489857858));
#38659=CARTESIAN_POINT('',(-0.0182542598980589,0.00605476811571894,0.0379863474074727));
#38660=CARTESIAN_POINT('',(-0.0168302625510012,0.00949424787791312,0.0378931324005353));
#38661=CARTESIAN_POINT('',(-0.0147127376841849,0.0125251302411581,0.0378027441799212));
#38662=CARTESIAN_POINT('',(-0.0119775777837324,0.0150476157199599,0.0377099881368222));
#38663=CARTESIAN_POINT('',(-0.00971403790835766,0.0166002034105028,0.0376412938168035));
#38664=CARTESIAN_POINT('',(-0.00719759777520637,0.0178354879993317,0.0375721916540058));
#38665=CARTESIAN_POINT('',(-0.0045852920319042,0.0186774722401391,0.0375041777335244));
#38666=CARTESIAN_POINT('',(-0.00183392773622591,0.0191462390263392,0.0374342939225838));
#38667=CARTESIAN_POINT('',(0.000930292961064554,0.0192097121327847,0.0373657490387983));
#38668=CARTESIAN_POINT('',(0.00367415075193295,0.0188787530141101,0.0372974987999961));
#38669=CARTESIAN_POINT('',(0.00636867754597101,0.0181475082599207,0.0372277545078323));
#38670=CARTESIAN_POINT('',(0.00888701139462942,0.0170572583903196,0.0371591969319872));
#38671=CARTESIAN_POINT('',(0.0112717973743793,0.0155837321927682,0.0370901295748675));
#38672=CARTESIAN_POINT('',(0.0133751805831766,0.0138197199427338,0.0370220059714728));
#38673=CARTESIAN_POINT('',(0.0158546750963597,0.0110463770905087,0.0369288203331229));
#38674=CARTESIAN_POINT('',(0.0176676936866646,0.00782393198606787,0.0368386594887747));
#38675=CARTESIAN_POINT('',(0.0187543862598064,0.00426286323505308,0.0367455323277807));
#38676=CARTESIAN_POINT('',(0.0191708150624781,0.00155072179234026,0.0366771182045157));
#38677=CARTESIAN_POINT('',(0.0191921575802405,-0.00125232563135686,0.0366080604046766));
#38678=CARTESIAN_POINT('',(0.0188173194808651,-0.00397257306730293,0.0365398125587642));
#38679=CARTESIAN_POINT('',(0.0180470622439191,-0.00665228714291196,0.0364699901440749));
#38680=CARTESIAN_POINT('',(0.0169033075242486,-0.00917314068262214,0.0364016127764803));
#38681=CARTESIAN_POINT('',(0.0154167509158799,-0.0114995951877568,0.0363332673933967));
#38682=CARTESIAN_POINT('',(0.0135873852996124,-0.0136118387317986,0.0362633074197483));
#38683=CARTESIAN_POINT('',(0.0115130064335834,-0.0154069235218565,0.0361950572005525));
#38684=CARTESIAN_POINT('',(0.00915099589266125,-0.0169163410861854,0.0361259786168976));
#38685=CARTESIAN_POINT('',(0.00664816293250691,-0.0180467741812788,0.0360576130065278));
#38686=CARTESIAN_POINT('',(0.00307582408105403,-0.0190768596647923,0.0359646146664873));
#38687=CARTESIAN_POINT('',(-0.000614380751948974,-0.0193129186119715,0.0358744750087052));
#38688=CARTESIAN_POINT('',(-0.0042960343038314,-0.018747026369487,0.0357810926952821));
#38689=CARTESIAN_POINT('',(-0.00691981570441502,-0.0179453056330825,0.0357129970754028));
#38690=CARTESIAN_POINT('',(-0.00945357573199342,-0.0167490017306704,0.0356439203566654));
#38691=CARTESIAN_POINT('',(-0.0125098522922861,-0.0147235243482249,0.0355523919411737));
#38692=CARTESIAN_POINT('',(-0.0151185474142208,-0.0120303297988389,0.0354600967454023));
#38693=CARTESIAN_POINT('',(-0.0170481137245165,-0.00890303733159082,0.0353690195303689));
#38694=CARTESIAN_POINT('',(-0.0181594653228968,-0.0063361992120837,0.0352988708491257));
#38695=CARTESIAN_POINT('',(-0.018875971452887,-0.00368907908914855,0.0352309647005051));
#38696=CARTESIAN_POINT('',(-0.019211490669188,-0.000906538208031904,0.0351617804587047));
#38697=CARTESIAN_POINT('',(-0.0191443011592234,0.00184013369332341,0.035093185607839));
#38698=CARTESIAN_POINT('',(-0.018522526050253,0.00550381644714024,0.0350005226370239));
#38699=CARTESIAN_POINT('',(-0.0171351337536918,0.00893101889174432,0.0349102021080862));
#38700=CARTESIAN_POINT('',(-0.0150269900835202,0.0120043229327353,0.0348166884810567));
#38701=CARTESIAN_POINT('',(-0.0131662745690762,0.0140198448206814,0.0347489116431167));
#38702=CARTESIAN_POINT('',(-0.0109900340176108,0.0157836795334412,0.0346796934145625));
#38703=CARTESIAN_POINT('',(-0.00783682721710034,0.0176592587274472,0.0345878893869752));
#38704=CARTESIAN_POINT('',(-0.00162495554055579,0.0197288917722028,0.0344274670366339));
#38705=CARTESIAN_POINT('',(0.00407409956719794,0.0190912786150354,0.0342894074497274));
#38706=CARTESIAN_POINT('',(0.00748331487893838,0.0176454543212183,0.0341971457690361));
#38707=CARTESIAN_POINT('',(0.0135247164963182,0.0135491354261317,0.0340048173228733));
#38708=CARTESIAN_POINT('',(0.0134522998980134,0.0134185657624297,0.0340037511130871));
#38709=CARTESIAN_POINT('',(0.0135568792897986,0.013312063097876,0.034));
#38710=CARTESIAN_POINT('',(0.0135234994968269,0.0135502855516948,0.0339374949028807));
#38711=CARTESIAN_POINT('',(0.0134507948637152,0.0134196591751994,0.0339250904797292));
#38712=CARTESIAN_POINT('',(0.0135557820741085,0.0133131804919685,0.033921285990061));
#38713=CARTESIAN_POINT('',(0.0135278548856968,0.0135569617878143,0.0338714576447267));
#38714=CARTESIAN_POINT('',(0.0134558017982309,0.0134272067953835,0.0338479166793451));
#38715=CARTESIAN_POINT('',(0.0135612061032408,0.0133207522704363,0.0338440728084942));
#38716=CARTESIAN_POINT('',(0.0135375715470061,0.013568951169631,0.0338067616450345));
#38717=CARTESIAN_POINT('',(0.0134670675691026,0.01344095421085,0.0337722952163498));
#38718=CARTESIAN_POINT('',(0.0135729078908396,0.0133345360558799,0.0337684261530207));
#38719=CARTESIAN_POINT('',(0.0135726991431301,0.0133342900396015,0.0337697801684402));
#38720=CARTESIAN_POINT('',(0.0135610979456742,0.0133206611476437,0.0338451346978836));
#38721=CARTESIAN_POINT('',(0.0135557655877528,0.0133131972815174,0.0339225654745483));
#38722=CARTESIAN_POINT('',(0.0135568792897986,0.013312063097876,0.034));
#38723=CARTESIAN_POINT('',(0.0135726991431301,0.0133342900396015,0.0337697801684401));
#38724=CARTESIAN_POINT('',(0.0135726991346738,0.0133342900312937,0.0337697801656355));
#38725=CARTESIAN_POINT('',(0.0135608689083288,0.0133411879010404,0.0337850169067288));
#38726=CARTESIAN_POINT('',(0.0135261534936828,0.0133696145659868,0.0338380484731189));
#38727=CARTESIAN_POINT('',(0.013493225546999,0.0134285620019686,0.0339197948589413));
#38728=CARTESIAN_POINT('',(0.0135054310078758,0.0135145300695567,0.0339890626438917));
#38729=CARTESIAN_POINT('',(0.0135239956136941,0.0135478241103007,0.0340048065022042));
#38730=CARTESIAN_POINT('',(0.00741375790559351,0.0174938901824966,0.0340000000000028));
#38731=CARTESIAN_POINT('',(0.0074176279605962,0.0174922500869796,0.0341689995579579));
#38732=CARTESIAN_POINT('',(0.00748331487893827,0.0176454543212184,0.0341971457690361));
#38733=CARTESIAN_POINT('',(0.00799464401290268,0.0172477157224201,0.0339801794998395));
#38734=CARTESIAN_POINT('',(0.00800212560069349,0.0172407233498891,0.0341524362276056));
#38735=CARTESIAN_POINT('',(0.00806923059913374,0.0173969713509321,0.0341812894236565));
#38736=CARTESIAN_POINT('',(0.00856561383670638,0.0169720369215461,0.0339604377545791));
#38737=CARTESIAN_POINT('',(0.00857099591731754,0.0169613822002568,0.0341359610403092));
#38738=CARTESIAN_POINT('',(0.0086450247826401,0.0171185073952909,0.0341654757873373));
#38739=CARTESIAN_POINT('',(0.00967269163952337,0.0163690746593947,0.0339214044506673));
#38740=CARTESIAN_POINT('',(0.00967397428338661,0.0163519147228243,0.0341031417042596));
#38741=CARTESIAN_POINT('',(0.00976117260934767,0.0165091869101672,0.0341341741865354));
#38742=CARTESIAN_POINT('',(0.0102074312117974,0.0160428532240274,0.0339021292666557));
#38743=CARTESIAN_POINT('',(0.0102059284872208,0.016022110139271,0.034086845502193));
#38744=CARTESIAN_POINT('',(0.0103001539749249,0.0161794310522496,0.0341187042517711));
#38745=CARTESIAN_POINT('',(0.0112404839068122,0.0153423684648806,0.0338637517753579));
#38746=CARTESIAN_POINT('',(0.0112332853866827,0.0153154078586966,0.0340542850074699));
#38747=CARTESIAN_POINT('',(0.011341079607521,0.0154713323131514,0.0340878936508673));
#38748=CARTESIAN_POINT('',(0.0117387955300322,0.0149681033735197,0.0338446492933245));
#38749=CARTESIAN_POINT('',(0.0117280389869818,0.0149376995987162,0.034038022302507));
#38750=CARTESIAN_POINT('',(0.0118430241296028,0.0150929851913844,0.0340725528860564));
#38751=CARTESIAN_POINT('',(0.0126990967570012,0.014171558726067,0.033806541009908));
#38752=CARTESIAN_POINT('',(0.0126809315014158,0.0141354605322774,0.0340053832026719));
#38753=CARTESIAN_POINT('',(0.012809866962313,0.0142877563781691,0.0340419258464437));
#38754=CARTESIAN_POINT('',(0.0131608718072554,0.0137489868194859,0.0337890310203656));
#38755=CARTESIAN_POINT('',(0.0131389206922079,0.0137100385174954,0.0339891335836076));
#38756=CARTESIAN_POINT('',(0.0132735769552999,0.0138601685116395,0.0340276462825612));
#38757=CARTESIAN_POINT('',(0.0136044777921139,0.0133023653697072,0.0337683091703764));
#38758=CARTESIAN_POINT('',(0.0135736223072447,0.0132643239162051,0.0339726046099247));
#38759=CARTESIAN_POINT('',(0.0137210863278384,0.0134089001480767,0.0340111781184431));
#38760=CARTESIAN_POINT('',(0.00741375790559351,0.0174938901824966,0.034));
#38761=CARTESIAN_POINT('',(0.00970786016513252,0.0165216696766245,0.0339225654745483));
#38762=CARTESIAN_POINT('',(0.0118113590310252,0.0151016843440063,0.0338451346978836));
#38763=CARTESIAN_POINT('',(0.0135726991431301,0.0133342900396015,0.0337697801684402));
#38764=CARTESIAN_POINT('',(0.00748331487893827,0.0176454543212184,0.0341971457690361));
#38765=CARTESIAN_POINT('',(0.00861748461183809,0.0171644604609653,0.034166452298313));
#38766=CARTESIAN_POINT('',(0.0107946770544553,0.0159827433342134,0.0341051551118467));
#38767=CARTESIAN_POINT('',(0.0126732556571759,0.0144434668614907,0.0340483193425882));
#38768=CARTESIAN_POINT('',(0.0135476845953551,0.013581764079206,0.0340174277337795));
#38769=CARTESIAN_POINT('',(0.0134350288425444,0.0134350288425444,0.044));
#38770=CARTESIAN_POINT('',(0.0134350288425444,0.0134350288425444,0.044));
#38771=CARTESIAN_POINT('',(0.0134350288425449,0.0134350288425438,0.035));
#38772=CARTESIAN_POINT('',(0.0134350288425449,0.0134350288425438,0.035));
#38773=CARTESIAN_POINT('',(-0.04,0.,-0.04));
#38774=CARTESIAN_POINT('',(0.,0.,-0.04));
#38775=CARTESIAN_POINT('',(-0.04,0.,-0.04));
#38776=CARTESIAN_POINT('',(0.,0.,0.046));
#38777=CARTESIAN_POINT('',(0.,0.,0.046));
#38778=CARTESIAN_POINT('',(0.0188,0.,0.046));
#38779=CARTESIAN_POINT('',(0.,0.,0.046));
#38780=CARTESIAN_POINT('',(0.0123,0.,0.046));
#38781=CARTESIAN_POINT('',(1.08184846837294E-17,0.,0.03));
#38782=CARTESIAN_POINT('',(-0.0175,0.0303108891324553,0.03));
#38783=CARTESIAN_POINT('',(-0.0183131446174913,0.0432854332797865,0.03));
#38784=CARTESIAN_POINT('',(-0.0283297125253659,0.0375023651018189,0.03));
#38785=CARTESIAN_POINT('',(0.,0.,0.03));
#38786=CARTESIAN_POINT('',(0.,0.,0.03));
#38787=CARTESIAN_POINT('',(-0.019,0.,0.03));
#38788=CARTESIAN_POINT('',(1.0775734895605E-17,0.,0.033));
#38789=CARTESIAN_POINT('',(0.,0.,0.033));
#38790=CARTESIAN_POINT('',(-0.0259053349880927,0.0357284848849959,0.033));
#38791=CARTESIAN_POINT('',(-0.0179891080550886,0.0402989206357321,0.033));
#38792=CARTESIAN_POINT('',(-0.0175,0.0303108891324553,0.033));
#38793=CARTESIAN_POINT('',(0.,0.,0.033));
#38794=CARTESIAN_POINT('',(0.02,0.,0.033));
#38795=CARTESIAN_POINT('',(0.,0.,0.0396457076047696));
#38796=CARTESIAN_POINT('',(0.,0.,0.0396457076047696));
#38797=CARTESIAN_POINT('',(0.05,0.,0.0396457076047696));
#38798=CARTESIAN_POINT('',(-0.0179891080550886,0.0402989206357321,0.033));
#38799=CARTESIAN_POINT('',(-0.0187458295220114,0.0402618644285296,0.03331100188783));
#38800=CARTESIAN_POINT('',(-0.0202815477394373,0.0400153314880262,0.0338032106110653));
#38801=CARTESIAN_POINT('',(-0.0225425615656762,0.0390633626363814,0.0340721518705467));
#38802=CARTESIAN_POINT('',(-0.0245020780652921,0.0375846816769992,0.0338078665554804));
#38803=CARTESIAN_POINT('',(-0.0254946132923719,0.0363657146815882,0.0333112059722862));
#38804=CARTESIAN_POINT('',(-0.0259053349880927,0.0357284848849959,0.033));
#38805=CARTESIAN_POINT('',(-0.0175,0.0303108891324553,0.107));
#38806=CARTESIAN_POINT('',(0.,0.,0.046));
#38807=CARTESIAN_POINT('',(0.,0.,0.034));
#38808=CARTESIAN_POINT('',(0.,0.,0.0458));
#38809=CARTESIAN_POINT('',(0.019,0.,0.0458));
#38810=CARTESIAN_POINT('',(0.,0.,0.));
#38811=CARTESIAN_POINT('',(0.,0.,0.0442));
#38812=CARTESIAN_POINT('',(-0.0121,0.,0.0442));
#38813=CARTESIAN_POINT('',(0.,0.,0.0458));
#38814=CARTESIAN_POINT('',(0.0121,0.,0.0458));
#38815=CARTESIAN_POINT('',(0.,0.,0.046));
#38816=CARTESIAN_POINT('',(0.,0.,0.033));
#38817=CARTESIAN_POINT('',(-0.016,0.,0.033));
#38818=CARTESIAN_POINT('',(0.,0.,0.0400107279868694));
#38819=CARTESIAN_POINT('',(-0.016,0.,0.0400107279868694));
#38820=CARTESIAN_POINT('',(0.,0.,0.));
#38821=CARTESIAN_POINT('',(0.,0.,-0.03));
#38822=CARTESIAN_POINT('',(-0.05,0.,-0.03));
#38823=CARTESIAN_POINT('',(0.,0.,0.027));
#38824=CARTESIAN_POINT('',(-0.05,0.,0.027));
#38825=CARTESIAN_POINT('',(0.,0.,-0.03));
#38826=CARTESIAN_POINT('',(0.0119917500543135,0.0150793149034488,0.0430647002772689));
#38827=CARTESIAN_POINT('',(0.0125011351272437,0.0145712292566673,0.0430467550241789));
#38828=CARTESIAN_POINT('',(0.013010520200174,0.0140631436098858,0.043028809771089));
#38829=CARTESIAN_POINT('',(0.0135199052731042,0.0135550579631043,0.0430108645179991));
#38830=CARTESIAN_POINT('',(0.0150074761996503,0.0120712817856836,0.042958458512828));
#38831=CARTESIAN_POINT('',(0.0162575507862789,0.01032732078082,0.0429056768871633));
#38832=CARTESIAN_POINT('',(0.0185852198899116,0.00558586532020392,0.0427738987465939));
#38833=CARTESIAN_POINT('',(0.0192552744826652,0.00239702668057813,0.0426950802007972));
#38834=CARTESIAN_POINT('',(0.0190021699218141,-0.0039291638470396,0.0425371897621086));
#38835=CARTESIAN_POINT('',(0.0180761838518777,-0.00705722965242059,0.0424582447351112));
#38836=CARTESIAN_POINT('',(0.0148422268308121,-0.0125000201568053,0.0423003225632235));
#38837=CARTESIAN_POINT('',(0.0125382516416315,-0.0148092920302629,0.042221379417481));
#38838=CARTESIAN_POINT('',(0.00710378716781687,-0.0180571812145946,0.0420635018522572));
#38839=CARTESIAN_POINT('',(0.0039786824719132,-0.0189926412444474,0.0419845627080643));
#38840=CARTESIAN_POINT('',(-0.00234668519603218,-0.0192623405937001,0.0418266349581681));
#38841=CARTESIAN_POINT('',(-0.00554006854269375,-0.0185965109372015,0.0417476957409817));
#38842=CARTESIAN_POINT('',(-0.011231462134108,-0.0158233918460566,0.041589817663171));
#38843=CARTESIAN_POINT('',(-0.0137238699102723,-0.0137188110133377,0.0415108784584664));
#38844=CARTESIAN_POINT('',(-0.0174093010078421,-0.00857093437562775,0.0413529508414693));
#38845=CARTESIAN_POINT('',(-0.0185985058296419,-0.00553336791248007,0.0412740115167333));
#38846=CARTESIAN_POINT('',(-0.0193898407789082,0.000748028528479798,0.0411161334534399));
#38847=CARTESIAN_POINT('',(-0.0189911740659409,0.00398568545192271,0.0410371942485536));
#38848=CARTESIAN_POINT('',(-0.0166972840647074,0.00988662641355999,0.0408792666290302));
#38849=CARTESIAN_POINT('',(-0.0148047686356766,0.0125435802427221,0.040800327306438));
#38850=CARTESIAN_POINT('',(-0.00997901329099115,0.0166416575456676,0.0406424492429172));
#38851=CARTESIAN_POINT('',(-0.00705050542285551,0.0180787376270981,0.0405635100380233));
#38852=CARTESIAN_POINT('',(-0.000855796548201768,0.019385878604594,0.0404055824185264));
#38853=CARTESIAN_POINT('',(0.0024036239598539,0.0192547441300795,0.040326643095907));
#38854=CARTESIAN_POINT('',(0.00847383490058702,0.0174562193561262,0.0401687650323922));
#38855=CARTESIAN_POINT('',(0.0112786521558426,0.015790579041134,0.0400898258274887));
#38856=CARTESIAN_POINT('',(0.0157611313736707,0.0113195147787425,0.0399318982080082));
#38857=CARTESIAN_POINT('',(0.0174340840310036,0.0085191134315629,0.039852958885376));
#38858=CARTESIAN_POINT('',(0.0192485100731383,0.00245363650347758,0.0396950808218705));
#38859=CARTESIAN_POINT('',(0.0193881814683697,-0.000805481382629234,0.0396161416169616));
#38860=CARTESIAN_POINT('',(0.0180968400976795,-0.00700350308644694,0.0394582139974826));
#38861=CARTESIAN_POINT('',(0.0166674563386305,-0.00993571732966755,0.0393792746748263));
#38862=CARTESIAN_POINT('',(0.0125820393617557,-0.0147721954235223,0.0392213966113676));
#38863=CARTESIAN_POINT('',(0.009930008131089,-0.0166716921584716,0.0391424574064428));
#38864=CARTESIAN_POINT('',(0.00403493534485767,-0.0189806210057407,0.0389845297869488));
#38865=CARTESIAN_POINT('',(0.000798385059068726,-0.0193877580180761,0.0389055904643503));
#38866=CARTESIAN_POINT('',(-0.00548506356453857,-0.0186128866597783,0.038747712400791));
#38867=CARTESIAN_POINT('',(-0.00852578215354342,-0.0174316212550832,0.0386687731959199));
#38868=CARTESIAN_POINT('',(-0.0136830391876003,-0.01375932831178,0.0385108455764191));
#38869=CARTESIAN_POINT('',(-0.0157941058636261,-0.0112724797461941,0.0384319062538021));
#38870=CARTESIAN_POINT('',(-0.0185821301893177,-0.00558837272865016,0.0382740281902866));
#38871=CARTESIAN_POINT('',(-0.0192563298219162,-0.00239669411864687,0.0381950889853776));
#38872=CARTESIAN_POINT('',(-0.0190027615072474,0.003929342451488,0.0380371613659087));
#38873=CARTESIAN_POINT('',(-0.0180754992816383,0.00705683394845448,0.0379582220432658));
#38874=CARTESIAN_POINT('',(-0.0148418601975698,0.0124997863184206,0.0378003439797702));
#38875=CARTESIAN_POINT('',(-0.0125386461030731,0.0148098863875077,0.0377214047748604));
#38876=CARTESIAN_POINT('',(-0.00710401162363045,0.0180576215447498,0.0375634771553734));
#38877=CARTESIAN_POINT('',(-0.00397861621492044,0.0189919244067349,0.0374845378327532));
#38878=CARTESIAN_POINT('',(0.00234667399305028,0.0192618429362422,0.0373266597692301));
#38879=CARTESIAN_POINT('',(0.00554035103904963,0.0185971742818825,0.0372477205643357));
#38880=CARTESIAN_POINT('',(0.0112317093616142,0.0158238232365207,0.0370897929448454));
#38881=CARTESIAN_POINT('',(0.0137233056605262,0.0137183621985592,0.0370108536222324));
#38882=CARTESIAN_POINT('',(0.0174088782338546,0.00857067271353671,0.0368529755586984));
#38883=CARTESIAN_POINT('',(0.0185992156954128,0.00553349405207063,0.0367740363538192));
#38884=CARTESIAN_POINT('',(0.0193903371194134,-0.000747999597473434,0.0366161087343093));
#38885=CARTESIAN_POINT('',(0.0189904897234335,-0.00398545853288628,0.0365371694116723));
#38886=CARTESIAN_POINT('',(0.016696833777141,-0.00988641562708066,0.0363792913482067));
#38887=CARTESIAN_POINT('',(0.0148052624952997,-0.0125441055225229,0.0363003521432767));
#38888=CARTESIAN_POINT('',(0.00997930898393624,-0.0166420572405772,0.0361424245237952));
#38889=CARTESIAN_POINT('',(0.00705032109213422,-0.018078040606426,0.0360634852011783));
#38890=CARTESIAN_POINT('',(0.000855726728281628,-0.0193853863493642,0.0359056071375901));
#38891=CARTESIAN_POINT('',(-0.00240379359650828,-0.0192554448703678,0.0358266679332148));
#38892=CARTESIAN_POINT('',(-0.00847400777758182,-0.0174566855184124,0.0356687403131495));
#38893=CARTESIAN_POINT('',(-0.0112781694595669,-0.015790043478278,0.0355898009903084));
#38894=CARTESIAN_POINT('',(-0.0157607575092302,-0.01131918706518,0.0354319229308719));
#38895=CARTESIAN_POINT('',(-0.0174347630819637,-0.00851935491177149,0.035352983696314));
#38896=CARTESIAN_POINT('',(-0.0192489951359535,-0.00245374648858159,0.0351950561117514));
#38897=CARTESIAN_POINT('',(-0.019387468746271,0.000805369882804851,0.0351161167829709));
#38898=CARTESIAN_POINT('',(-0.018096358790058,0.00700336721469534,0.0349582385556631));
#38899=CARTESIAN_POINT('',(-0.0166680470003033,0.00993616961891969,0.0348793005385675));
#38900=CARTESIAN_POINT('',(-0.0125823814601453,0.0147725289177495,0.0347213713419553));
#38901=CARTESIAN_POINT('',(-0.00992974481013676,0.0166710547380506,0.034642433347362));
#38902=CARTESIAN_POINT('',(-0.00403488070884202,0.0189802566810074,0.0344845596813018));
#38903=CARTESIAN_POINT('',(-0.000797607311307338,0.0193877129329866,0.0344055828137047));
#38904=CARTESIAN_POINT('',(0.00443737678994076,0.0187430425425944,0.0342740271499158));
#38905=CARTESIAN_POINT('',(0.00648716110805819,0.018136769321841,0.0342214697017214));
#38906=CARTESIAN_POINT('',(0.0102850157450545,0.0162842186741472,0.034116047314547));
#38907=CARTESIAN_POINT('',(0.0120323096863351,0.0150388096576012,0.0340632655330976));
#38908=CARTESIAN_POINT('',(0.0135198806212156,0.0135550334919025,0.0340108594337564));
#38909=CARTESIAN_POINT('',(0.0140292460652998,0.0130469674307547,0.0339929148400313));
#38910=CARTESIAN_POINT('',(0.0145386115093839,0.0125389013696069,0.0339749702463062));
#38911=CARTESIAN_POINT('',(0.0150479769534681,0.0120308353084591,0.0339570256525811));
#38912=CARTESIAN_POINT('',(0.0123579083616226,0.0155369748779275,0.0431499982326393));
#38913=CARTESIAN_POINT('',(0.0128829926152429,0.0150130780695355,0.0431320339636127));
#38914=CARTESIAN_POINT('',(0.0134080768688632,0.0144891812611435,0.0431140696945862));
#38915=CARTESIAN_POINT('',(0.0139331611224835,0.0139652844527515,0.0430961054255596));
#38916=CARTESIAN_POINT('',(0.0154665787885716,0.0124353345148957,0.0430436438876373));
#38917=CARTESIAN_POINT('',(0.0167531705810892,0.0106397945897671,0.0429909630839482));
#38918=CARTESIAN_POINT('',(0.0191517105955881,0.00575220601775009,0.0428590290562634));
#38919=CARTESIAN_POINT('',(0.0198412884492578,0.00246649476446469,0.0427802902482966));
#38920=CARTESIAN_POINT('',(0.0195795672614152,-0.00405098811972438,0.0426224546125279));
#38921=CARTESIAN_POINT('',(0.0186253272917594,-0.00727387508204592,0.0425435404344177));
#38922=CARTESIAN_POINT('',(0.0152913159926029,-0.012883209458447,0.042385492980283));
#38923=CARTESIAN_POINT('',(0.0129169889019614,-0.0152618586794028,0.0423065754957256));
#38924=CARTESIAN_POINT('',(0.00731750168182736,-0.0186072475248359,0.0421487662461117));
#38925=CARTESIAN_POINT('',(0.00409770260301624,-0.0195708558383439,0.0420698594839678));
#38926=CARTESIAN_POINT('',(-0.00242185886210048,-0.0198478911012018,0.0419117993361283));
#38927=CARTESIAN_POINT('',(-0.00571179382904948,-0.0191611066251957,0.0418328929598499));
#38928=CARTESIAN_POINT('',(-0.0115750659571972,-0.0163031656068709,0.0416750818535991));
#38929=CARTESIAN_POINT('',(-0.0141428342863435,-0.0141347036578673,0.041596175228296));
#38930=CARTESIAN_POINT('',(-0.0179406202137328,-0.00882826737024687,0.0414381154495285));
#38931=CARTESIAN_POINT('',(-0.019165091247219,-0.00569840984033663,0.0413592086996603));
#38932=CARTESIAN_POINT('',(-0.0199794247667977,0.000773270772147167,0.0412013976528512));
#38933=CARTESIAN_POINT('',(-0.0195684972398856,0.00410895666889318,0.0411224910179569));
#38934=CARTESIAN_POINT('',(-0.0172033186830933,0.0101906812348328,0.040964431232204));
#38935=CARTESIAN_POINT('',(-0.0152528290560035,0.0129276371826344,0.0408855244900124));
#38936=CARTESIAN_POINT('',(-0.0102803532064448,0.0171490436955882,0.0407277134421433));
#38937=CARTESIAN_POINT('',(-0.00726307273913791,0.018629476200455,0.0406488068074326));
#38938=CARTESIAN_POINT('',(-0.000878026746687795,0.019975816048429,0.0404907470217698));
#38939=CARTESIAN_POINT('',(0.00248007773407933,0.0198399045301169,0.0404118402794289));
#38940=CARTESIAN_POINT('',(0.00873378426508795,0.0179860049520613,0.0402540292316663));
#38941=CARTESIAN_POINT('',(0.0116234487256334,0.016269758721003,0.0401751225968814));
#38942=CARTESIAN_POINT('',(0.016242848459799,0.0116607903540324,0.0400170628112677));
#38943=CARTESIAN_POINT('',(0.0179657769533042,0.00877516129764991,0.039938156068967));
#38944=CARTESIAN_POINT('',(0.019834207640852,0.00252578086536967,0.0397803450210755));
#38945=CARTESIAN_POINT('',(0.0199779204821912,-0.000832047069362478,0.0397014383863677));
#38946=CARTESIAN_POINT('',(0.0186460188421592,-0.00722012043564429,0.0395433786007287));
#38947=CARTESIAN_POINT('',(0.0171726194934967,-0.0102407879122063,0.039464471858345));
#38948=CARTESIAN_POINT('',(0.0129627824089968,-0.0152230625677496,0.0393066608106448));
#38949=CARTESIAN_POINT('',(0.0102303248960628,-0.0171799319451898,0.0392277541758899));
#38950=CARTESIAN_POINT('',(0.00415396286427654,-0.019558853501359,0.0390696943901538));
#38951=CARTESIAN_POINT('',(0.00081928825096348,-0.0199775214705671,0.0389907876480876));
#38952=CARTESIAN_POINT('',(-0.00565426771542406,-0.0191782329298862,0.0388329765998498));
#38953=CARTESIAN_POINT('',(-0.00878700576444731,-0.0179610171988101,0.0387540699653644));
#38954=CARTESIAN_POINT('',(-0.0141020141670623,-0.0141752373594727,0.0385960101796268));
#38955=CARTESIAN_POINT('',(-0.0162764030938681,-0.0116125492318197,0.0385171034373905));
#38956=CARTESIAN_POINT('',(-0.0191479650339184,-0.00575593578666817,0.0383592923894944));
#38957=CARTESIAN_POINT('',(-0.0198423981325784,-0.00246755860460705,0.0382803857547962));
#38958=CARTESIAN_POINT('',(-0.019580104213294,0.00405261357194303,0.0381223259691423));
#38959=CARTESIAN_POINT('',(-0.0186239856370404,0.00727459664337587,0.0380434192268031));
#38960=CARTESIAN_POINT('',(-0.0152916206987856,0.0128818359766005,0.0378856081790289));
#38961=CARTESIAN_POINT('',(-0.0129185204582689,0.0152617639310929,0.0378067015442879));
#38962=CARTESIAN_POINT('',(-0.00731658970352529,0.0186083764170049,0.0376486417585979));
#38963=CARTESIAN_POINT('',(-0.00409630618835518,0.0195702037021567,0.0375697350162963));
#38964=CARTESIAN_POINT('',(0.00242051748217053,0.0198473287079597,0.037411923968483));
#38965=CARTESIAN_POINT('',(0.00571087619192717,0.0191623459481707,0.0373330173337259));
#38966=CARTESIAN_POINT('',(0.0115765136891496,0.0163030208419731,0.0371749575481073));
#38967=CARTESIAN_POINT('',(0.0141430513875155,0.0141331770946469,0.0370960508058741));
#38968=CARTESIAN_POINT('',(0.0179394158558112,0.00882908378426575,0.0369382397578527));
#38969=CARTESIAN_POINT('',(0.0191656268871714,0.00569985571227749,0.0368593331232383));
#38970=CARTESIAN_POINT('',(0.0199800953830214,-0.000774561974363728,0.0367012733375423));
#38971=CARTESIAN_POINT('',(0.0195673380013996,-0.0041099733415498,0.0366223665951662));
#38972=CARTESIAN_POINT('',(0.0172033434382891,-0.0101892264804572,0.0364645555475094));
#38973=CARTESIAN_POINT('',(0.0152543324585768,-0.0129272947815325,0.0363856489127126));
#38974=CARTESIAN_POINT('',(0.0102796390483894,-0.0171503113323094,0.0362275891269953));
#38975=CARTESIAN_POINT('',(0.00726158757166494,-0.0186290617929636,0.0361486823847811));
#38976=CARTESIAN_POINT('',(0.000879258158690037,-0.0199750410971762,0.035990871336678));
#38977=CARTESIAN_POINT('',(-0.00247896880992777,-0.0198409758490944,0.0359119647037807));
#38978=CARTESIAN_POINT('',(-0.00873523608853893,-0.0179861004206441,0.0357539049165843));
#38979=CARTESIAN_POINT('',(-0.0116239141146855,-0.0162682887157641,0.035674998171292));
#38980=CARTESIAN_POINT('',(-0.0162415262239483,-0.0116613973674352,0.0355171871399266));
#38981=CARTESIAN_POINT('',(-0.0179660669468812,-0.0087766758040901,0.0354382803995636));
#38982=CARTESIAN_POINT('',(-0.019835081866255,-0.00252461750601295,0.0352802207143626));
#38983=CARTESIAN_POINT('',(-0.0199769439065618,0.000833241001588936,0.0352013140439823));
#38984=CARTESIAN_POINT('',(-0.0186458014531443,0.00721867902972497,0.0350435023781893));
#38985=CARTESIAN_POINT('',(-0.0171740650283368,0.0102402163951023,0.0349645994515329));
#38986=CARTESIAN_POINT('',(-0.0129622644515052,0.015224425520243,0.0348065356824445));
#38987=CARTESIAN_POINT('',(-0.0102288601536968,0.0171797724257991,0.0347276300560009));
#38988=CARTESIAN_POINT('',(-0.00415512526945464,0.0195580042445408,0.0345698307327648));
#38989=CARTESIAN_POINT('',(-0.000819776313066147,0.0199776088263763,0.0344908525598553));
#38990=CARTESIAN_POINT('',(0.00457554999791865,0.0193123964644629,0.0343592181992749));
#38991=CARTESIAN_POINT('',(0.00668677785486926,0.0186876138390362,0.0343067695837959));
#38992=CARTESIAN_POINT('',(0.0106011348363567,0.0167775405869371,0.0342012224760503));
#38993=CARTESIAN_POINT('',(0.0123997205100048,0.0154952123480511,0.0341485415302033));
#38994=CARTESIAN_POINT('',(0.0139331382238583,0.0139652624610575,0.0340960799060637));
#38995=CARTESIAN_POINT('',(0.0144582022570879,0.0134413858610635,0.034078116299858));
#38996=CARTESIAN_POINT('',(0.0149832662903176,0.0129175092610696,0.0340601526936523));
#38997=CARTESIAN_POINT('',(0.0155083303235472,0.0123936326610756,0.0340421890874466));
#38998=CARTESIAN_POINT('',(0.0125376913185148,0.0157448176443322,0.0436067635510525));
#38999=CARTESIAN_POINT('',(0.013069857522132,0.01521323886892,0.0435887903654682));
#39000=CARTESIAN_POINT('',(0.0136020237257492,0.0146816600935077,0.0435708171798839));
#39001=CARTESIAN_POINT('',(0.0141341899293665,0.0141500813180954,0.0435528439942997));
#39002=CARTESIAN_POINT('',(0.015688289204474,0.0125976975253717,0.0435003564171141));
#39003=CARTESIAN_POINT('',(0.0169910078588997,0.0107772885016299,0.0434477228199255));
#39004=CARTESIAN_POINT('',(0.0194202296550407,0.00581999520554101,0.0433157157855861));
#39005=CARTESIAN_POINT('',(0.0201171636591806,0.00248850671300494,0.0432370143799227));
#39006=CARTESIAN_POINT('',(0.0198479246134623,-0.00411846085620159,0.0430792043811867));
#39007=CARTESIAN_POINT('',(0.0188787232202822,-0.00738525137746305,0.0430003046693479));
#39008=CARTESIAN_POINT('',(0.0154949070329289,-0.0130708753781158,0.0428421985013649));
#39009=CARTESIAN_POINT('',(0.0130863407397065,-0.015480768630216,0.0427632930662205));
#39010=CARTESIAN_POINT('',(0.00740774361997622,-0.0188688364441183,0.0426055158280661));
#39011=CARTESIAN_POINT('',(0.00414307297942253,-0.0198439056459545,0.0425266242112103));
#39012=CARTESIAN_POINT('',(-0.00246761697490749,-0.0201209799677763,0.0423685020300179));
#39013=CARTESIAN_POINT('',(-0.00580243147975463,-0.0194226134955046,0.0422896110657924));
#39014=CARTESIAN_POINT('',(-0.0117447007023978,-0.016521789522652,0.042131831338449));
#39015=CARTESIAN_POINT('',(-0.014346607338881,-0.0143220301077307,0.0420529399532225));
#39016=CARTESIAN_POINT('',(-0.0181942681687709,-0.00893932562358545,0.0418948182511038));
#39017=CARTESIAN_POINT('',(-0.0194335901567592,-0.00576556174660454,0.0418159267887342));
#39018=CARTESIAN_POINT('',(-0.0202552307852466,0.00079570735416269,0.0416581471419614));
#39019=CARTESIAN_POINT('',(-0.0198367739599844,0.0041770907819769,0.0415792557426705));
#39020=CARTESIAN_POINT('',(-0.0174350252151398,0.0103422836945221,0.0414211340314944));
#39021=CARTESIAN_POINT('',(-0.0154559013647298,0.0131156868572235,0.04134224257939));
#39022=CARTESIAN_POINT('',(-0.0104124216457013,0.0173922108962518,0.0411844629311661));
#39023=CARTESIAN_POINT('',(-0.00735276660167522,0.0188913343050469,0.0411055715321491));
#39024=CARTESIAN_POINT('',(-0.000877841710304256,0.0202527116759036,0.0409474498210928));
#39025=CARTESIAN_POINT('',(0.00252643659268623,0.0201127632828363,0.0408685583687824));
#39026=CARTESIAN_POINT('',(0.0088651211044794,0.0182295680747286,0.0407107787207111));
#39027=CARTESIAN_POINT('',(0.0117936096599621,0.0164880702240289,0.0406318873215896));
#39028=CARTESIAN_POINT('',(0.0164747574023958,0.0118120830012056,0.0404737656105987));
#39029=CARTESIAN_POINT('',(0.0182195610466526,0.00888559080746583,0.040394874158353));
#39030=CARTESIAN_POINT('',(0.0201099449649453,0.00254904646741491,0.0402370945100878));
#39031=CARTESIAN_POINT('',(0.020253752763945,-0.000855095025009617,0.0401582031110839));
#39032=CARTESIAN_POINT('',(0.0188995181437999,-0.00733151759369263,0.0400000814000518));
#39033=CARTESIAN_POINT('',(0.0174038741197876,-0.0103928482309152,0.039921189947697));
#39034=CARTESIAN_POINT('',(0.0131330736126197,-0.0154411755340625,0.0397634102996911));
#39035=CARTESIAN_POINT('',(0.0103618958786451,-0.0174234555219608,0.0396845189006242));
#39036=CARTESIAN_POINT('',(0.00419935587391573,-0.0198320030893957,0.0395263971894589));
#39037=CARTESIAN_POINT('',(0.000818472741390671,-0.0202542892027093,0.0394475057375415));
#39038=CARTESIAN_POINT('',(-0.00574372411914673,-0.0194400915024628,0.0392897260887942));
#39039=CARTESIAN_POINT('',(-0.00891891303299861,-0.0182043587867157,0.0392108346900979));
#39040=CARTESIAN_POINT('',(-0.0143058582227063,-0.0143626375295573,0.0390527129789325));
#39041=CARTESIAN_POINT('',(-0.0165085498030464,-0.011763244115922,0.0389738215267757));
#39042=CARTESIAN_POINT('',(-0.0194161122680683,-0.00582426894810843,0.0388160418785074));
#39043=CARTESIAN_POINT('',(-0.020118261990339,-0.00249022549443076,0.038737150479517));
#39044=CARTESIAN_POINT('',(-0.0198484814844665,0.0041207668042561,0.0385790287684607));
#39045=CARTESIAN_POINT('',(-0.018877114557488,0.00738651979706084,0.0385001373161633));
#39046=CARTESIAN_POINT('',(-0.0154954895666888,0.0130689451554609,0.038342357668067));
#39047=CARTESIAN_POINT('',(-0.013088379647488,0.0154803102917281,0.0382634662690125));
#39048=CARTESIAN_POINT('',(-0.00740632255619973,0.0188703291568485,0.0381053445579125));
#39049=CARTESIAN_POINT('',(-0.00414105627275388,0.0198433309117916,0.0380264531056587));
#39050=CARTESIAN_POINT('',(0.00246565331268841,0.020120339910877,0.0378686734575188));
#39051=CARTESIAN_POINT('',(0.00580093170832172,0.0194240798968512,0.0377897820584329));
#39052=CARTESIAN_POINT('',(0.0117467325233343,0.016521416746776,0.0376316603474395));
#39053=CARTESIAN_POINT('',(0.0143472283554195,0.0143200267894043,0.0375527688952839));
#39054=CARTESIAN_POINT('',(0.0181926586425167,0.00894062055461352,0.0373949892468412));
#39055=CARTESIAN_POINT('',(0.0194339974740309,0.00576761915391247,0.0373160978479599));
#39056=CARTESIAN_POINT('',(0.020256029991367,-0.000797612238432598,0.03715797613686));
#39057=CARTESIAN_POINT('',(0.0198354365189604,-0.00417870635836715,0.0370790846845077));
#39058=CARTESIAN_POINT('',(0.0174352289591533,-0.0103402280211969,0.0369213050365665));
#39059=CARTESIAN_POINT('',(0.0154578465385381,-0.0131149025509978,0.0368424136374416));
#39060=CARTESIAN_POINT('',(0.010411264065787,-0.017393921836124,0.0366842919262981));
#39061=CARTESIAN_POINT('',(0.00735068258450235,-0.0188910982815803,0.0366054004741736));
#39062=CARTESIAN_POINT('',(0.00087967408912319,-0.0202517578968002,0.0364476208256344));
#39063=CARTESIAN_POINT('',(-0.00252471609431332,-0.0201139627377015,0.0363687294290392));
#39064=CARTESIAN_POINT('',(-0.00886718657456291,-0.0182295347893614,0.0362106077159948));
#39065=CARTESIAN_POINT('',(-0.0117945519274473,-0.0164861964499937,0.036131716259469));
#39066=CARTESIAN_POINT('',(-0.016472956754427,-0.0118130953090526,0.0359739366335474));
#39067=CARTESIAN_POINT('',(-0.0182196238625896,-0.00888768738915584,0.0358950450932448));
#39068=CARTESIAN_POINT('',(-0.0201110470261814,-0.00254729901032419,0.0357369235135449));
#39069=CARTESIAN_POINT('',(-0.0202526988688433,0.000856909313547677,0.0356580321690692));
#39070=CARTESIAN_POINT('',(-0.0188993787123355,0.00732945390426337,0.035500251691036));
#39071=CARTESIAN_POINT('',(-0.0174056823841494,0.0103917663907847,0.0354213651815531));
#39072=CARTESIAN_POINT('',(-0.0131321880026628,0.015443052118062,0.0352632383541236));
#39073=CARTESIAN_POINT('',(-0.0103598867730791,0.0174235644042914,0.0351843479349766));
#39074=CARTESIAN_POINT('',(-0.00420107043822686,0.0198308773727001,0.0350265834252997));
#39075=CARTESIAN_POINT('',(-0.000819557590625485,0.0202544098310457,0.0349476046181466));
#39076=CARTESIAN_POINT('',(0.00465054363677044,0.0195767431377992,0.0348159334247739));
#39077=CARTESIAN_POINT('',(0.0067902080359049,0.0189421083623588,0.0347635357583031));
#39078=CARTESIAN_POINT('',(0.0107581630684882,0.0170030639864308,0.0346579301873415));
#39079=CARTESIAN_POINT('',(0.0125800788597369,0.0157024545619653,0.0346052965200256));
#39080=CARTESIAN_POINT('',(0.0141341782018793,0.0141500708378154,0.0345528089000304));
#39081=CARTESIAN_POINT('',(0.0146663239187657,0.013618512572929,0.0345348363924741));
#39082=CARTESIAN_POINT('',(0.0151984696356521,0.0130869543080425,0.0345168638849177));
#39083=CARTESIAN_POINT('',(0.0157306153525384,0.012555396043156,0.0344988913773613));
#39084=CARTESIAN_POINT('',(0.0125465175185849,0.0157377537294883,0.0440539195793887));
#39085=CARTESIAN_POINT('',(0.0130783902203003,0.0152058810275692,0.0440359463862592));
#39086=CARTESIAN_POINT('',(0.0136102629220156,0.0146740083256501,0.0440179731931296));
#39087=CARTESIAN_POINT('',(0.0141421356237309,0.014142135623731,0.044));
#39088=CARTESIAN_POINT('',(0.0156953777773417,0.0125888934695251,0.0439475124007797));
#39089=CARTESIAN_POINT('',(0.0169970423533304,0.0107677303981291,0.0438948787697366));
#39090=CARTESIAN_POINT('',(0.0194235570551383,0.0058091099397162,0.0437628717686972));
#39091=CARTESIAN_POINT('',(0.0201185695458997,0.00247720350148128,0.0436841704089366));
#39092=CARTESIAN_POINT('',(0.01984559628717,-0.00412961236453083,0.0435263603675614));
#39093=CARTESIAN_POINT('',(0.0188745457210623,-0.00739584186127215,0.0434474606693054));
#39094=CARTESIAN_POINT('',(0.0154875898783386,-0.0130795979874077,0.0432893544847642));
#39095=CARTESIAN_POINT('',(0.0130776532928583,-0.0154881380856146,0.0432104490779356));
#39096=CARTESIAN_POINT('',(0.00739713377664075,-0.0188729847428303,0.0430526718436316));
#39097=CARTESIAN_POINT('',(0.00413192193560115,-0.0198462007289697,0.0429737801981818));
#39098=CARTESIAN_POINT('',(-0.00247892142177586,-0.0201196295423519,0.0428156580158873));
#39099=CARTESIAN_POINT('',(-0.00581335213997824,-0.0194193705481011,0.0427367670786146));
#39100=CARTESIAN_POINT('',(-0.0117539766613564,-0.0165151764007151,0.0425789873520905));
#39101=CARTESIAN_POINT('',(-0.0143546277377461,-0.0143139501213873,0.0425000959407626));
#39102=CARTESIAN_POINT('',(-0.0181993204388129,-0.00892912321441055,0.0423419742368419));
#39103=CARTESIAN_POINT('',(-0.0194368483323084,-0.00575464561573629,0.0422630828015258));
#39104=CARTESIAN_POINT('',(-0.0202547679627867,0.00080708991130746,0.0421053031556577));
#39105=CARTESIAN_POINT('',(-0.019834396408894,0.00418822452499619,0.0420264117301959));
#39106=CARTESIAN_POINT('',(-0.0174292474333672,0.0103520934760813,0.0418682900172373));
#39107=CARTESIAN_POINT('',(-0.0154485447986849,0.0131243850498825,0.0417893985921814));
#39108=CARTESIAN_POINT('',(-0.0104026394106094,0.0173980491055669,0.0416316189448621));
#39109=CARTESIAN_POINT('',(-0.00734214540805515,0.0188954334792125,0.0415527275196745));
#39110=CARTESIAN_POINT('',(-0.000866469142916212,0.0202532401525842,0.0413946058068358));
#39111=CARTESIAN_POINT('',(0.00253774208826097,0.0201113620728414,0.0413157143815739));
#39112=CARTESIAN_POINT('',(0.00887535903306692,0.0182245719132231,0.0411579347344072));
#39113=CARTESIAN_POINT('',(0.01180285059346,0.0164814205525399,0.041079043309115));
#39114=CARTESIAN_POINT('',(0.0164814200301334,0.0118028513183548,0.0409209215963417));
#39115=CARTESIAN_POINT('',(0.0182245715205425,0.00887535983630872,0.0408420301711456));
#39116=CARTESIAN_POINT('',(0.0201113619622517,0.00253774297547744,0.0406842505237827));
#39117=CARTESIAN_POINT('',(0.0202532401934251,-0.000866468250329324,0.0406053590986105));
#39118=CARTESIAN_POINT('',(0.0188954338003623,-0.00734214457422893,0.0404472373857936));
#39119=CARTESIAN_POINT('',(0.0173980495632035,-0.0104026386425633,0.0403683459604884));
#39120=CARTESIAN_POINT('',(0.0131243857321058,-0.0154485442207657,0.0402105663133872));
#39121=CARTESIAN_POINT('',(0.0103520942461436,-0.0174292469797191,0.0401316748881496));
#39122=CARTESIAN_POINT('',(0.00418822539793767,-0.01983439622144,0.0399735531752019));
#39123=CARTESIAN_POINT('',(0.00080709080647619,-0.0202547679266353,0.039894661750333));
#39124=CARTESIAN_POINT('',(-0.00575464475690967,-0.0194368485899185,0.0397368821024903));
#39125=CARTESIAN_POINT('',(-0.00892912243213517,-0.0181993208157078,0.0396579906776233));
#39126=CARTESIAN_POINT('',(-0.0143139494659693,-0.0143546283873442,0.0394998689646755));
#39127=CARTESIAN_POINT('',(-0.0165151759031107,-0.0117539773787766,0.0394209775395684));
#39128=CARTESIAN_POINT('',(-0.0194193704330004,-0.00581335285115579,0.0392631978922023));
#39129=CARTESIAN_POINT('',(-0.0201196283819678,-0.00247892301874085,0.0391843064670424));
#39130=CARTESIAN_POINT('',(-0.019846201989664,0.00413192110745882,0.0390261847542038));
#39131=CARTESIAN_POINT('',(-0.0188729808890436,0.00739713537075163,0.0389472933289547));
#39132=CARTESIAN_POINT('',(-0.0154881330235243,0.0130776433210231,0.0387895136817632));
#39133=CARTESIAN_POINT('',(-0.0130796649391004,0.0154876360572498,0.0387106222565379));
#39134=CARTESIAN_POINT('',(-0.00739573778198963,0.0188745216658114,0.0385525005436556));
#39135=CARTESIAN_POINT('',(-0.00412990836797088,0.019845676511613,0.0384736091184501));
#39136=CARTESIAN_POINT('',(0.00247695877305382,0.0201189387051795,0.0383158294712149));
#39137=CARTESIAN_POINT('',(0.00581183108735372,0.019420791049107,0.0382369380459571));
#39138=CARTESIAN_POINT('',(0.0117560316740477,0.0165148486136556,0.0380788163331838));
#39139=CARTESIAN_POINT('',(0.0143552893388841,0.0143119770586781,0.0379999249080766));
#39140=CARTESIAN_POINT('',(0.0181976691008663,0.00893038961533982,0.0378421452605361));
#39141=CARTESIAN_POINT('',(0.0194372055562126,0.00575669572993267,0.0377632538354854));
#39142=CARTESIAN_POINT('',(0.0202556175238696,-0.000808989603994321,0.0376051321226031));
#39143=CARTESIAN_POINT('',(0.0198331064944038,-0.00418985752894618,0.0375262406973004));
#39144=CARTESIAN_POINT('',(0.0174294044206095,-0.0103500184023128,0.0373684610502614));
#39145=CARTESIAN_POINT('',(0.0154504564687845,-0.0131235627964765,0.0372895696249671));
#39146=CARTESIAN_POINT('',(0.0104015137184082,-0.0173997993613175,0.0371314479120412));
#39147=CARTESIAN_POINT('',(0.00734007279563755,-0.0188952467752599,0.0370525564869662));
#39148=CARTESIAN_POINT('',(0.000868292189651466,-0.0202522366194585,0.0368947768393292));
#39149=CARTESIAN_POINT('',(-0.00253600814635427,-0.0201125127235025,0.0368158854165646));
#39150=CARTESIAN_POINT('',(-0.0088774399761798,-0.018224586826797,0.0366577637017353));
#39151=CARTESIAN_POINT('',(-0.0118038279130671,-0.0164795833028888,0.0365788722722735));
#39152=CARTESIAN_POINT('',(-0.0164795828284599,-0.0118038285955315,0.0364210926472371));
#39153=CARTESIAN_POINT('',(-0.0182245861741416,-0.00887744099613647,0.0363422010807297));
#39154=CARTESIAN_POINT('',(-0.0201125128390728,-0.00253600893042723,0.0361840794994547));
#39155=CARTESIAN_POINT('',(-0.0202522359742467,0.000868291897198348,0.0361051881812469));
#39156=CARTESIAN_POINT('',(-0.0188952453448132,0.00734006951024311,0.0359474077050742));
#39157=CARTESIAN_POINT('',(-0.0173998172706736,0.0104015239313007,0.0358685211701349));
#39158=CARTESIAN_POINT('',(-0.013123538002664,0.0154504543843868,0.0357103943350004));
#39159=CARTESIAN_POINT('',(-0.0103501050287235,0.0174294035933487,0.03563150396077));
#39160=CARTESIAN_POINT('',(-0.00418992058649385,0.0198332176625935,0.0354737394315266));
#39161=CARTESIAN_POINT('',(-0.000808179644509043,0.0202548576790242,0.0353947606000568));
#39162=CARTESIAN_POINT('',(0.00466154596368762,0.0195741550782838,0.035263089448488));
#39163=CARTESIAN_POINT('',(0.00680083319771015,0.0189382544178338,0.035210691736618));
#39164=CARTESIAN_POINT('',(0.0107677296476345,0.0169970428264161,0.0351050861356576));
#39165=CARTESIAN_POINT('',(0.0125888927781881,0.0156953783332082,0.0350524525049133));
#39166=CARTESIAN_POINT('',(0.0141421349996867,0.0141421362469037,0.0349999649054552));
#39167=CARTESIAN_POINT('',(0.0146739872262749,0.013610284066608,0.034981992404931));
#39168=CARTESIAN_POINT('',(0.015205839452863,0.0130784318863123,0.0349640199044069));
#39169=CARTESIAN_POINT('',(0.0157376916794511,0.0125465797060166,0.0349460474038827));
#39170=CARTESIAN_POINT('',(0.0125553467792133,0.0157306873651733,0.0445012306627941));
#39171=CARTESIAN_POINT('',(0.0130869258772525,0.0151985206348258,0.0444832574621166));
#39172=CARTESIAN_POINT('',(0.0136185049752917,0.0146663539044784,0.0444652842614391));
#39173=CARTESIAN_POINT('',(0.0141500840733309,0.014134187174131,0.0444473110607616));
#39174=CARTESIAN_POINT('',(0.0157024688082309,0.012580086360799,0.0443948234394989));
#39175=CARTESIAN_POINT('',(0.0170030789402721,0.0107581689802764,0.0443421897745895));
#39176=CARTESIAN_POINT('',(0.0194268856090395,0.005798220899335,0.0442101828068617));
#39177=CARTESIAN_POINT('',(0.0201199759201218,0.00246589637047508,0.0441314814930198));
#39178=CARTESIAN_POINT('',(0.0198432671535113,-0.00414076773973825,0.0439736714089908));
#39179=CARTESIAN_POINT('',(0.0188703667732599,-0.00740643601741953,0.0438947717243222));
#39180=CARTESIAN_POINT('',(0.0154802701864641,-0.0130883236213368,0.043736665523217));
#39181=CARTESIAN_POINT('',(0.0130689628335657,-0.015495510096433,0.0436577601447141));
#39182=CARTESIAN_POINT('',(0.00738652025425392,-0.0188771344799994,0.0434999829142618));
#39183=CARTESIAN_POINT('',(0.00412076702506264,-0.019848496607824,0.0434210912402082));
#39184=CARTESIAN_POINT('',(-0.00249022978855514,-0.0201182786486563,0.0432629690568112));
#39185=CARTESIAN_POINT('',(-0.00582427658703155,-0.0194161264761786,0.0431840781465005));
#39186=CARTESIAN_POINT('',(-0.0117632558368309,-0.0165085609856232,0.0430262984207961));
#39187=CARTESIAN_POINT('',(-0.0143626509177512,-0.0143058673332415,0.0429474069833575));
#39188=CARTESIAN_POINT('',(-0.0182043744607715,-0.00891891726746548,0.0427892852776344));
#39189=CARTESIAN_POINT('',(-0.0194401076376572,-0.00574372569960893,0.0427103938693811));
#39190=CARTESIAN_POINT('',(-0.0202543049798394,0.00081847641544852,0.0425526142244181));
#39191=CARTESIAN_POINT('',(-0.019832018033368,0.00419936212873341,0.0424737227727762));
#39192=CARTESIAN_POINT('',(-0.0174234676481007,0.0103619066592638,0.0423156010580346));
#39193=CARTESIAN_POINT('',(-0.0154411856816897,0.013133086258712,0.0422367096600366));
#39194=CARTESIAN_POINT('',(-0.0103928537834461,0.0174038893393296,0.0420789300136223));
#39195=CARTESIAN_POINT('',(-0.00733152053144792,0.0188995340748007,0.0420000385622549));
#39196=CARTESIAN_POINT('',(-0.000855092631995909,0.0202537688125186,0.0418419168476332));
#39197=CARTESIAN_POINT('',(0.00254905150411026,0.0201099603769654,0.041763025449429));
#39198=CARTESIAN_POINT('',(0.00888560051174127,0.018219574019257,0.0416052458031673));
#39199=CARTESIAN_POINT('',(0.0118120947313283,0.0164747685752221,0.0415263543516954));
#39200=CARTESIAN_POINT('',(0.0164880849681926,0.0117936164343411,0.0413682326371391));
#39201=CARTESIAN_POINT('',(0.0182295837318557,0.00886512531747734,0.041289341239002));
#39202=CARTESIAN_POINT('',(0.0201127794509136,0.0025264355639602,0.0411315615925416));
#39203=CARTESIAN_POINT('',(0.0202527274451672,-0.000877845419409433,0.0410526701411921));
#39204=CARTESIAN_POINT('',(0.0188913480406447,-0.00735277523975905,0.0408945484265898));
#39205=CARTESIAN_POINT('',(0.0173922229869061,-0.010412432449118,0.0408156570283436));
#39206=CARTESIAN_POINT('',(0.013115694838997,-0.0154559154626221,0.0406578773821473));
#39207=CARTESIAN_POINT('',(0.0103422892148445,-0.0174350404457136,0.04057898593073));
#39208=CARTESIAN_POINT('',(0.00417709106237456,-0.0198367901833228,0.0404208642159993));
#39209=CARTESIAN_POINT('',(0.000795704924781183,-0.0202552468165628,0.0403419728181881));
#39210=CARTESIAN_POINT('',(-0.00576556918149452,-0.0194336045528674,0.0401841931712504));
#39211=CARTESIAN_POINT('',(-0.00893933537146573,-0.0181942810977416,0.0401053017202037));
#39212=CARTESIAN_POINT('',(-0.0143220435149382,-0.0143466164678946,0.0399471800054729));
#39213=CARTESIAN_POINT('',(-0.0165218043008303,-0.0117447074283131,0.0398682886074247));
#39214=CARTESIAN_POINT('',(-0.0194226297277284,-0.00580243296895581,0.0397105089609612));
#39215=CARTESIAN_POINT('',(-0.0201209952474043,-0.00246761662382356,0.0396316175096228));
#39216=CARTESIAN_POINT('',(-0.0198439217044277,0.00414307927850888,0.0394734957950011));
#39217=CARTESIAN_POINT('',(-0.0188688457872152,0.00740775462548082,0.0393946043968098));
#39218=CARTESIAN_POINT('',(-0.0154807739294173,0.0130863445027465,0.0392368247505233));
#39219=CARTESIAN_POINT('',(-0.0130709472088153,0.0154949643630416,0.0391579332991183));
#39220=CARTESIAN_POINT('',(-0.0073851493374211,0.0188787156285615,0.0389998115844529));
#39221=CARTESIAN_POINT('',(-0.00411875659755924,0.0198480229247906,0.0389209201863052));
#39222=CARTESIAN_POINT('',(0.00248826815368158,0.0201175370136022,0.038763140539975));
#39223=CARTESIAN_POINT('',(0.00582273424583599,0.0194175010609274,0.0386842490885363));
#39224=CARTESIAN_POINT('',(0.0117653340493188,0.0165082782029806,0.0385261273739824));
#39225=CARTESIAN_POINT('',(0.0143633531175618,0.0143039245366409,0.0384472359759329));
#39226=CARTESIAN_POINT('',(0.0182026812966341,0.0089201551284029,0.038289456329295));
#39227=CARTESIAN_POINT('',(0.0194404147508235,0.00574576851816482,0.0382105648780657));
#39228=CARTESIAN_POINT('',(0.0202552049133456,-0.00082037091475211,0.0380524431634004));
#39229=CARTESIAN_POINT('',(0.0198307756618918,-0.00420101256628627,0.0379735517651567));
#39230=CARTESIAN_POINT('',(0.0174235778623587,-0.0103598121783247,0.0378157721190203));
#39231=CARTESIAN_POINT('',(0.0154430638364627,-0.0131322260449673,0.0377368806675474));
#39232=CARTESIAN_POINT('',(0.0103917599900155,-0.0174056789245918,0.0375787589528385));
#39233=CARTESIAN_POINT('',(0.00732945932774028,-0.0188993967074641,0.0374998675548225));
#39234=CARTESIAN_POINT('',(0.000856906343411505,-0.0202527155081179,0.0373420879080881));
#39235=CARTESIAN_POINT('',(-0.00254730411400811,-0.020111062206499,0.037263196459145));
#39236=CARTESIAN_POINT('',(-0.00888769693324891,-0.0182196371484855,0.0371050747425303));
#39237=CARTESIAN_POINT('',(-0.0118131071152121,-0.0164729678626203,0.0370261833401418));
#39238=CARTESIAN_POINT('',(-0.0164862112001391,-0.0117945586687005,0.0368684037159908));
#39239=CARTESIAN_POINT('',(-0.0182295502064164,-0.00886719105009516,0.0367895121232697));
#39240=CARTESIAN_POINT('',(-0.0201139791602471,-0.00252471493560122,0.036631390540419));
#39241=CARTESIAN_POINT('',(-0.0202517729191377,0.0008796784278545,0.0365524992484881));
#39242=CARTESIAN_POINT('',(-0.0188911105440114,0.00735068879727244,0.0363947187741767));
#39243=CARTESIAN_POINT('',(-0.017393950123421,0.0104112848553249,0.036315832213772));
#39244=CARTESIAN_POINT('',(-0.0131148850032058,0.015457859217509,0.0361577053709299));
#39245=CARTESIAN_POINT('',(-0.0103403198924667,0.0174352448071932,0.0360788150416316));
#39246=CARTESIAN_POINT('',(-0.00417876686845709,0.0198355587640019,0.0359210504928149));
#39247=CARTESIAN_POINT('',(-0.000796797752995223,0.0202553056822977,0.0358420716370199));
#39248=CARTESIAN_POINT('',(0.0046725521057531,0.0195715661213371,0.0357104005272695));
#39249=CARTESIAN_POINT('',(0.00681146204387857,0.0189343991369214,0.0356580027699848));
#39250=CARTESIAN_POINT('',(0.0107772995440717,0.0169910195785142,0.035552397139015));
#39251=CARTESIAN_POINT('',(0.0125977097529387,0.01568829965071,0.0354997635448551));
#39252=CARTESIAN_POINT('',(0.0141500945565799,0.0141341989046066,0.0354472759659412));
#39253=CARTESIAN_POINT('',(0.0146816531910996,0.013602052706984,0.0354293034724516));
#39254=CARTESIAN_POINT('',(0.0152132118256192,0.0130699065093615,0.0354113309789621));
#39255=CARTESIAN_POINT('',(0.0157447704601389,0.0125377603117389,0.0353933584854725));
#39256=CARTESIAN_POINT('',(0.0123934894645848,0.0155082763123231,0.0449580753891009));
#39257=CARTESIAN_POINT('',(0.012917382287782,0.0149831956652547,0.0449401110951834));
#39258=CARTESIAN_POINT('',(0.0134412751109791,0.0144581150181862,0.0449221468012659));
#39259=CARTESIAN_POINT('',(0.0139651679341763,0.0139330343711178,0.0449041825073484));
#39260=CARTESIAN_POINT('',(0.0154951062339604,0.0123996272373401,0.0448517208967365));
#39261=CARTESIAN_POINT('',(0.016777425009008,0.010601053512311,0.0447990399263663));
#39262=CARTESIAN_POINT('',(0.0191649977879812,0.00570814164951054,0.0446671060793837));
#39263=CARTESIAN_POINT('',(0.0198468001189922,0.00242076902532767,0.0445883674334732));
#39264=CARTESIAN_POINT('',(0.0195699819612324,-0.0040960439270075,0.0444305316090981));
#39265=CARTESIAN_POINT('',(0.0186082730960355,-0.00731663434116805,0.0443516174767989));
#39266=CARTESIAN_POINT('',(0.015261595968773,-0.0129183666546227,0.0441935699927201));
#39267=CARTESIAN_POINT('',(0.0128817488018725,-0.0152915238210584,0.0441146526150789));
#39268=CARTESIAN_POINT('',(0.00727453700603762,-0.0186238589222907,0.0439568433608528));
#39269=CARTESIAN_POINT('',(0.00405257752468377,-0.0195799653309641,0.0438779364735199));
#39270=CARTESIAN_POINT('',(-0.00246754686692629,-0.0198422575935462,0.0437198763603395));
#39271=CARTESIAN_POINT('',(-0.00575590144654004,-0.01914782678123,0.0436409700833429));
#39272=CARTESIAN_POINT('',(-0.0116124723502935,-0.0162762833167919,0.0434831589606206));
#39273=CARTESIAN_POINT('',(-0.0141751414837983,-0.0141019088846481,0.0434042522201484));
#39274=CARTESIAN_POINT('',(-0.0179608924119463,-0.00878693729344424,0.0432461924731406));
#39275=CARTESIAN_POINT('',(-0.0191780984979996,-0.00565422105111067,0.0431672858230386));
#39276=CARTESIAN_POINT('',(-0.0199773791436797,0.000819289371129895,0.043009474760093));
#39277=CARTESIAN_POINT('',(-0.0195587129181748,0.0041539402136244,0.0429305680097516));
#39278=CARTESIAN_POINT('',(-0.0171798063834406,0.0102302578552052,0.0427725082558356));
#39279=CARTESIAN_POINT('',(-0.0152229499734908,0.0129626953923687,0.0426936016133913));
#39280=CARTESIAN_POINT('',(-0.0102407091285208,0.0171725009568401,0.0425357905493827));
#39281=CARTESIAN_POINT('',(-0.00722006250668779,0.0186458887612477,0.0424568837992276));
#39282=CARTESIAN_POINT('',(-0.000832034517765779,0.0199777786987247,0.0422988240454017));
#39283=CARTESIAN_POINT('',(0.00252576960124855,0.0198340657872349,0.0422199174028092));
#39284=CARTESIAN_POINT('',(0.00877510515323934,0.0179656461646544,0.0420621063389043));
#39285=CARTESIAN_POINT('',(0.0116607131388107,0.0162427288161061,0.0419831995886749));
#39286=CARTESIAN_POINT('',(0.0162696468896929,0.0116233606696467,0.041825139834901));
#39287=CARTESIAN_POINT('',(0.0179858800358563,0.00873371610839782,0.0417462331923493));
#39288=CARTESIAN_POINT('',(0.0198397643303848,0.00248005320174727,0.0415884221283116));
#39289=CARTESIAN_POINT('',(0.0199756736539967,-0.000878027543581936,0.0415095153781676));
#39290=CARTESIAN_POINT('',(0.0186293413170257,-0.00726302727977779,0.0413514556243556));
#39291=CARTESIAN_POINT('',(0.0171489183145194,-0.0102802859091026,0.0412725489817254));
#39292=CARTESIAN_POINT('',(0.0129275399628127,-0.0152527251032007,0.0411147379178828));
#39293=CARTESIAN_POINT('',(0.0101906026857989,-0.0172031999115253,0.0410358311676849));
#39294=CARTESIAN_POINT('',(0.00410892095107614,-0.019568359455848,0.0408777714137857));
#39295=CARTESIAN_POINT('',(0.000773258535901459,-0.0199792829940002,0.0407988647714664));
#39296=CARTESIAN_POINT('',(-0.005698375986877,-0.0191649530051426,0.0406410537070893));
#39297=CARTESIAN_POINT('',(-0.008828210915612,-0.0179404894672697,0.0405621469571608));
#39298=CARTESIAN_POINT('',(-0.0141346078249767,-0.0141427290439189,0.0404040872032571));
#39299=CARTESIAN_POINT('',(-0.0163030536505294,-0.0115749781595783,0.0403251805607742));
#39300=CARTESIAN_POINT('',(-0.019160972463498,-0.00571174638979979,0.0401673694967289));
#39301=CARTESIAN_POINT('',(-0.0198477500854794,-0.00242183542833849,0.0400884627465911));
#39302=CARTESIAN_POINT('',(-0.0195707163823238,0.00409768025304344,0.0399304029927742));
#39303=CARTESIAN_POINT('',(-0.0186071088678102,0.00731745702488812,0.0398514963501819));
#39304=CARTESIAN_POINT('',(-0.0152617412065595,0.0129168946697514,0.0396936852862684));
#39305=CARTESIAN_POINT('',(-0.0128831697885874,0.0152912526136711,0.0396147785360814));
#39306=CARTESIAN_POINT('',(-0.00727372673197496,0.0186251663778611,0.0394567187822312));
#39307=CARTESIAN_POINT('',(-0.00405119419586402,0.0195795174434124,0.0393778121396736));
#39308=CARTESIAN_POINT('',(0.00246620997808876,0.0198414898863339,0.0392200010757239));
#39309=CARTESIAN_POINT('',(0.00575489811217428,0.0191488803332586,0.0391410943255175));
#39310=CARTESIAN_POINT('',(0.011614013504857,0.0162763206370897,0.0389830345717425));
#39311=CARTESIAN_POINT('',(0.0141755224604208,0.0141005049802241,0.0389041279292564));
#39312=CARTESIAN_POINT('',(0.0179595192168192,0.00878763802580743,0.0387463168650887));
#39313=CARTESIAN_POINT('',(0.0191784316338705,0.00565563704304498,0.0386674101150348));
#39314=CARTESIAN_POINT('',(0.0199782533217446,-0.000820559190878668,0.0385093503611727));
#39315=CARTESIAN_POINT('',(0.0195577459963842,-0.00415502698829191,0.0384304437185515));
#39316=CARTESIAN_POINT('',(0.0171796419344795,-0.0102287250214563,0.0382726326547425));
#39317=CARTESIAN_POINT('',(0.0152243176035623,-0.0129621998058823,0.0381937259045076));
#39318=CARTESIAN_POINT('',(0.0102401242086823,-0.017173927313282,0.0380356661506272));
#39319=CARTESIAN_POINT('',(0.00721862383931954,-0.0186456736966964,0.0379567595081661));
#39320=CARTESIAN_POINT('',(0.000833227810519059,-0.0199768026475956,0.0377989484439109));
#39321=CARTESIAN_POINT('',(-0.00252460669506535,-0.0198349396539981,0.0377200416955754));
#39322=CARTESIAN_POINT('',(-0.00877661916499571,-0.0179659366380679,0.0375619819402062));
#39323=CARTESIAN_POINT('',(-0.0116613199831515,-0.0162414067754668,0.0374830752947276));
#39324=CARTESIAN_POINT('',(-0.016268177126898,-0.011623825758288,0.0373252642471344));
#39325=CARTESIAN_POINT('',(-0.0179859753970511,-0.00873516787953567,0.0372463573912147));
#39326=CARTESIAN_POINT('',(-0.019840835829584,-0.00247894445095143,0.0370882977386692));
#39327=CARTESIAN_POINT('',(-0.0199748980239041,0.000879258931138491,0.0370093911648565));
#39328=CARTESIAN_POINT('',(-0.0186289256182034,0.0072615402658288,0.0368515794869236));
#39329=CARTESIAN_POINT('',(-0.0171501996025803,0.0102795817780441,0.0367726764469661));
#39330=CARTESIAN_POINT('',(-0.0129271754315416,0.0152542235327993,0.0366146126864771));
#39331=CARTESIAN_POINT('',(-0.0101892187172689,0.0172032332553386,0.0365357072320943));
#39332=CARTESIAN_POINT('',(-0.00411000464968758,0.0195672966718648,0.0363779078077777));
#39333=CARTESIAN_POINT('',(-0.000773762353009196,0.0199792454619298,0.0362989295369263));
#39334=CARTESIAN_POINT('',(0.00461999775143137,0.0193017632934899,0.0361672953686332));
#39335=CARTESIAN_POINT('',(0.00672968236710639,0.0186718674536964,0.0361148465374304));
#39336=CARTESIAN_POINT('',(0.0106397244891325,0.0167530479282312,0.036009299345223));
#39337=CARTESIAN_POINT('',(0.0124352515814873,0.0154664643618175,0.0359566185174661));
#39338=CARTESIAN_POINT('',(0.0139651899324739,0.0139330572761716,0.0359041569927753));
#39339=CARTESIAN_POINT('',(0.014489062582375,0.0134079968821915,0.0358861934206222));
#39340=CARTESIAN_POINT('',(0.0150129352322761,0.0128829364882113,0.0358682298484692));
#39341=CARTESIAN_POINT('',(0.0155368078821772,0.0123578760942311,0.0358502662763162));
#39342=CARTESIAN_POINT('',(0.0120305257775094,0.015047717626688,0.0450430352084097));
#39343=CARTESIAN_POINT('',(0.0125386004906958,0.0145383434030553,0.0450250899362179));
#39344=CARTESIAN_POINT('',(0.0130466752038823,0.0140289691794226,0.0450071446640261));
#39345=CARTESIAN_POINT('',(0.0135547499170688,0.0135195949557899,0.0449891993918343));
#39346=CARTESIAN_POINT('',(0.015038494164818,0.0120320557127389,0.0449367933308794));
#39347=CARTESIAN_POINT('',(0.0162838776612131,0.0102847972275788,0.0448840114797136));
#39348=CARTESIAN_POINT('',(0.0185995162676072,0.0055375795976936,0.0447522336035345));
#39349=CARTESIAN_POINT('',(0.0192610546483522,0.00234696454026363,0.0446734152009566));
#39350=CARTESIAN_POINT('',(0.0189914348903327,-0.00397841114725085,0.0445155245324582));
#39351=CARTESIAN_POINT('',(0.0180572885482573,-0.00710392355101288,0.0444365795423942));
#39352=CARTESIAN_POINT('',(0.0148095155549984,-0.0125383247637423,0.0442786573913219));
#39353=CARTESIAN_POINT('',(0.0124995304672202,-0.0148415576411829,0.0441997143515908));
#39354=CARTESIAN_POINT('',(0.00705668445210766,-0.0180751219128047,0.0440418367521038));
#39355=CARTESIAN_POINT('',(0.00392925637374929,-0.0190023614305585,0.0439628974570812));
#39356=CARTESIAN_POINT('',(-0.00239664418868276,-0.0192559260685448,0.0438049698017331));
#39357=CARTESIAN_POINT('',(-0.00558825700628719,-0.0185817388652116,0.0437260306791333));
#39358=CARTESIAN_POINT('',(-0.0112722447088396,-0.015793772453778,0.0435681525546579));
#39359=CARTESIAN_POINT('',(-0.0137590407905356,-0.0136827495892477,0.0434892132100029));
#39360=CARTESIAN_POINT('',(-0.0174312553179828,-0.00852560155963431,0.0433312856842805));
#39361=CARTESIAN_POINT('',(-0.0186124958588404,-0.00548494660580613,0.0432523464547741));
#39362=CARTESIAN_POINT('',(-0.0193873503391936,0.000798370606699635,0.0430944683451649));
#39363=CARTESIAN_POINT('',(-0.0189802212997522,0.0040348530646949,0.0430155290000279));
#39364=CARTESIAN_POINT('',(-0.0166713408352946,0.00992980053306335,0.0428576014718638));
#39365=CARTESIAN_POINT('',(-0.0147718837601594,0.0125817761690868,0.0427786622444798));
#39366=CARTESIAN_POINT('',(-0.00993550644959224,0.0166671071404195,0.0426207841346389));
#39367=CARTESIAN_POINT('',(-0.00700335335034363,0.0180964604736507,0.0425418447894979));
#39368=CARTESIAN_POINT('',(-0.000805463021044599,0.0193877738074862,0.0423839172613603));
#39369=CARTESIAN_POINT('',(0.00245358663115674,0.0192481052063996,0.0423049780339514));
#39370=CARTESIAN_POINT('',(0.00851893643492141,0.0174337164957497,0.0421470999241113));
#39371=CARTESIAN_POINT('',(0.0113192788681312,0.0157607983849654,0.0420681605789608));
#39372=CARTESIAN_POINT('',(0.01579024780393,0.0112784138147657,0.0419102330508445));
#39373=CARTESIAN_POINT('',(0.0174558531374492,0.00847365521083588,0.0418312938234208));
#39374=CARTESIAN_POINT('',(0.019254339634141,0.00240357111284854,0.0416734157135893));
#39375=CARTESIAN_POINT('',(0.0193854708067216,-0.000855781179293895,0.0415944763684416));
#39376=CARTESIAN_POINT('',(0.0180783569263752,-0.00705035848239528,0.0414365488403111));
#39377=CARTESIAN_POINT('',(0.0166413068129427,-0.0099788049861067,0.0413576096128707));
#39378=CARTESIAN_POINT('',(0.0125433147624612,-0.014804458909604,0.0411997315030867));
#39379=CARTESIAN_POINT('',(0.0098864162360075,-0.0166969342644347,0.0411207921579174));
#39380=CARTESIAN_POINT('',(0.00398560024159757,-0.0189907749869355,0.0409628646297827));
#39381=CARTESIAN_POINT('',(0.00074801108265274,-0.019389433225327,0.040883925402392));
#39382=CARTESIAN_POINT('',(-0.00553325382190865,-0.0185981141783993,0.0407260472925128));
#39383=CARTESIAN_POINT('',(-0.00857075650521062,-0.0174089337051664,0.040647107947397));
#39384=CARTESIAN_POINT('',(-0.0137185235041463,-0.0137235803184355,0.0404891804192505));
#39385=CARTESIAN_POINT('',(-0.015823060245059,-0.0112312245935179,0.0404102411918493));
#39386=CARTESIAN_POINT('',(-0.0185961207351541,-0.00553994967888425,0.0402523630820029));
#39387=CARTESIAN_POINT('',(-0.0192619352045528,-0.00234663418538221,0.0401734237368522));
#39388=CARTESIAN_POINT('',(-0.0189922425670375,0.0039786010308927,0.0400154962087426));
#39389=CARTESIAN_POINT('',(-0.0180567983964916,0.00710363801585321,0.0399365569813077));
#39390=CARTESIAN_POINT('',(-0.014808974146672,0.0125379836321928,0.0397786788714918));
#39391=CARTESIAN_POINT('',(-0.0124998034587373,0.0148419592142143,0.0396997395263325));
#39392=CARTESIAN_POINT('',(-0.00705702067722423,0.018075757329926,0.0395418119982097));
#39393=CARTESIAN_POINT('',(-0.00392920500396389,0.0190018680510246,0.0394628727707926));
#39394=CARTESIAN_POINT('',(0.00239663846866875,0.0192552037872495,0.0393049946609543));
#39395=CARTESIAN_POINT('',(0.00558844624724444,0.0185821986957283,0.0392260553158074));
#39396=CARTESIAN_POINT('',(0.0112725936445692,0.0157944033255879,0.0390681277876822));
#39397=CARTESIAN_POINT('',(0.0137586555167324,0.0136824354468426,0.0389891885602771));
#39398=CARTESIAN_POINT('',(0.0174306481390726,0.00852521285931437,0.0388313104504172));
#39399=CARTESIAN_POINT('',(0.0186129842221382,0.00548503948671966,0.0387523711052963));
#39400=CARTESIAN_POINT('',(0.0193880693395357,-0.000798317714726632,0.0385944435771406));
#39401=CARTESIAN_POINT('',(0.0189797475904416,-0.00403470231839642,0.0385155043497221));
#39402=CARTESIAN_POINT('',(0.0166706833201622,-0.00992950484529438,0.0383576262399204));
#39403=CARTESIAN_POINT('',(0.0147722286277553,-0.012582134206778,0.0382786868947513));
#39404=CARTESIAN_POINT('',(0.00993594398497793,-0.0166676801329163,0.0381207593666291));
#39405=CARTESIAN_POINT('',(0.00700322045568562,-0.0180959814502239,0.0380418201392278));
#39406=CARTESIAN_POINT('',(0.000805350935101188,-0.0193870616326328,0.0378839420293038));
#39407=CARTESIAN_POINT('',(-0.00245369774827242,-0.0192485897388964,0.0378050026846886));
#39408=CARTESIAN_POINT('',(-0.00851917681047392,-0.0174343961879857,0.0376470751559724));
#39409=CARTESIAN_POINT('',(-0.0113189505446799,-0.0157604251224328,0.0375681359284152));
#39410=CARTESIAN_POINT('',(-0.0157897129232712,-0.0112779304094601,0.0374102578225529));
#39411=CARTESIAN_POINT('',(-0.0174563193909108,-0.00847382750256133,0.0373313184476594));
#39412=CARTESIAN_POINT('',(-0.019255040384606,-0.0024037413944109,0.0371733909553239));
#39413=CARTESIAN_POINT('',(-0.0193849780691145,0.00085571010424288,0.0370944517182392));
#39414=CARTESIAN_POINT('',(-0.0180776585182107,0.0070501732653501,0.0369365734491815));
#39415=CARTESIAN_POINT('',(-0.0166417173926014,0.00997911260897645,0.0368576352931063));
#39416=CARTESIAN_POINT('',(-0.0125438251053851,0.0148049402006138,0.0366997061634564));
#39417=CARTESIAN_POINT('',(-0.00988624181041278,0.0166965076677071,0.0366207683432865));
#39418=CARTESIAN_POINT('',(-0.00398545896551984,0.018990177231314,0.0364628945348312));
#39419=CARTESIAN_POINT('',(-0.00074725003243382,0.019389251433117,0.0363839175606247));
#39420=CARTESIAN_POINT('',(0.0044859517746727,0.0187311643862688,0.0362523621408917));
#39421=CARTESIAN_POINT('',(0.00653402122317466,0.0181193042775869,0.0361998044101114));
#39422=CARTESIAN_POINT('',(0.0103271047795814,0.0162572081871673,0.0360943819838573));
#39423=CARTESIAN_POINT('',(0.0120710301301553,0.0150071588432212,0.0360416002884952));
#39424=CARTESIAN_POINT('',(0.0135547743899825,0.0135196196088883,0.0359891943217175));
#39425=CARTESIAN_POINT('',(0.0140628295261061,0.0130102650195225,0.0359712497733841));
#39426=CARTESIAN_POINT('',(0.0145708846622297,0.0125009104301567,0.0359533052250506));
#39427=CARTESIAN_POINT('',(0.0150789397983533,0.0119915558407908,0.0359353606767172));
#39428=CARTESIAN_POINT('',(0.,0.,0.034));
#39429=CARTESIAN_POINT('',(0.,0.,0.0458));
#39430=CARTESIAN_POINT('',(0.,0.,0.0442));
#39431=CARTESIAN_POINT('',(0.,0.,0.0440005108565096));
#39432=CARTESIAN_POINT('',(0.0122857142857138,0.,0.0440005108565096));
#39433=CARTESIAN_POINT('',(0.,0.,0.0458));
#39434=CARTESIAN_POINT('',(-0.0175,0.0303108891324553,-0.0157695526217005));
#39435=CARTESIAN_POINT('',(-0.0283297125253659,0.0375023651018189,0.03));
#39436=CARTESIAN_POINT('',(-0.0277718804811134,0.0383424097188667,0.03));
#39437=CARTESIAN_POINT('',(-0.0264885007929982,0.0398605778598196,0.0298963633816331));
#39438=CARTESIAN_POINT('',(-0.0240577626239275,0.0416704416785127,0.0297946825337269));
#39439=CARTESIAN_POINT('',(-0.0212962525642577,0.0428638448919929,0.0298954697823391));
#39440=CARTESIAN_POINT('',(-0.0193192917538977,0.0432223757172947,0.03));
#39441=CARTESIAN_POINT('',(-0.0183131446174913,0.0432854332797865,0.03));
#39442=CARTESIAN_POINT('',(-0.0175,0.0303108891324553,0.022));
#39443=CARTESIAN_POINT('',(-0.0305,0.0303108891324553,0.022));
#39444=CARTESIAN_POINT('',(-0.0175,0.0303108891324553,0.022));
#39445=CARTESIAN_POINT('',(0.,0.,0.0400107279868694));
#39446=CARTESIAN_POINT('',(0.,0.,0.033));
#39447=CARTESIAN_POINT('',(0.,0.,0.027));
#39448=CARTESIAN_POINT('',(0.,0.,-0.033));
#39449=CARTESIAN_POINT('',(0.,0.,-0.033));
#39450=CARTESIAN_POINT('',(-0.053,0.,-0.033));
#39451=CARTESIAN_POINT('',(4.33053857950996E-16,-0.043,0.083));
#39452=CARTESIAN_POINT('',(-0.043,1.7347234759768E-17,0.083));
#39453=CARTESIAN_POINT('',(-1.32786462810487E-16,0.043,0.083));
#39454=CARTESIAN_POINT('',(0.043,-1.7347234759768E-17,0.083));
#39455=CARTESIAN_POINT('',(0.,0.,0.));
#39456=CARTESIAN_POINT('',(-0.04368363807983,-0.0108046177216235,0.083));
#39457=CARTESIAN_POINT('',(-0.0485373756442556,-0.0120051308018038,0.083));
#39458=CARTESIAN_POINT('',(-0.04368363807983,0.0108046177216235,0.083));
#39459=CARTESIAN_POINT('',(-0.0485373756442556,0.0120051308018039,0.083));
#39460=CARTESIAN_POINT('',(0.,0.,0.));
#45463=MECHANICAL_DESIGN_GEOMETRIC_PRESENTATION_REPRESENTATION('',(#13549),#45464);
#45464=(
GEOMETRIC_REPRESENTATION_CONTEXT(3)
GLOBAL_UNCERTAINTY_ASSIGNED_CONTEXT((#45492))
GLOBAL_UNIT_ASSIGNED_CONTEXT((#45522,#45521,#45520))
REPRESENTATION_CONTEXT('MAS-690','TOP_LEVEL_ASSEMBLY_PART')
);
#45485=(
GEOMETRIC_REPRESENTATION_CONTEXT(3)
GLOBAL_UNCERTAINTY_ASSIGNED_CONTEXT((#45513))
GLOBAL_UNIT_ASSIGNED_CONTEXT((#45522,#45521,#45520))
REPRESENTATION_CONTEXT('Bottle','COMPONENT_PART')
);
#45492=UNCERTAINTY_MEASURE_WITH_UNIT(LENGTH_MEASURE(1.E-8),#45522,
'DISTANCE_ACCURACY_VALUE','Maximum Tolerance applied to model');
#45513=UNCERTAINTY_MEASURE_WITH_UNIT(LENGTH_MEASURE(2.E-5),#45522,
'DISTANCE_ACCURACY_VALUE','Maximum Tolerance applied to model');
#45520=(
NAMED_UNIT(*)
SI_UNIT($,.STERADIAN.)
SOLID_ANGLE_UNIT()
);
#45521=(
NAMED_UNIT(*)
PLANE_ANGLE_UNIT()
SI_UNIT($,.RADIAN.)
);
#45522=(
LENGTH_UNIT()
NAMED_UNIT(*)
SI_UNIT($,.METRE.)
);
#45569=PRODUCT_DEFINITION_SHAPE('','',#45606);
#45606=PRODUCT_DEFINITION('','',#45662,#45634);
#45634=PRODUCT_DEFINITION_CONTEXT('',#45782,'design');
#45662=PRODUCT_DEFINITION_FORMATION_WITH_SPECIFIED_SOURCE('','',#45718,
 .NOT_KNOWN.);
#45718=PRODUCT('Bottle','Bottle','Bottle',(#45774));
#45774=PRODUCT_CONTEXT('',#45782,'mechanical');
#45782=APPLICATION_CONTEXT('managed model based 3d engineering');
ENDSEC;
END-ISO-10303-21;
